ISO-10303-21;
HEADER;
FILE_DESCRIPTION (('STEP AP214'),
    '1' );
FILE_NAME ('6266N13_Heavy Duty Locking-Slotted Fitting1_6266N13.step',
    '2026-10-09T16:01:55',
    ( '' ),
    ( '' ),
    'SwSTEP 2.0',
    'SolidWorks 2024',
    '' );
FILE_SCHEMA (( 'AUTOMOTIVE_DESIGN' ));
ENDSEC;

DATA;
#3=PLANE ( 'NONE',  #28714 ) ;
#9=ORIENTED_EDGE ( 'NONE', *, *, #69803, .T. ) ;
#13=ORIENTED_EDGE ( 'NONE', *, *, #42356, .F. ) ;
#15=ADVANCED_FACE ( 'NONE', ( #41711 ), #19784, .T. ) ;
#17=AXIS2_PLACEMENT_3D ( 'NONE', #56008, #906, #7566 ) ;
#27=DIRECTION ( 'NONE',  ( -1.000000000000000000, 1.794541526872559352E-16, 0.000000000000000000 ) ) ;
#44=DIRECTION ( 'NONE',  ( -1.000000000000000000, 0.000000000000000000, 0.000000000000000000 ) ) ;
#50=VERTEX_POINT ( 'NONE', #59375 ) ;
#70=EDGE_CURVE ( 'NONE', #46124, #11076, #48766, .T. ) ;
#71=ADVANCED_FACE ( 'NONE', ( #55074 ), #31476, .T. ) ;
#80=PLANE ( 'NONE',  #21958 ) ;
#88=PLANE ( 'NONE',  #65914 ) ;
#92=FACE_OUTER_BOUND ( 'NONE', #31226, .T. ) ;
#103=CARTESIAN_POINT ( 'NONE',  ( 0.000000000000000000, -8.249999999999998224, -13.50000000000000178 ) ) ;
#127=VERTEX_POINT ( 'NONE', #32847 ) ;
#132=DIRECTION ( 'NONE',  ( 0.000000000000000000, 0.000000000000000000, 1.000000000000000000 ) ) ;
#149=VECTOR ( 'NONE', #1157, 1000.000000000000000 ) ;
#163=CIRCLE ( 'NONE', #63398, 0.1999999999999987899 ) ;
#168=DIRECTION ( 'NONE',  ( 1.000000000000000000, -0.000000000000000000, 0.000000000000000000 ) ) ;
#169=EDGE_LOOP ( 'NONE', ( #39486, #29430, #2363, #22947 ) ) ;
#175=ORIENTED_EDGE ( 'NONE', *, *, #63248, .F. ) ;
#178=CARTESIAN_POINT ( 'NONE',  ( -7.250000000000000888, 7.250000000000001776, -18.00000000000000000 ) ) ;
#180=ORIENTED_EDGE ( 'NONE', *, *, #26893, .F. ) ;
#181=ORIENTED_EDGE ( 'NONE', *, *, #42792, .T. ) ;
#190=VERTEX_POINT ( 'NONE', #61701 ) ;
#196=EDGE_CURVE ( 'NONE', #13160, #36733, #7955, .T. ) ;
#198=DIRECTION ( 'NONE',  ( 1.000000000000000000, 0.000000000000000000, 0.000000000000000000 ) ) ;
#209=CARTESIAN_POINT ( 'NONE',  ( -7.450000000000001954, 0.000000000000000000, -18.00000000000000000 ) ) ;
#214=LINE ( 'NONE', #16474, #66351 ) ;
#219=DIRECTION ( 'NONE',  ( 0.000000000000000000, 0.000000000000000000, -1.000000000000000000 ) ) ;
#224=ORIENTED_EDGE ( 'NONE', *, *, #41153, .T. ) ;
#228=ADVANCED_FACE ( 'NONE', ( #56750 ), #13963, .T. ) ;
#230=DIRECTION ( 'NONE',  ( 0.000000000000000000, 0.000000000000000000, -1.000000000000000000 ) ) ;
#236=LINE ( 'NONE', #68848, #62717 ) ;
#244=CARTESIAN_POINT ( 'NONE',  ( 7.450000000000004619, -1.336933437520057563E-15, -23.00000000000000000 ) ) ;
#246=CARTESIAN_POINT ( 'NONE',  ( 7.250000000000005329, -8.249999999999998224, -20.00000000000000000 ) ) ;
#260=VECTOR ( 'NONE', #28913, 1000.000000000000000 ) ;
#262=ORIENTED_EDGE ( 'NONE', *, *, #61325, .F. ) ;
#272=ADVANCED_FACE ( 'NONE', ( #34467 ), #50744, .F. ) ;
#275=EDGE_CURVE ( 'NONE', #16443, #31143, #40125, .T. ) ;
#279=FACE_OUTER_BOUND ( 'NONE', #56428, .T. ) ;
#285=EDGE_CURVE ( 'NONE', #49229, #23467, #8668, .T. ) ;
#292=FACE_OUTER_BOUND ( 'NONE', #58833, .T. ) ;
#309=DIRECTION ( 'NONE',  ( 1.000000000000000000, 0.000000000000000000, 0.000000000000000000 ) ) ;
#310=CARTESIAN_POINT ( 'NONE',  ( -7.250000000000000888, 8.250000000000001776, -19.50000000000000000 ) ) ;
#313=AXIS2_PLACEMENT_3D ( 'NONE', #44992, #2555, #62301 ) ;
#317=ORIENTED_EDGE ( 'NONE', *, *, #26344, .F. ) ;
#320=CARTESIAN_POINT ( 'NONE',  ( 8.250000000000005329, -7.249999999999998224, -19.50000000000000000 ) ) ;
#327=CARTESIAN_POINT ( 'NONE',  ( -9.689999999999999503, -9.750000000000001776, -5.000000000000000000 ) ) ;
#334=EDGE_CURVE ( 'NONE', #43309, #34406, #4773, .T. ) ;
#338=VECTOR ( 'NONE', #2632, 1000.000000000000000 ) ;
#343=LINE ( 'NONE', #58702, #21159 ) ;
#349=DIRECTION ( 'NONE',  ( -0.000000000000000000, 0.000000000000000000, -1.000000000000000000 ) ) ;
#357=PLANE ( 'NONE',  #20890 ) ;
#380=CARTESIAN_POINT ( 'NONE',  ( 6.500000000000000888, -6.500000000000002665, -1.000000000000000000 ) ) ;
#381=VERTEX_POINT ( 'NONE', #68418 ) ;
#389=PLANE ( 'NONE',  #20249 ) ;
#393=LINE ( 'NONE', #21950, #33380 ) ;
#396=ORIENTED_EDGE ( 'NONE', *, *, #62344, .F. ) ;
#402=ORIENTED_EDGE ( 'NONE', *, *, #57864, .T. ) ;
#403=ADVANCED_FACE ( 'NONE', ( #57802 ), #20668, .T. ) ;
#407=EDGE_CURVE ( 'NONE', #41205, #12761, #63817, .T. ) ;
#411=CYLINDRICAL_SURFACE ( 'NONE', #53076, 0.1999999999999987899 ) ;
#415=VECTOR ( 'NONE', #51891, 1000.000000000000000 ) ;
#419=VECTOR ( 'NONE', #6445, 1000.000000000000000 ) ;
#422=VECTOR ( 'NONE', #20592, 1000.000000000000000 ) ;
#424=EDGE_CURVE ( 'NONE', #60302, #2392, #26333, .T. ) ;
#435=ADVANCED_FACE ( 'NONE', ( #60581 ), #22758, .F. ) ;
#437=DIRECTION ( 'NONE',  ( -1.000000000000000000, 0.000000000000000000, -0.000000000000000000 ) ) ;
#447=CARTESIAN_POINT ( 'NONE',  ( 7.450000000000006395, 7.250000000000000888, -13.00000000000000178 ) ) ;
#448=EDGE_CURVE ( 'NONE', #36079, #28576, #31997, .T. ) ;
#453=VECTOR ( 'NONE', #50729, 1000.000000000000000 ) ;
#454=CARTESIAN_POINT ( 'NONE',  ( 8.250000000000005329, -8.249999999999998224, -26.00000000000001066 ) ) ;
#455=DIRECTION ( 'NONE',  ( -1.000000000000000000, 0.000000000000000000, 0.000000000000000000 ) ) ;
#457=ORIENTED_EDGE ( 'NONE', *, *, #46961, .T. ) ;
#468=ORIENTED_EDGE ( 'NONE', *, *, #39229, .F. ) ;
#471=CARTESIAN_POINT ( 'NONE',  ( -8.250000000000001776, 7.250000000000000888, -18.50000000000000000 ) ) ;
#484=CIRCLE ( 'NONE', #15171, 0.1999999999999996503 ) ;
#491=ORIENTED_EDGE ( 'NONE', *, *, #68790, .F. ) ;
#494=AXIS2_PLACEMENT_3D ( 'NONE', #5103, #65205, #17093 ) ;
#497=CARTESIAN_POINT ( 'NONE',  ( 8.250000000000005329, -8.249999999999998224, -26.00000000000001066 ) ) ;
#500=DIRECTION ( 'NONE',  ( 0.000000000000000000, 0.000000000000000000, -1.000000000000000000 ) ) ;
#501=EDGE_CURVE ( 'NONE', #12761, #21320, #43973, .T. ) ;
#508=ORIENTED_EDGE ( 'NONE', *, *, #1282, .F. ) ;
#509=FACE_OUTER_BOUND ( 'NONE', #40006, .T. ) ;
#511=VECTOR ( 'NONE', #43350, 1000.000000000000000 ) ;
#519=VECTOR ( 'NONE', #50986, 1000.000000000000000 ) ;
#530=CARTESIAN_POINT ( 'NONE',  ( -8.250000000000001776, 0.000000000000000000, -24.00000000000000000 ) ) ;
#532=ORIENTED_EDGE ( 'NONE', *, *, #12088, .T. ) ;
#537=ADVANCED_FACE ( 'NONE', ( #5475 ), #48597, .T. ) ;
#538=CYLINDRICAL_SURFACE ( 'NONE', #54810, 0.2000000000000005107 ) ;
#543=FACE_OUTER_BOUND ( 'NONE', #55140, .T. ) ;
#547=AXIS2_PLACEMENT_3D ( 'NONE', #67792, #14039, #9095 ) ;
#556=ADVANCED_FACE ( 'NONE', ( #509 ), #65220, .T. ) ;
#573=AXIS2_PLACEMENT_3D ( 'NONE', #21075, #15076, #32996 ) ;
#585=DIRECTION ( 'NONE',  ( 1.000000000000000000, -0.000000000000000000, 0.000000000000000000 ) ) ;
#592=DIRECTION ( 'NONE',  ( -1.000000000000000000, 1.794541526872559352E-16, 0.000000000000000000 ) ) ;
#610=ORIENTED_EDGE ( 'NONE', *, *, #34222, .F. ) ;
#619=ORIENTED_EDGE ( 'NONE', *, *, #21968, .F. ) ;
#623=ORIENTED_EDGE ( 'NONE', *, *, #59248, .F. ) ;
#624=DIRECTION ( 'NONE',  ( -0.000000000000000000, -0.000000000000000000, -1.000000000000000000 ) ) ;
#626=CARTESIAN_POINT ( 'NONE',  ( 8.250000000000005329, -7.249999999999998224, -15.50000000000000000 ) ) ;
#628=ORIENTED_EDGE ( 'NONE', *, *, #33674, .F. ) ;
#630=CIRCLE ( 'NONE', #40114, 1.000000000000000000 ) ;
#632=EDGE_LOOP ( 'NONE', ( #12732, #36531, #57400, #6391 ) ) ;
#633=EDGE_CURVE ( 'NONE', #54560, #21685, #40408, .T. ) ;
#636=EDGE_LOOP ( 'NONE', ( #49737, #64125, #34092, #53225 ) ) ;
#643=CARTESIAN_POINT ( 'NONE',  ( 7.250000000000005329, 7.250000000000000888, -7.000000000000000000 ) ) ;
#646=AXIS2_PLACEMENT_3D ( 'NONE', #65623, #39094, #23527 ) ;
#647=CARTESIAN_POINT ( 'NONE',  ( 7.450000000000004619, -1.336933437520057563E-15, -19.50000000000000000 ) ) ;
#662=CIRCLE ( 'NONE', #5214, 0.2000000000000005107 ) ;
#664=ORIENTED_EDGE ( 'NONE', *, *, #67900, .F. ) ;
#668=CARTESIAN_POINT ( 'NONE',  ( 7.250000000000005329, -7.249999999999998224, -15.50000000000000000 ) ) ;
#669=LINE ( 'NONE', #60052, #57064 ) ;
#670=VECTOR ( 'NONE', #11222, 1000.000000000000000 ) ;
#671=CARTESIAN_POINT ( 'NONE',  ( 7.250000000000005329, -7.249999999999998224, -11.00000000000000000 ) ) ;
#691=EDGE_CURVE ( 'NONE', #33692, #7966, #2577, .T. ) ;
#706=ORIENTED_EDGE ( 'NONE', *, *, #9650, .T. ) ;
#707=LINE ( 'NONE', #53756, #64695 ) ;
#716=DIRECTION ( 'NONE',  ( 0.000000000000000000, 0.000000000000000000, 1.000000000000000000 ) ) ;
#718=ORIENTED_EDGE ( 'NONE', *, *, #64493, .F. ) ;
#723=LINE ( 'NONE', #42453, #25543 ) ;
#725=EDGE_CURVE ( 'NONE', #13178, #7022, #29794, .T. ) ;
#727=CARTESIAN_POINT ( 'NONE',  ( -9.690000000000001279, 10.50000000000000178, -4.250000000000000000 ) ) ;
#737=ORIENTED_EDGE ( 'NONE', *, *, #66754, .F. ) ;
#740=DIRECTION ( 'NONE',  ( 0.000000000000000000, 0.000000000000000000, 1.000000000000000000 ) ) ;
#741=CYLINDRICAL_SURFACE ( 'NONE', #16577, 1.000000000000000000 ) ;
#742=DIRECTION ( 'NONE',  ( -1.000000000000000000, 0.000000000000000000, 0.000000000000000000 ) ) ;
#744=EDGE_CURVE ( 'NONE', #11392, #21475, #55291, .T. ) ;
#752=CARTESIAN_POINT ( 'NONE',  ( 7.250000000000005329, -7.249999999999998224, -13.50000000000000178 ) ) ;
#754=DIRECTION ( 'NONE',  ( 0.000000000000000000, 0.000000000000000000, 1.000000000000000000 ) ) ;
#758=CARTESIAN_POINT ( 'NONE',  ( 7.250000000000005329, 7.250000000000000888, -13.50000000000000178 ) ) ;
#764=AXIS2_PLACEMENT_3D ( 'NONE', #53431, #27254, #16981 ) ;
#767=AXIS2_PLACEMENT_3D ( 'NONE', #45596, #44915, #2470 ) ;
#769=VECTOR ( 'NONE', #43138, 1000.000000000000000 ) ;
#778=VECTOR ( 'NONE', #33252, 1000.000000000000000 ) ;
#800=CARTESIAN_POINT ( 'NONE',  ( -7.450000000000001954, -7.249999999999998224, -21.50000000000000000 ) ) ;
#808=ADVANCED_FACE ( 'NONE', ( #69379 ), #15961, .T. ) ;
#826=DIRECTION ( 'NONE',  ( 1.000000000000000000, 0.000000000000000000, 0.000000000000000000 ) ) ;
#828=CARTESIAN_POINT ( 'NONE',  ( 7.250000000000005329, 7.250000000000000888, -15.50000000000000000 ) ) ;
#831=FACE_OUTER_BOUND ( 'NONE', #58240, .T. ) ;
#832=AXIS2_PLACEMENT_3D ( 'NONE', #15080, #68822, #58575 ) ;
#833=CARTESIAN_POINT ( 'NONE',  ( 8.250000000000005329, -7.249999999999998224, -20.50000000000000000 ) ) ;
#835=PLANE ( 'NONE',  #56604 ) ;
#837=LINE ( 'NONE', #29752, #22571 ) ;
#845=LINE ( 'NONE', #43946, #45658 ) ;
#847=EDGE_CURVE ( 'NONE', #21320, #24963, #58871, .T. ) ;
#869=LINE ( 'NONE', #32332, #41210 ) ;
#877=DIRECTION ( 'NONE',  ( 1.000000000000000000, 0.000000000000000000, 0.000000000000000000 ) ) ;
#887=AXIS2_PLACEMENT_3D ( 'NONE', #13239, #40098, #8984 ) ;
#888=CIRCLE ( 'NONE', #18921, 1.000000000000000000 ) ;
#896=FACE_OUTER_BOUND ( 'NONE', #41303, .T. ) ;
#898=ORIENTED_EDGE ( 'NONE', *, *, #30137, .F. ) ;
#904=ORIENTED_EDGE ( 'NONE', *, *, #11775, .T. ) ;
#906=DIRECTION ( 'NONE',  ( 0.000000000000000000, 0.000000000000000000, 1.000000000000000000 ) ) ;
#915=EDGE_LOOP ( 'NONE', ( #60259, #42478, #33687, #25586 ) ) ;
#923=DIRECTION ( 'NONE',  ( 0.000000000000000000, 0.000000000000000000, -1.000000000000000000 ) ) ;
#924=PLANE ( 'NONE',  #11913 ) ;
#942=CARTESIAN_POINT ( 'NONE',  ( 9.690000000000001279, 9.690000000000001279, -4.250000000000000000 ) ) ;
#947=DIRECTION ( 'NONE',  ( 0.000000000000000000, 0.000000000000000000, 1.000000000000000000 ) ) ;
#970=LINE ( 'NONE', #38776, #59466 ) ;
#978=ORIENTED_EDGE ( 'NONE', *, *, #3877, .F. ) ;
#981=LINE ( 'NONE', #11554, #670 ) ;
#997=VERTEX_POINT ( 'NONE', #28668 ) ;
#1000=DIRECTION ( 'NONE',  ( 1.000000000000000000, -5.981805089575194965E-17, 0.000000000000000000 ) ) ;
#1018=LINE ( 'NONE', #27529, #5657 ) ;
#1029=VERTEX_POINT ( 'NONE', #12734 ) ;
#1039=ORIENTED_EDGE ( 'NONE', *, *, #61435, .F. ) ;
#1043=VERTEX_POINT ( 'NONE', #33633 ) ;
#1044=PLANE ( 'NONE',  #51872 ) ;
#1046=FACE_OUTER_BOUND ( 'NONE', #30946, .T. ) ;
#1051=ORIENTED_EDGE ( 'NONE', *, *, #66369, .F. ) ;
#1053=ORIENTED_EDGE ( 'NONE', *, *, #19173, .F. ) ;
#1057=EDGE_CURVE ( 'NONE', #68976, #11076, #69099, .T. ) ;
#1059=ORIENTED_EDGE ( 'NONE', *, *, #53222, .F. ) ;
#1064=ORIENTED_EDGE ( 'NONE', *, *, #26942, .F. ) ;
#1071=AXIS2_PLACEMENT_3D ( 'NONE', #24574, #15367, #42221 ) ;
#1073=CARTESIAN_POINT ( 'NONE',  ( -8.250000000000000000, 7.250000000000001776, -18.00000000000000000 ) ) ;
#1075=CARTESIAN_POINT ( 'NONE',  ( -7.450000000000001954, 0.000000000000000000, -19.50000000000000000 ) ) ;
#1081=DIRECTION ( 'NONE',  ( -1.000000000000000000, 0.000000000000000000, 0.000000000000000000 ) ) ;
#1082=DIRECTION ( 'NONE',  ( 0.000000000000000000, 0.000000000000000000, 1.000000000000000000 ) ) ;
#1085=FACE_BOUND ( 'NONE', #67725, .T. ) ;
#1087=FACE_OUTER_BOUND ( 'NONE', #44944, .T. ) ;
#1091=ORIENTED_EDGE ( 'NONE', *, *, #28712, .T. ) ;
#1097=ORIENTED_EDGE ( 'NONE', *, *, #7601, .T. ) ;
#1100=CYLINDRICAL_SURFACE ( 'NONE', #41565, 0.1999999999999987899 ) ;
#1105=EDGE_LOOP ( 'NONE', ( #737, #1051, #33722, #17043 ) ) ;
#1108=ORIENTED_EDGE ( 'NONE', *, *, #21032, .T. ) ;
#1112=CARTESIAN_POINT ( 'NONE',  ( 8.250000000000005329, -7.249999999999998224, -26.00000000000001066 ) ) ;
#1123=DIRECTION ( 'NONE',  ( 0.000000000000000000, 0.000000000000000000, 1.000000000000000000 ) ) ;
#1134=ORIENTED_EDGE ( 'NONE', *, *, #62305, .F. ) ;
#1140=DIRECTION ( 'NONE',  ( 0.000000000000000000, -1.000000000000000000, 0.000000000000000000 ) ) ;
#1144=DIRECTION ( 'NONE',  ( 0.000000000000000000, 0.000000000000000000, 1.000000000000000000 ) ) ;
#1150=VERTEX_POINT ( 'NONE', #35007 ) ;
#1157=DIRECTION ( 'NONE',  ( 0.000000000000000000, 0.000000000000000000, 1.000000000000000000 ) ) ;
#1163=EDGE_CURVE ( 'NONE', #46897, #43093, #9208, .T. ) ;
#1168=ADVANCED_FACE ( 'NONE', ( #63657 ), #9917, .T. ) ;
#1169=VECTOR ( 'NONE', #44683, 1000.000000000000000 ) ;
#1178=CYLINDRICAL_SURFACE ( 'NONE', #52866, 0.1999999999999987899 ) ;
#1179=CARTESIAN_POINT ( 'NONE',  ( 0.000000000000000000, -8.249999999999998224, -8.000000000000000000 ) ) ;
#1181=VECTOR ( 'NONE', #42615, 1000.000000000000000 ) ;
#1182=DIRECTION ( 'NONE',  ( -1.000000000000000000, 0.000000000000000000, 0.000000000000000000 ) ) ;
#1183=ORIENTED_EDGE ( 'NONE', *, *, #37699, .F. ) ;
#1195=EDGE_LOOP ( 'NONE', ( #63285, #14361, #64812, #8946 ) ) ;
#1196=DIRECTION ( 'NONE',  ( -0.000000000000000000, -0.000000000000000000, 1.000000000000000000 ) ) ;
#1199=PLANE ( 'NONE',  #2400 ) ;
#1208=VERTEX_POINT ( 'NONE', #63300 ) ;
#1216=ADVANCED_FACE ( 'NONE', ( #51993 ), #13796, .T. ) ;
#1219=CARTESIAN_POINT ( 'NONE',  ( -7.250000000000000888, 7.250000000000001776, -22.50000000000000000 ) ) ;
#1229=EDGE_CURVE ( 'NONE', #15828, #25947, #67557, .T. ) ;
#1230=ORIENTED_EDGE ( 'NONE', *, *, #3922, .F. ) ;
#1238=EDGE_CURVE ( 'NONE', #64203, #14678, #3587, .T. ) ;
#1241=FACE_BOUND ( 'NONE', #47229, .T. ) ;
#1250=DIRECTION ( 'NONE',  ( -0.000000000000000000, -0.000000000000000000, 1.000000000000000000 ) ) ;
#1253=DIRECTION ( 'NONE',  ( 0.000000000000000000, -1.000000000000000000, -0.000000000000000000 ) ) ;
#1255=CARTESIAN_POINT ( 'NONE',  ( -8.250000000000001776, 7.250000000000000888, -15.50000000000000000 ) ) ;
#1257=CIRCLE ( 'NONE', #52086, 1.000000000000000000 ) ;
#1261=DIRECTION ( 'NONE',  ( -1.000000000000000000, 0.000000000000000000, 0.000000000000000000 ) ) ;
#1264=CARTESIAN_POINT ( 'NONE',  ( 7.250000000000005329, -7.249999999999998224, -22.50000000000000000 ) ) ;
#1265=CARTESIAN_POINT ( 'NONE',  ( -7.250000000000001776, -7.249999999999998224, -15.50000000000000000 ) ) ;
#1267=DIRECTION ( 'NONE',  ( 0.000000000000000000, 0.000000000000000000, 1.000000000000000000 ) ) ;
#1271=CYLINDRICAL_SURFACE ( 'NONE', #15837, 1.000000000000000000 ) ;
#1273=ADVANCED_FACE ( 'NONE', ( #25114 ), #46671, .T. ) ;
#1274=LINE ( 'NONE', #5889, #51165 ) ;
#1276=VERTEX_POINT ( 'NONE', #3906 ) ;
#1278=DIRECTION ( 'NONE',  ( -1.000000000000000000, 0.000000000000000000, 0.000000000000000000 ) ) ;
#1280=DIRECTION ( 'NONE',  ( 0.000000000000000000, 0.000000000000000000, -1.000000000000000000 ) ) ;
#1282=EDGE_CURVE ( 'NONE', #69741, #32938, #44251, .T. ) ;
#1288=EDGE_CURVE ( 'NONE', #48269, #20561, #46522, .T. ) ;
#1291=AXIS2_PLACEMENT_3D ( 'NONE', #46802, #14634, #58493 ) ;
#1293=FACE_OUTER_BOUND ( 'NONE', #53167, .T. ) ;
#1294=DIRECTION ( 'NONE',  ( 0.000000000000000000, -1.000000000000000000, 0.000000000000000000 ) ) ;
#1299=FACE_OUTER_BOUND ( 'NONE', #3983, .T. ) ;
#1306=ADVANCED_FACE ( 'NONE', ( #32167 ), #15577, .T. ) ;
#1325=DIRECTION ( 'NONE',  ( 0.000000000000000000, 0.000000000000000000, 1.000000000000000000 ) ) ;
#1335=CARTESIAN_POINT ( 'NONE',  ( 7.250000000000005329, 7.250000000000000888, -25.00000000000000000 ) ) ;
#1337=CARTESIAN_POINT ( 'NONE',  ( -7.250000000000000888, 7.250000000000001776, -12.00000000000000000 ) ) ;
#1347=ORIENTED_EDGE ( 'NONE', *, *, #34902, .T. ) ;
#1357=AXIS2_PLACEMENT_3D ( 'NONE', #2836, #24414, #25826 ) ;
#1358=ADVANCED_FACE ( 'NONE', ( #58696 ), #48778, .F. ) ;
#1382=FACE_BOUND ( 'NONE', #14584, .T. ) ;
#1397=DIRECTION ( 'NONE',  ( -0.000000000000000000, 0.000000000000000000, 1.000000000000000000 ) ) ;
#1398=DIRECTION ( 'NONE',  ( -1.000000000000000000, 0.000000000000000000, 0.000000000000000000 ) ) ;
#1399=LINE ( 'NONE', #17309, #22646 ) ;
#1402=VECTOR ( 'NONE', #11116, 1000.000000000000000 ) ;
#1415=DIRECTION ( 'NONE',  ( 0.000000000000000000, 0.000000000000000000, -1.000000000000000000 ) ) ;
#1424=DIRECTION ( 'NONE',  ( -1.000000000000000000, 0.000000000000000000, 0.000000000000000000 ) ) ;
#1428=DIRECTION ( 'NONE',  ( -0.000000000000000000, -0.000000000000000000, 1.000000000000000000 ) ) ;
#1432=PLANE ( 'NONE',  #65466 ) ;
#1433=EDGE_CURVE ( 'NONE', #8412, #16770, #34213, .T. ) ;
#1437=ORIENTED_EDGE ( 'NONE', *, *, #39757, .F. ) ;
#1442=CARTESIAN_POINT ( 'NONE',  ( 8.250000000000005329, -8.249999999999998224, -26.00000000000001066 ) ) ;
#1443=LINE ( 'NONE', #23016, #34040 ) ;
#1446=ORIENTED_EDGE ( 'NONE', *, *, #33690, .T. ) ;
#1451=CIRCLE ( 'NONE', #53416, 0.9999999999999991118 ) ;
#1453=ADVANCED_FACE ( 'NONE', ( #33197 ), #12649, .F. ) ;
#1460=DIRECTION ( 'NONE',  ( -0.000000000000000000, -0.000000000000000000, -1.000000000000000000 ) ) ;
#1464=AXIS2_PLACEMENT_3D ( 'NONE', #40636, #35310, #45228 ) ;
#1471=FACE_OUTER_BOUND ( 'NONE', #21863, .T. ) ;
#1474=ORIENTED_EDGE ( 'NONE', *, *, #23405, .F. ) ;
#1476=DIRECTION ( 'NONE',  ( 0.000000000000000000, 0.000000000000000000, -1.000000000000000000 ) ) ;
#1480=CARTESIAN_POINT ( 'NONE',  ( 7.250000000000005329, -7.249999999999998224, -24.00000000000000000 ) ) ;
#1512=( NAMED_UNIT ( * ) PLANE_ANGLE_UNIT ( ) SI_UNIT ( $, .RADIAN. ) );
#1515=EDGE_LOOP ( 'NONE', ( #52071, #22197, #20017, #42552 ) ) ;
#1522=LINE ( 'NONE', #33370, #9492 ) ;
#1528=DIRECTION ( 'NONE',  ( 0.000000000000000000, -1.000000000000000000, 0.000000000000000000 ) ) ;
#1542=CARTESIAN_POINT ( 'NONE',  ( 7.250000000000005329, -8.249999999999998224, -19.50000000000000000 ) ) ;
#1551=ORIENTED_EDGE ( 'NONE', *, *, #30265, .T. ) ;
#1555=VECTOR ( 'NONE', #67629, 1000.000000000000000 ) ;
#1558=EDGE_LOOP ( 'NONE', ( #62226, #31483, #47154, #67223 ) ) ;
#1560=CARTESIAN_POINT ( 'NONE',  ( -9.690000000000001279, 10.50000000000000178, -5.000000000000000000 ) ) ;
#1563=CARTESIAN_POINT ( 'NONE',  ( -7.450000000000001954, 0.000000000000000000, -21.00000000000000000 ) ) ;
#1571=CARTESIAN_POINT ( 'NONE',  ( -7.250000000000000888, -8.249999999999998224, -26.00000000000001066 ) ) ;
#1586=LINE ( 'NONE', #17861, #34253 ) ;
#1597=DIRECTION ( 'NONE',  ( 0.000000000000000000, 0.000000000000000000, -1.000000000000000000 ) ) ;
#1600=DIRECTION ( 'NONE',  ( 0.000000000000000000, 0.000000000000000000, -1.000000000000000000 ) ) ;
#1606=DIRECTION ( 'NONE',  ( 0.000000000000000000, 0.000000000000000000, -1.000000000000000000 ) ) ;
#1617=ORIENTED_EDGE ( 'NONE', *, *, #28712, .F. ) ;
#1626=ORIENTED_EDGE ( 'NONE', *, *, #18494, .T. ) ;
#1629=ORIENTED_EDGE ( 'NONE', *, *, #51776, .T. ) ;
#1631=VECTOR ( 'NONE', #48674, 1000.000000000000000 ) ;
#1635=CARTESIAN_POINT ( 'NONE',  ( -7.450000000000001954, 0.000000000000000000, -12.50000000000000000 ) ) ;
#1637=EDGE_LOOP ( 'NONE', ( #57088, #33379, #39872, #24268 ) ) ;
#1642=ORIENTED_EDGE ( 'NONE', *, *, #69015, .T. ) ;
#1646=CARTESIAN_POINT ( 'NONE',  ( -8.250000000000000000, 7.250000000000001776, -11.00000000000000000 ) ) ;
#1648=CIRCLE ( 'NONE', #34395, 0.1999999999999987899 ) ;
#1662=FACE_OUTER_BOUND ( 'NONE', #48471, .T. ) ;
#1666=EDGE_LOOP ( 'NONE', ( #15251, #59650 ) ) ;
#1670=CARTESIAN_POINT ( 'NONE',  ( -7.450000000000001954, 0.000000000000000000, -21.50000000000000000 ) ) ;
#1677=ORIENTED_EDGE ( 'NONE', *, *, #36142, .F. ) ;
#1684=ADVANCED_FACE ( 'NONE', ( #30332, #51905 ), #47297, .F. ) ;
#1685=EDGE_CURVE ( 'NONE', #67031, #20195, #1257, .T. ) ;
#1686=DIRECTION ( 'NONE',  ( 0.000000000000000000, 0.000000000000000000, -1.000000000000000000 ) ) ;
#1688=DIRECTION ( 'NONE',  ( 0.000000000000000000, 0.000000000000000000, -1.000000000000000000 ) ) ;
#1693=AXIS2_PLACEMENT_3D ( 'NONE', #11004, #37878, #59442 ) ;
#1696=EDGE_CURVE ( 'NONE', #66712, #58124, #15482, .T. ) ;
#1698=ORIENTED_EDGE ( 'NONE', *, *, #19092, .T. ) ;
#1699=DIRECTION ( 'NONE',  ( 0.000000000000000000, 0.000000000000000000, -1.000000000000000000 ) ) ;
#1717=VECTOR ( 'NONE', #40181, 1000.000000000000000 ) ;
#1725=DIRECTION ( 'NONE',  ( 0.000000000000000000, 1.000000000000000000, 0.000000000000000000 ) ) ;
#1733=VECTOR ( 'NONE', #60060, 1000.000000000000000 ) ;
#1736=FACE_BOUND ( 'NONE', #15930, .T. ) ;
#1754=ADVANCED_FACE ( 'NONE', ( #26086 ), #10508, .F. ) ;
#1758=EDGE_CURVE ( 'NONE', #28928, #18073, #29509, .T. ) ;
#1762=CARTESIAN_POINT ( 'NONE',  ( 7.250000000000005329, 7.250000000000000888, -26.00000000000001066 ) ) ;
#1764=CARTESIAN_POINT ( 'NONE',  ( 8.250000000000005329, 0.000000000000000000, -22.50000000000000000 ) ) ;
#1765=EDGE_LOOP ( 'NONE', ( #69753, #46852, #22162, #36717 ) ) ;
#1774=ADVANCED_FACE ( 'NONE', ( #16166 ), #10162, .T. ) ;
#1779=FACE_OUTER_BOUND ( 'NONE', #3037, .T. ) ;
#1781=CARTESIAN_POINT ( 'NONE',  ( -7.250000000000001776, -7.249999999999998224, -21.50000000000000000 ) ) ;
#1784=ORIENTED_EDGE ( 'NONE', *, *, #54013, .T. ) ;
#1786=AXIS2_PLACEMENT_3D ( 'NONE', #9014, #47217, #36238 ) ;
#1790=EDGE_LOOP ( 'NONE', ( #57606, #59148, #46088, #2843 ) ) ;
#1792=DIRECTION ( 'NONE',  ( 1.000000000000000000, 0.000000000000000000, 0.000000000000000000 ) ) ;
#1797=VECTOR ( 'NONE', #20042, 1000.000000000000000 ) ;
#1816=AXIS2_PLACEMENT_3D ( 'NONE', #7213, #50703, #50008 ) ;
#1818=CARTESIAN_POINT ( 'NONE',  ( 7.250000000000005329, -7.249999999999998224, -8.500000000000000000 ) ) ;
#1820=ORIENTED_EDGE ( 'NONE', *, *, #43998, .T. ) ;
#1822=DIRECTION ( 'NONE',  ( 0.000000000000000000, 0.000000000000000000, -1.000000000000000000 ) ) ;
#1830=DIRECTION ( 'NONE',  ( -1.000000000000000000, 0.000000000000000000, 0.000000000000000000 ) ) ;
#1847=EDGE_CURVE ( 'NONE', #52946, #36081, #39115, .T. ) ;
#1848=EDGE_CURVE ( 'NONE', #62579, #21671, #44749, .T. ) ;
#1851=LINE ( 'NONE', #23424, #50706 ) ;
#1864=ORIENTED_EDGE ( 'NONE', *, *, #57969, .T. ) ;
#1868=( LENGTH_UNIT ( ) NAMED_UNIT ( * ) SI_UNIT ( .MILLI., .METRE. ) );
#1873=CARTESIAN_POINT ( 'NONE',  ( 7.450000000000006395, 7.250000000000000888, -20.50000000000000000 ) ) ;
#1886=ADVANCED_FACE ( 'NONE', ( #56075 ), #49723, .T. ) ;
#1889=CARTESIAN_POINT ( 'NONE',  ( 8.250000000000005329, 8.250000000000001776, -26.00000000000001066 ) ) ;
#1897=ORIENTED_EDGE ( 'NONE', *, *, #9600, .T. ) ;
#1905=DIRECTION ( 'NONE',  ( 0.000000000000000000, 0.000000000000000000, -1.000000000000000000 ) ) ;
#1907=VECTOR ( 'NONE', #23645, 1000.000000000000000 ) ;
#1909=ORIENTED_EDGE ( 'NONE', *, *, #6875, .T. ) ;
#1911=VERTEX_POINT ( 'NONE', #55727 ) ;
#1920=CARTESIAN_POINT ( 'NONE',  ( -7.250000000000001776, -7.249999999999998224, -24.50000000000000000 ) ) ;
#1921=DIRECTION ( 'NONE',  ( 0.000000000000000000, 1.000000000000000000, 0.000000000000000000 ) ) ;
#1926=DIRECTION ( 'NONE',  ( 0.000000000000000000, 0.000000000000000000, 1.000000000000000000 ) ) ;
#1927=PLANE ( 'NONE',  #35705 ) ;
#1939=EDGE_CURVE ( 'NONE', #21232, #11735, #66678, .T. ) ;
#1959=VECTOR ( 'NONE', #10259, 1000.000000000000000 ) ;
#1961=ORIENTED_EDGE ( 'NONE', *, *, #27199, .F. ) ;
#1967=ORIENTED_EDGE ( 'NONE', *, *, #37147, .T. ) ;
#1975=ORIENTED_EDGE ( 'NONE', *, *, #6677, .T. ) ;
#1980=CARTESIAN_POINT ( 'NONE',  ( 7.250000000000005329, 7.250000000000000888, -23.50000000000000000 ) ) ;
#1981=DIRECTION ( 'NONE',  ( 0.000000000000000000, 1.000000000000000000, 0.000000000000000000 ) ) ;
#1991=ORIENTED_EDGE ( 'NONE', *, *, #21479, .T. ) ;
#2000=AXIS2_PLACEMENT_3D ( 'NONE', #65464, #17351, #33284 ) ;
#2003=LINE ( 'NONE', #24627, #50876 ) ;
#2007=CIRCLE ( 'NONE', #27961, 0.1999999999999996503 ) ;
#2011=DIRECTION ( 'NONE',  ( 0.000000000000000000, 0.000000000000000000, -1.000000000000000000 ) ) ;
#2015=FACE_OUTER_BOUND ( 'NONE', #59268, .T. ) ;
#2016=EDGE_CURVE ( 'NONE', #55203, #57776, #46157, .T. ) ;
#2020=ORIENTED_EDGE ( 'NONE', *, *, #22789, .F. ) ;
#2024=CYLINDRICAL_SURFACE ( 'NONE', #64138, 0.2000000000000005107 ) ;
#2027=ADVANCED_FACE ( 'NONE', ( #51819 ), #8321, .T. ) ;
#2044=CARTESIAN_POINT ( 'NONE',  ( 9.750000000000000000, -9.690000000000001279, -4.250000000000000000 ) ) ;
#2045=CARTESIAN_POINT ( 'NONE',  ( -7.250000000000000888, 7.250000000000001776, -14.00000000000000000 ) ) ;
#2047=ORIENTED_EDGE ( 'NONE', *, *, #25845, .T. ) ;
#2049=DIRECTION ( 'NONE',  ( 1.000000000000000000, 0.000000000000000000, 0.000000000000000000 ) ) ;
#2063=VERTEX_POINT ( 'NONE', #63126 ) ;
#2078=EDGE_CURVE ( 'NONE', #5855, #17298, #46421, .T. ) ;
#2079=CARTESIAN_POINT ( 'NONE',  ( -7.450000000000001954, -7.249999999999998224, -15.00000000000000000 ) ) ;
#2081=CARTESIAN_POINT ( 'NONE',  ( -7.450000000000001954, -7.249999999999998224, -15.50000000000000000 ) ) ;
#2082=DIRECTION ( 'NONE',  ( 0.000000000000000000, -0.000000000000000000, 1.000000000000000000 ) ) ;
#2083=ORIENTED_EDGE ( 'NONE', *, *, #62101, .F. ) ;
#2085=EDGE_LOOP ( 'NONE', ( #62596, #47715, #4125, #262 ) ) ;
#2088=CARTESIAN_POINT ( 'NONE',  ( 7.250000000000005329, 7.250000000000000888, -17.00000000000000000 ) ) ;
#2091=ADVANCED_FACE ( 'NONE', ( #57116, #8684 ), #30257, .F. ) ;
#2092=EDGE_LOOP ( 'NONE', ( #50879, #11296, #52153, #39882 ) ) ;
#2096=ORIENTED_EDGE ( 'NONE', *, *, #38243, .F. ) ;
#2099=CARTESIAN_POINT ( 'NONE',  ( -7.250000000000000888, 7.250000000000001776, -18.00000000000000000 ) ) ;
#2100=EDGE_CURVE ( 'NONE', #59106, #61047, #48858, .T. ) ;
#2107=CARTESIAN_POINT ( 'NONE',  ( -7.250000000000000888, 7.450000000000003730, -12.50000000000000000 ) ) ;
#2109=DIRECTION ( 'NONE',  ( 0.000000000000000000, 0.000000000000000000, -1.000000000000000000 ) ) ;
#2111=CARTESIAN_POINT ( 'NONE',  ( 7.250000000000005329, 8.250000000000001776, -19.00000000000000000 ) ) ;
#2112=EDGE_CURVE ( 'NONE', #6054, #21483, #22689, .T. ) ;
#2114=DIRECTION ( 'NONE',  ( 1.000000000000000000, 0.000000000000000000, 0.000000000000000000 ) ) ;
#2122=DIRECTION ( 'NONE',  ( -1.000000000000000000, 0.000000000000000000, 0.000000000000000000 ) ) ;
#2126=ORIENTED_EDGE ( 'NONE', *, *, #11507, .T. ) ;
#2128=DIRECTION ( 'NONE',  ( 1.000000000000000000, 0.000000000000000000, 0.000000000000000000 ) ) ;
#2131=FACE_OUTER_BOUND ( 'NONE', #52391, .T. ) ;
#2134=ORIENTED_EDGE ( 'NONE', *, *, #60821, .F. ) ;
#2135=ORIENTED_EDGE ( 'NONE', *, *, #36829, .T. ) ;
#2145=VERTEX_POINT ( 'NONE', #800 ) ;
#2149=DIRECTION ( 'NONE',  ( -1.000000000000000000, 2.602085213965213008E-15, 0.000000000000000000 ) ) ;
#2150=DIRECTION ( 'NONE',  ( -0.000000000000000000, -0.000000000000000000, -1.000000000000000000 ) ) ;
#2153=LINE ( 'NONE', #61900, #46929 ) ;
#2161=EDGE_LOOP ( 'NONE', ( #1446, #41553, #21929, #49721 ) ) ;
#2164=DIRECTION ( 'NONE',  ( -0.000000000000000000, -0.000000000000000000, 1.000000000000000000 ) ) ;
#2168=EDGE_LOOP ( 'NONE', ( #23384, #4521, #24581, #34063 ) ) ;
#2171=AXIS2_PLACEMENT_3D ( 'NONE', #40725, #66546, #67248 ) ;
#2187=EDGE_LOOP ( 'NONE', ( #7754, #52608, #38102, #50654 ) ) ;
#2190=CARTESIAN_POINT ( 'NONE',  ( -8.250000000000001776, -7.249999999999998224, -21.00000000000000000 ) ) ;
#2210=CARTESIAN_POINT ( 'NONE',  ( -7.250000000000000888, 7.450000000000003730, -18.00000000000000000 ) ) ;
#2211=CARTESIAN_POINT ( 'NONE',  ( 7.250000000000005329, -7.249999999999998224, -20.50000000000000000 ) ) ;
#2213=FACE_BOUND ( 'NONE', #64525, .T. ) ;
#2218=DIRECTION ( 'NONE',  ( 0.000000000000000000, -1.000000000000000000, 0.000000000000000000 ) ) ;
#2225=ORIENTED_EDGE ( 'NONE', *, *, #20728, .F. ) ;
#2226=ORIENTED_EDGE ( 'NONE', *, *, #54155, .F. ) ;
#2231=DIRECTION ( 'NONE',  ( -1.000000000000000000, 0.000000000000000000, 0.000000000000000000 ) ) ;
#2232=DIRECTION ( 'NONE',  ( 0.000000000000000000, 0.000000000000000000, 1.000000000000000000 ) ) ;
#2239=ADVANCED_FACE ( 'NONE', ( #28329 ), #19119, .T. ) ;
#2243=ORIENTED_EDGE ( 'NONE', *, *, #19085, .T. ) ;
#2247=EDGE_CURVE ( 'NONE', #11267, #58003, #18402, .T. ) ;
#2251=CARTESIAN_POINT ( 'NONE',  ( -7.450000000000001954, -7.249999999999998224, -9.000000000000001776 ) ) ;
#2261=VERTEX_POINT ( 'NONE', #39292 ) ;
#2266=CARTESIAN_POINT ( 'NONE',  ( -7.250000000000000888, 7.450000000000003730, -25.50000000000000355 ) ) ;
#2268=AXIS2_PLACEMENT_3D ( 'NONE', #16757, #38326, #64167 ) ;
#2269=PLANE ( 'NONE',  #43619 ) ;
#2270=CARTESIAN_POINT ( 'NONE',  ( -7.250000000000000888, 7.450000000000003730, -7.500000000000000000 ) ) ;
#2272=CARTESIAN_POINT ( 'NONE',  ( -7.250000000000000888, 7.250000000000001776, -16.50000000000000000 ) ) ;
#2274=ORIENTED_EDGE ( 'NONE', *, *, #51239, .T. ) ;
#2279=DIRECTION ( 'NONE',  ( 0.000000000000000000, 0.000000000000000000, 1.000000000000000000 ) ) ;
#2282=EDGE_CURVE ( 'NONE', #18722, #29792, #61186, .T. ) ;
#2283=PLANE ( 'NONE',  #26407 ) ;
#2286=ORIENTED_EDGE ( 'NONE', *, *, #28874, .T. ) ;
#2289=FACE_BOUND ( 'NONE', #31446, .T. ) ;
#2290=LINE ( 'NONE', #34443, #44964 ) ;
#2291=ADVANCED_FACE ( 'NONE', ( #2502 ), #55217, .T. ) ;
#2292=ADVANCED_FACE ( 'NONE', ( #44943 ), #34314, .F. ) ;
#2293=ORIENTED_EDGE ( 'NONE', *, *, #51053, .T. ) ;
#2295=PLANE ( 'NONE',  #37676 ) ;
#2304=CARTESIAN_POINT ( 'NONE',  ( 0.000000000000000000, -8.249999999999998224, -21.50000000000000000 ) ) ;
#2309=DIRECTION ( 'NONE',  ( -5.981805089575196197E-17, -1.000000000000000000, 0.000000000000000000 ) ) ;
#2314=CARTESIAN_POINT ( 'NONE',  ( 8.250000000000005329, -8.249999999999998224, -26.00000000000001066 ) ) ;
#2334=VECTOR ( 'NONE', #12590, 1000.000000000000000 ) ;
#2339=VERTEX_POINT ( 'NONE', #45627 ) ;
#2353=AXIS2_PLACEMENT_3D ( 'NONE', #35085, #12474, #55625 ) ;
#2356=DIRECTION ( 'NONE',  ( 0.000000000000000000, 0.000000000000000000, -1.000000000000000000 ) ) ;
#2360=DIRECTION ( 'NONE',  ( 1.000000000000000000, 0.000000000000000000, 0.000000000000000000 ) ) ;
#2363=ORIENTED_EDGE ( 'NONE', *, *, #27751, .F. ) ;
#2367=ADVANCED_FACE ( 'NONE', ( #58002 ), #26186, .F. ) ;
#2369=CARTESIAN_POINT ( 'NONE',  ( -7.450000000000001954, 7.250000000000000000, -17.50000000000000000 ) ) ;
#2371=EDGE_CURVE ( 'NONE', #4784, #36435, #56940, .T. ) ;
#2375=PLANE ( 'NONE',  #28245 ) ;
#2381=CARTESIAN_POINT ( 'NONE',  ( 7.250000000000005329, 7.250000000000000888, -20.00000000000000000 ) ) ;
#2390=CARTESIAN_POINT ( 'NONE',  ( 0.000000000000000000, -8.749999999999998224, -26.00000000000001066 ) ) ;
#2392=VERTEX_POINT ( 'NONE', #47741 ) ;
#2397=ORIENTED_EDGE ( 'NONE', *, *, #30198, .F. ) ;
#2398=FACE_OUTER_BOUND ( 'NONE', #46831, .T. ) ;
#2400=AXIS2_PLACEMENT_3D ( 'NONE', #42936, #53913, #22423 ) ;
#2409=EDGE_CURVE ( 'NONE', #54217, #10955, #51106, .T. ) ;
#2413=EDGE_CURVE ( 'NONE', #3133, #53573, #22890, .T. ) ;
#2415=VERTEX_POINT ( 'NONE', #57652 ) ;
#2416=CARTESIAN_POINT ( 'NONE',  ( -7.450000000000001954, 7.250000000000000000, -15.50000000000000000 ) ) ;
#2420=ORIENTED_EDGE ( 'NONE', *, *, #58009, .T. ) ;
#2430=ORIENTED_EDGE ( 'NONE', *, *, #3927, .T. ) ;
#2435=LINE ( 'NONE', #28605, #32407 ) ;
#2438=LINE ( 'NONE', #51223, #26802 ) ;
#2450=DIRECTION ( 'NONE',  ( -0.000000000000000000, 0.000000000000000000, 1.000000000000000000 ) ) ;
#2455=DIRECTION ( 'NONE',  ( -1.000000000000000000, 0.000000000000000000, 0.000000000000000000 ) ) ;
#2470=DIRECTION ( 'NONE',  ( -1.000000000000000000, 0.000000000000000000, 0.000000000000000000 ) ) ;
#2477=VERTEX_POINT ( 'NONE', #36434 ) ;
#2479=VERTEX_POINT ( 'NONE', #25839 ) ;
#2481=AXIS2_PLACEMENT_3D ( 'NONE', #21834, #28173, #43392 ) ;
#2497=VECTOR ( 'NONE', #23027, 1000.000000000000000 ) ;
#2502=FACE_OUTER_BOUND ( 'NONE', #50544, .T. ) ;
#2505=ORIENTED_EDGE ( 'NONE', *, *, #70, .F. ) ;
#2506=VECTOR ( 'NONE', #69563, 1000.000000000000000 ) ;
#2522=DIRECTION ( 'NONE',  ( 1.000000000000000000, 0.000000000000000000, 0.000000000000000000 ) ) ;
#2527=DIRECTION ( 'NONE',  ( -1.000000000000000000, 0.000000000000000000, 0.000000000000000000 ) ) ;
#2542=CARTESIAN_POINT ( 'NONE',  ( 7.250000000000005329, 7.250000000000000888, -18.00000000000000000 ) ) ;
#2545=EDGE_CURVE ( 'NONE', #47184, #28252, #707, .T. ) ;
#2549=ORIENTED_EDGE ( 'NONE', *, *, #41455, .T. ) ;
#2555=DIRECTION ( 'NONE',  ( 0.000000000000000000, -1.000000000000000000, -0.000000000000000000 ) ) ;
#2557=EDGE_LOOP ( 'NONE', ( #44770, #32187, #8325, #48343, #63761, #17815, #62283, #18705 ) ) ;
#2558=DIRECTION ( 'NONE',  ( 0.000000000000000000, 0.000000000000000000, 1.000000000000000000 ) ) ;
#2565=DIRECTION ( 'NONE',  ( 1.000000000000000000, 0.000000000000000000, 0.000000000000000000 ) ) ;
#2566=ORIENTED_EDGE ( 'NONE', *, *, #50955, .F. ) ;
#2567=CARTESIAN_POINT ( 'NONE',  ( -7.250000000000000888, 7.250000000000001776, -20.00000000000000000 ) ) ;
#2568=AXIS2_PLACEMENT_3D ( 'NONE', #22917, #50483, #12979 ) ;
#2572=CARTESIAN_POINT ( 'NONE',  ( 8.250000000000005329, 8.250000000000001776, -26.00000000000001066 ) ) ;
#2577=LINE ( 'NONE', #44651, #35107 ) ;
#2580=ORIENTED_EDGE ( 'NONE', *, *, #11812, .F. ) ;
#2581=LINE ( 'NONE', #24151, #30320 ) ;
#2582=DIRECTION ( 'NONE',  ( 1.000000000000000000, 0.000000000000000000, -0.000000000000000000 ) ) ;
#2585=CARTESIAN_POINT ( 'NONE',  ( 7.250000000000005329, 7.250000000000000888, -14.50000000000000000 ) ) ;
#2587=EDGE_LOOP ( 'NONE', ( #29678, #44585, #8119, #42358 ) ) ;
#2595=CARTESIAN_POINT ( 'NONE',  ( -7.250000000000000888, 8.250000000000001776, -26.00000000000001066 ) ) ;
#2596=EDGE_CURVE ( 'NONE', #28581, #54560, #38196, .T. ) ;
#2599=ORIENTED_EDGE ( 'NONE', *, *, #57099, .T. ) ;
#2603=EDGE_LOOP ( 'NONE', ( #9284, #22098, #66841, #24413 ) ) ;
#2604=EDGE_LOOP ( 'NONE', ( #30349, #21481, #8721, #31210 ) ) ;
#2619=VECTOR ( 'NONE', #5543, 1000.000000000000000 ) ;
#2621=DIRECTION ( 'NONE',  ( 1.000000000000000000, 0.000000000000000000, 0.000000000000000000 ) ) ;
#2627=CARTESIAN_POINT ( 'NONE',  ( 8.250000000000005329, -7.249999999999998224, -20.00000000000000000 ) ) ;
#2632=DIRECTION ( 'NONE',  ( -1.000000000000000000, 0.000000000000000000, 0.000000000000000000 ) ) ;
#2645=DIRECTION ( 'NONE',  ( -0.000000000000000000, -0.000000000000000000, 1.000000000000000000 ) ) ;
#2646=VERTEX_POINT ( 'NONE', #6681 ) ;
#2653=ORIENTED_EDGE ( 'NONE', *, *, #691, .F. ) ;
#2655=ORIENTED_EDGE ( 'NONE', *, *, #55583, .F. ) ;
#2656=VECTOR ( 'NONE', #54838, 1000.000000000000000 ) ;
#2670=ORIENTED_EDGE ( 'NONE', *, *, #56541, .T. ) ;
#2671=DIRECTION ( 'NONE',  ( -1.000000000000000000, 0.000000000000000000, 0.000000000000000000 ) ) ;
#2673=CARTESIAN_POINT ( 'NONE',  ( 7.250000000000005329, -7.449999999999998401, -17.00000000000000000 ) ) ;
#2684=ORIENTED_EDGE ( 'NONE', *, *, #42449, .F. ) ;
#2689=CARTESIAN_POINT ( 'NONE',  ( 7.250000000000005329, -8.249999999999998224, -23.50000000000000000 ) ) ;
#2693=CARTESIAN_POINT ( 'NONE',  ( -8.250000000000001776, -7.249999999999998224, -25.00000000000000000 ) ) ;
#2705=AXIS2_PLACEMENT_3D ( 'NONE', #68691, #36871, #20929 ) ;
#2714=ORIENTED_EDGE ( 'NONE', *, *, #49535, .F. ) ;
#2722=CARTESIAN_POINT ( 'NONE',  ( -7.450000000000001954, 0.000000000000000000, -7.000000000000000000 ) ) ;
#2724=LINE ( 'NONE', #57178, #51191 ) ;
#2729=CARTESIAN_POINT ( 'NONE',  ( 7.250000000000005329, 8.250000000000001776, -21.00000000000000000 ) ) ;
#2731=DIRECTION ( 'NONE',  ( 0.000000000000000000, 0.000000000000000000, 1.000000000000000000 ) ) ;
#2734=VERTEX_POINT ( 'NONE', #23982 ) ;
#2739=ORIENTED_EDGE ( 'NONE', *, *, #17158, .T. ) ;
#2746=EDGE_LOOP ( 'NONE', ( #41710, #2684, #54465, #30416 ) ) ;
#2749=ORIENTED_EDGE ( 'NONE', *, *, #59616, .T. ) ;
#2774=DIRECTION ( 'NONE',  ( 0.000000000000000000, 0.000000000000000000, 1.000000000000000000 ) ) ;
#2775=CIRCLE ( 'NONE', #13550, 1.500000000000000444 ) ;
#2780=CYLINDRICAL_SURFACE ( 'NONE', #16505, 0.2000000000000005107 ) ;
#2784=DIRECTION ( 'NONE',  ( 1.000000000000000000, 0.000000000000000000, 0.000000000000000000 ) ) ;
#2802=CARTESIAN_POINT ( 'NONE',  ( -7.250000000000000888, 7.250000000000001776, -21.50000000000000000 ) ) ;
#2810=EDGE_CURVE ( 'NONE', #40458, #40971, #67490, .T. ) ;
#2816=DIRECTION ( 'NONE',  ( 0.000000000000000000, 0.000000000000000000, 1.000000000000000000 ) ) ;
#2833=DIRECTION ( 'NONE',  ( -1.000000000000000000, 0.000000000000000000, 0.000000000000000000 ) ) ;
#2834=ORIENTED_EDGE ( 'NONE', *, *, #7554, .F. ) ;
#2836=CARTESIAN_POINT ( 'NONE',  ( -7.250000000000000888, 7.250000000000001776, -13.50000000000000178 ) ) ;
#2838=ORIENTED_EDGE ( 'NONE', *, *, #50383, .F. ) ;
#2841=CARTESIAN_POINT ( 'NONE',  ( -7.250000000000000888, 8.250000000000001776, -26.00000000000001066 ) ) ;
#2843=ORIENTED_EDGE ( 'NONE', *, *, #43763, .T. ) ;
#2844=CARTESIAN_POINT ( 'NONE',  ( -9.690000000000001279, 10.50000000000000000, 0.000000000000000000 ) ) ;
#2851=EDGE_LOOP ( 'NONE', ( #17852, #14614, #51041, #19801, #22167, #60121, #33535, #32845 ) ) ;
#2859=CARTESIAN_POINT ( 'NONE',  ( 0.000000000000000000, -7.449999999999998401, -19.00000000000000000 ) ) ;
#2864=EDGE_CURVE ( 'NONE', #53691, #10351, #6052, .T. ) ;
#2865=CYLINDRICAL_SURFACE ( 'NONE', #11702, 1.500000000000000444 ) ;
#2898=CARTESIAN_POINT ( 'NONE',  ( -7.250000000000000888, 7.250000000000001776, -26.00000000000001066 ) ) ;
#2908=ADVANCED_FACE ( 'NONE', ( #51917, #3480 ), #68171, .T. ) ;
#2915=CARTESIAN_POINT ( 'NONE',  ( -8.250000000000001776, 7.250000000000000888, -22.50000000000000000 ) ) ;
#2923=CARTESIAN_POINT ( 'NONE',  ( 7.250000000000005329, -7.449999999999998401, -16.50000000000000000 ) ) ;
#2927=VERTEX_POINT ( 'NONE', #24575 ) ;
#2929=DIRECTION ( 'NONE',  ( -1.794541526872559352E-16, -1.000000000000000000, 0.000000000000000000 ) ) ;
#2932=DIRECTION ( 'NONE',  ( 0.000000000000000000, 0.000000000000000000, -1.000000000000000000 ) ) ;
#2933=DIRECTION ( 'NONE',  ( 1.000000000000000000, 0.000000000000000000, 0.000000000000000000 ) ) ;
#2935=FACE_OUTER_BOUND ( 'NONE', #41692, .T. ) ;
#2940=ORIENTED_EDGE ( 'NONE', *, *, #28231, .T. ) ;
#2941=ORIENTED_EDGE ( 'NONE', *, *, #46000, .T. ) ;
#2944=CARTESIAN_POINT ( 'NONE',  ( 0.000000000000000000, -7.449999999999998401, -21.00000000000000000 ) ) ;
#2946=CARTESIAN_POINT ( 'NONE',  ( 7.250000000000005329, -8.249999999999998224, -12.50000000000000000 ) ) ;
#2956=ORIENTED_EDGE ( 'NONE', *, *, #12121, .T. ) ;
#2982=EDGE_CURVE ( 'NONE', #25281, #14316, #55359, .T. ) ;
#2986=TOROIDAL_SURFACE ( 'NONE', #21058, 0.06000000000000080963, 0.7500000000000000000 ) ;
#2993=EDGE_CURVE ( 'NONE', #66919, #61999, #62493, .T. ) ;
#2994=ORIENTED_EDGE ( 'NONE', *, *, #3222, .T. ) ;
#3009=CARTESIAN_POINT ( 'NONE',  ( -7.250000000000000888, 7.250000000000001776, -26.00000000000001066 ) ) ;
#3015=EDGE_CURVE ( 'NONE', #1150, #54119, #7240, .T. ) ;
#3018=AXIS2_PLACEMENT_3D ( 'NONE', #66870, #39988, #18424 ) ;
#3028=AXIS2_PLACEMENT_3D ( 'NONE', #23897, #41203, #13985 ) ;
#3037=EDGE_LOOP ( 'NONE', ( #43907, #36774, #68467, #9501 ) ) ;
#3048=CARTESIAN_POINT ( 'NONE',  ( -7.450000000000001954, 0.000000000000000000, -20.50000000000000000 ) ) ;
#3050=ORIENTED_EDGE ( 'NONE', *, *, #7320, .F. ) ;
#3058=DIRECTION ( 'NONE',  ( 1.000000000000000000, -0.000000000000000000, 0.000000000000000000 ) ) ;
#3062=ORIENTED_EDGE ( 'NONE', *, *, #53073, .F. ) ;
#3064=CARTESIAN_POINT ( 'NONE',  ( 8.250000000000005329, -7.249999999999998224, -26.00000000000001066 ) ) ;
#3074=CARTESIAN_POINT ( 'NONE',  ( -7.450000000000001954, 0.000000000000000000, -24.50000000000000000 ) ) ;
#3084=EDGE_LOOP ( 'NONE', ( #28669, #10413, #22405, #32746, #30230, #35069, #12461, #48495 ) ) ;
#3088=DIRECTION ( 'NONE',  ( 1.000000000000000000, 0.000000000000000000, 0.000000000000000000 ) ) ;
#3095=DIRECTION ( 'NONE',  ( -0.000000000000000000, 0.000000000000000000, 1.000000000000000000 ) ) ;
#3100=DIRECTION ( 'NONE',  ( -0.000000000000000000, -0.000000000000000000, 1.000000000000000000 ) ) ;
#3107=AXIS2_PLACEMENT_3D ( 'NONE', #38321, #11093, #33353 ) ;
#3109=LINE ( 'NONE', #61799, #41579 ) ;
#3120=AXIS2_PLACEMENT_3D ( 'NONE', #34000, #56960, #1830 ) ;
#3122=DIRECTION ( 'NONE',  ( 0.000000000000000000, 0.000000000000000000, 1.000000000000000000 ) ) ;
#3130=DIRECTION ( 'NONE',  ( 0.000000000000000000, -0.000000000000000000, 1.000000000000000000 ) ) ;
#3133=VERTEX_POINT ( 'NONE', #69104 ) ;
#3173=ORIENTED_EDGE ( 'NONE', *, *, #6778, .T. ) ;
#3178=EDGE_CURVE ( 'NONE', #52634, #66712, #35446, .T. ) ;
#3198=CARTESIAN_POINT ( 'NONE',  ( 8.689999999999999503, 9.750000000000000000, -5.000000000000000000 ) ) ;
#3205=DIRECTION ( 'NONE',  ( 0.000000000000000000, 0.000000000000000000, 1.000000000000000000 ) ) ;
#3210=DIRECTION ( 'NONE',  ( 1.000000000000000000, 0.000000000000000000, 0.000000000000000000 ) ) ;
#3222=EDGE_CURVE ( 'NONE', #7022, #61584, #27588, .T. ) ;
#3224=ORIENTED_EDGE ( 'NONE', *, *, #29632, .T. ) ;
#3228=ORIENTED_EDGE ( 'NONE', *, *, #20624, .T. ) ;
#3230=DIRECTION ( 'NONE',  ( 0.000000000000000000, 0.000000000000000000, 1.000000000000000000 ) ) ;
#3231=DIRECTION ( 'NONE',  ( -1.000000000000000000, 0.000000000000000000, 0.000000000000000000 ) ) ;
#3237=ORIENTED_EDGE ( 'NONE', *, *, #59425, .T. ) ;
#3242=DIRECTION ( 'NONE',  ( -0.000000000000000000, -0.000000000000000000, -1.000000000000000000 ) ) ;
#3244=CARTESIAN_POINT ( 'NONE',  ( 8.250000000000005329, -7.249999999999998224, -26.00000000000001066 ) ) ;
#3252=LINE ( 'NONE', #61230, #63039 ) ;
#3263=DIRECTION ( 'NONE',  ( 0.000000000000000000, 0.000000000000000000, 1.000000000000000000 ) ) ;
#3269=CARTESIAN_POINT ( 'NONE',  ( -7.450000000000001954, 7.250000000000000000, -19.00000000000000000 ) ) ;
#3281=AXIS2_PLACEMENT_3D ( 'NONE', #43789, #49779, #33852 ) ;
#3286=DIRECTION ( 'NONE',  ( 0.000000000000000000, 1.000000000000000000, -0.000000000000000000 ) ) ;
#3293=VERTEX_POINT ( 'NONE', #59881 ) ;
#3300=ORIENTED_EDGE ( 'NONE', *, *, #39904, .T. ) ;
#3306=ORIENTED_EDGE ( 'NONE', *, *, #66074, .F. ) ;
#3311=ORIENTED_EDGE ( 'NONE', *, *, #8644, .T. ) ;
#3325=EDGE_LOOP ( 'NONE', ( #7327, #55183, #54105, #41269 ) ) ;
#3329=DIRECTION ( 'NONE',  ( 1.000000000000000000, -5.981805089575194965E-17, 0.000000000000000000 ) ) ;
#3331=AXIS2_PLACEMENT_3D ( 'NONE', #24277, #2011, #13660 ) ;
#3334=DIRECTION ( 'NONE',  ( 0.000000000000000000, 0.000000000000000000, 1.000000000000000000 ) ) ;
#3336=CARTESIAN_POINT ( 'NONE',  ( -7.250000000000000888, 7.450000000000003730, -8.000000000000000000 ) ) ;
#3342=CARTESIAN_POINT ( 'NONE',  ( 7.250000000000005329, 7.250000000000000888, -12.00000000000000000 ) ) ;
#3347=ORIENTED_EDGE ( 'NONE', *, *, #5702, .F. ) ;
#3352=DIRECTION ( 'NONE',  ( -1.000000000000000000, 0.000000000000000000, 0.000000000000000000 ) ) ;
#3354=EDGE_CURVE ( 'NONE', #11776, #53694, #5804, .T. ) ;
#3357=DIRECTION ( 'NONE',  ( 0.000000000000000000, 0.000000000000000000, -1.000000000000000000 ) ) ;
#3359=EDGE_CURVE ( 'NONE', #20472, #66751, #38884, .T. ) ;
#3364=DIRECTION ( 'NONE',  ( 0.000000000000000000, -0.000000000000000000, 1.000000000000000000 ) ) ;
#3370=CARTESIAN_POINT ( 'NONE',  ( 7.450000000000006395, 7.250000000000000888, -12.50000000000000000 ) ) ;
#3377=CIRCLE ( 'NONE', #41737, 0.9999999999999991118 ) ;
#3379=ORIENTED_EDGE ( 'NONE', *, *, #5782, .F. ) ;
#3380=CARTESIAN_POINT ( 'NONE',  ( 0.000000000000000000, 0.000000000000000000, -13.50000000000000178 ) ) ;
#3382=CARTESIAN_POINT ( 'NONE',  ( -7.450000000000001954, 0.000000000000000000, -8.500000000000000000 ) ) ;
#3384=CYLINDRICAL_SURFACE ( 'NONE', #32649, 1.000000000000000000 ) ;
#3392=VERTEX_POINT ( 'NONE', #3198 ) ;
#3403=VECTOR ( 'NONE', #9401, 1000.000000000000000 ) ;
#3405=ORIENTED_EDGE ( 'NONE', *, *, #45452, .F. ) ;
#3411=VECTOR ( 'NONE', #55701, 1000.000000000000000 ) ;
#3412=FACE_OUTER_BOUND ( 'NONE', #37528, .T. ) ;
#3414=FACE_OUTER_BOUND ( 'NONE', #14135, .T. ) ;
#3419=CARTESIAN_POINT ( 'NONE',  ( 0.000000000000000000, 0.000000000000000000, -5.000000000000000000 ) ) ;
#3420=CARTESIAN_POINT ( 'NONE',  ( -8.750000000000003553, 7.750000000000001776, -5.000000000000000000 ) ) ;
#3422=AXIS2_PLACEMENT_3D ( 'NONE', #30318, #14410, #61419 ) ;
#3423=EDGE_CURVE ( 'NONE', #23467, #13987, #41157, .T. ) ;
#3428=VECTOR ( 'NONE', #42885, 1000.000000000000000 ) ;
#3429=LINE ( 'NONE', #41607, #53628 ) ;
#3442=ORIENTED_EDGE ( 'NONE', *, *, #15762, .F. ) ;
#3449=ORIENTED_EDGE ( 'NONE', *, *, #54668, .T. ) ;
#3454=CARTESIAN_POINT ( 'NONE',  ( 10.50000000000000000, -9.690000000000001279, -4.250000000000000000 ) ) ;
#3462=DIRECTION ( 'NONE',  ( -1.000000000000000000, 1.794541526872559352E-16, 0.000000000000000000 ) ) ;
#3473=CARTESIAN_POINT ( 'NONE',  ( 6.500000000000000888, -6.500000000000002665, 0.000000000000000000 ) ) ;
#3478=DIRECTION ( 'NONE',  ( 1.000000000000000000, 0.000000000000000000, 0.000000000000000000 ) ) ;
#3480=FACE_OUTER_BOUND ( 'NONE', #44384, .T. ) ;
#3483=AXIS2_PLACEMENT_3D ( 'NONE', #17526, #1606, #19274 ) ;
#3496=LINE ( 'NONE', #68552, #42494 ) ;
#3498=DIRECTION ( 'NONE',  ( -1.000000000000000000, 0.000000000000000000, 0.000000000000000000 ) ) ;
#3508=LINE ( 'NONE', #45573, #46427 ) ;
#3519=LINE ( 'NONE', #67868, #25490 ) ;
#3531=ORIENTED_EDGE ( 'NONE', *, *, #54033, .F. ) ;
#3532=VECTOR ( 'NONE', #22074, 1000.000000000000000 ) ;
#3537=EDGE_CURVE ( 'NONE', #32501, #53195, #14049, .T. ) ;
#3538=CARTESIAN_POINT ( 'NONE',  ( 7.250000000000005329, -7.249999999999998224, -16.50000000000000000 ) ) ;
#3553=DIRECTION ( 'NONE',  ( 1.000000000000000000, 0.000000000000000000, 0.000000000000000000 ) ) ;
#3563=DIRECTION ( 'NONE',  ( -1.794541526872559352E-16, -1.000000000000000000, 0.000000000000000000 ) ) ;
#3577=ADVANCED_FACE ( 'NONE', ( #9203, #25464 ), #42422, .T. ) ;
#3587=CIRCLE ( 'NONE', #12587, 1.000000000000000000 ) ;
#3590=CARTESIAN_POINT ( 'NONE',  ( 0.000000000000000000, -7.449999999999998401, -15.50000000000000000 ) ) ;
#3599=CARTESIAN_POINT ( 'NONE',  ( -7.250000000000000888, 7.250000000000001776, -26.00000000000001066 ) ) ;
#3600=ORIENTED_EDGE ( 'NONE', *, *, #3776, .F. ) ;
#3601=CARTESIAN_POINT ( 'NONE',  ( 8.250000000000005329, -7.249999999999998224, -26.00000000000001066 ) ) ;
#3602=DIRECTION ( 'NONE',  ( -1.000000000000000000, 0.000000000000000000, 0.000000000000000000 ) ) ;
#3620=VECTOR ( 'NONE', #24809, 1000.000000000000000 ) ;
#3623=EDGE_LOOP ( 'NONE', ( #63033, #36895, #20347, #67571 ) ) ;
#3624=DIRECTION ( 'NONE',  ( 1.000000000000000000, 0.000000000000000000, 0.000000000000000000 ) ) ;
#3629=CARTESIAN_POINT ( 'NONE',  ( -8.250000000000001776, 7.250000000000000888, -23.50000000000000000 ) ) ;
#3638=ORIENTED_EDGE ( 'NONE', *, *, #55636, .T. ) ;
#3640=DIRECTION ( 'NONE',  ( -1.000000000000000000, 0.000000000000000000, 0.000000000000000000 ) ) ;
#3649=ORIENTED_EDGE ( 'NONE', *, *, #66500, .T. ) ;
#3651=DIRECTION ( 'NONE',  ( 1.000000000000000000, -0.000000000000000000, 0.000000000000000000 ) ) ;
#3653=DIRECTION ( 'NONE',  ( 0.000000000000000000, -1.000000000000000000, -0.000000000000000000 ) ) ;
#3663=DIRECTION ( 'NONE',  ( 0.000000000000000000, 0.000000000000000000, 1.000000000000000000 ) ) ;
#3667=CARTESIAN_POINT ( 'NONE',  ( 9.690000000000001279, 10.50000000000000000, -5.000000000000000000 ) ) ;
#3685=DIRECTION ( 'NONE',  ( 0.000000000000000000, 1.000000000000000000, 0.000000000000000000 ) ) ;
#3689=CIRCLE ( 'NONE', #66911, 0.1999999999999996503 ) ;
#3705=FACE_OUTER_BOUND ( 'NONE', #11044, .T. ) ;
#3706=CARTESIAN_POINT ( 'NONE',  ( 7.250000000000004441, 7.450000000000001954, -10.50000000000000000 ) ) ;
#3712=CARTESIAN_POINT ( 'NONE',  ( -7.250000000000000888, -8.249999999999998224, -12.50000000000000000 ) ) ;
#3718=DIRECTION ( 'NONE',  ( 1.000000000000000000, 0.000000000000000000, 0.000000000000000000 ) ) ;
#3719=EDGE_LOOP ( 'NONE', ( #20012, #42351, #27753, #59783, #45690, #7277, #18294, #48856 ) ) ;
#3726=ORIENTED_EDGE ( 'NONE', *, *, #37311, .F. ) ;
#3729=DIRECTION ( 'NONE',  ( -1.000000000000000000, 0.000000000000000000, 0.000000000000000000 ) ) ;
#3737=ORIENTED_EDGE ( 'NONE', *, *, #11898, .F. ) ;
#3743=LINE ( 'NONE', #68456, #51962 ) ;
#3749=ORIENTED_EDGE ( 'NONE', *, *, #32880, .F. ) ;
#3755=VECTOR ( 'NONE', #66982, 1000.000000000000000 ) ;
#3761=ORIENTED_EDGE ( 'NONE', *, *, #62597, .F. ) ;
#3766=CARTESIAN_POINT ( 'NONE',  ( 7.250000000000005329, -8.249999999999998224, -18.00000000000000000 ) ) ;
#3767=EDGE_CURVE ( 'NONE', #33875, #43298, #46234, .T. ) ;
#3776=EDGE_CURVE ( 'NONE', #28873, #9556, #39867, .T. ) ;
#3777=DIRECTION ( 'NONE',  ( 0.000000000000000000, 0.000000000000000000, 1.000000000000000000 ) ) ;
#3779=AXIS2_PLACEMENT_3D ( 'NONE', #28224, #29250, #2049 ) ;
#3787=DIRECTION ( 'NONE',  ( 1.000000000000000000, -5.981805089575194965E-17, 0.000000000000000000 ) ) ;
#3814=CARTESIAN_POINT ( 'NONE',  ( 0.000000000000000000, 8.750000000000001776, -26.00000000000001066 ) ) ;
#3818=PLANE ( 'NONE',  #29311 ) ;
#3821=CARTESIAN_POINT ( 'NONE',  ( 0.000000000000000000, -8.249999999999998224, -11.50000000000000000 ) ) ;
#3823=VERTEX_POINT ( 'NONE', #51901 ) ;
#3829=ADVANCED_FACE ( 'NONE', ( #7349 ), #34209, .F. ) ;
#3834=ORIENTED_EDGE ( 'NONE', *, *, #43361, .T. ) ;
#3838=VECTOR ( 'NONE', #66631, 1000.000000000000000 ) ;
#3859=CARTESIAN_POINT ( 'NONE',  ( -8.250000000000001776, -7.249999999999998224, -17.50000000000000000 ) ) ;
#3877=EDGE_CURVE ( 'NONE', #65338, #69217, #14423, .T. ) ;
#3881=FACE_OUTER_BOUND ( 'NONE', #9573, .T. ) ;
#3896=ORIENTED_EDGE ( 'NONE', *, *, #49673, .T. ) ;
#3897=EDGE_LOOP ( 'NONE', ( #26435, #40381, #63681, #65893 ) ) ;
#3899=VECTOR ( 'NONE', #31828, 1000.000000000000000 ) ;
#3901=DIRECTION ( 'NONE',  ( 1.000000000000000000, -5.981805089575196197E-17, 0.000000000000000000 ) ) ;
#3905=ORIENTED_EDGE ( 'NONE', *, *, #4942, .T. ) ;
#3906=CARTESIAN_POINT ( 'NONE',  ( -8.250000000000001776, -7.249999999999998224, -14.50000000000000000 ) ) ;
#3922=EDGE_CURVE ( 'NONE', #26084, #36185, #15479, .T. ) ;
#3923=LINE ( 'NONE', #15595, #37239 ) ;
#3927=EDGE_CURVE ( 'NONE', #4784, #69381, #15124, .T. ) ;
#3936=FACE_OUTER_BOUND ( 'NONE', #28872, .T. ) ;
#3945=CARTESIAN_POINT ( 'NONE',  ( 0.000000000000000000, 0.000000000000000000, -9.500000000000001776 ) ) ;
#3957=VERTEX_POINT ( 'NONE', #37048 ) ;
#3962=DIRECTION ( 'NONE',  ( -0.000000000000000000, -0.000000000000000000, 1.000000000000000000 ) ) ;
#3964=PLANE ( 'NONE',  #63662 ) ;
#3967=DIRECTION ( 'NONE',  ( -1.000000000000000000, 2.602085213965213008E-15, 0.000000000000000000 ) ) ;
#3968=DIRECTION ( 'NONE',  ( 1.000000000000000000, 0.000000000000000000, 0.000000000000000000 ) ) ;
#3978=CARTESIAN_POINT ( 'NONE',  ( 7.250000000000005329, -8.249999999999998224, -13.00000000000000178 ) ) ;
#3980=AXIS2_PLACEMENT_3D ( 'NONE', #11441, #500, #22068 ) ;
#3983=EDGE_LOOP ( 'NONE', ( #39861, #53404, #36851, #35733 ) ) ;
#3987=VERTEX_POINT ( 'NONE', #4861 ) ;
#3991=CARTESIAN_POINT ( 'NONE',  ( -9.750000000000001776, -9.690000000000001279, -5.000000000000000000 ) ) ;
#3992=DIRECTION ( 'NONE',  ( 0.000000000000000000, -1.000000000000000000, 0.000000000000000000 ) ) ;
#4000=EDGE_LOOP ( 'NONE', ( #10172, #49038, #56270, #10583 ) ) ;
#4007=EDGE_CURVE ( 'NONE', #22338, #26887, #57896, .T. ) ;
#4010=EDGE_LOOP ( 'NONE', ( #52793, #35835, #26362, #19222 ) ) ;
#4026=CARTESIAN_POINT ( 'NONE',  ( 8.250000000000005329, -7.249999999999998224, -26.00000000000001066 ) ) ;
#4034=ORIENTED_EDGE ( 'NONE', *, *, #22127, .T. ) ;
#4038=PLANE ( 'NONE',  #1291 ) ;
#4047=DIRECTION ( 'NONE',  ( 0.000000000000000000, 0.000000000000000000, 1.000000000000000000 ) ) ;
#4058=EDGE_CURVE ( 'NONE', #40904, #26371, #38431, .T. ) ;
#4065=EDGE_CURVE ( 'NONE', #24148, #53899, #65019, .T. ) ;
#4074=EDGE_CURVE ( 'NONE', #34907, #34803, #31159, .T. ) ;
#4094=DIRECTION ( 'NONE',  ( 0.000000000000000000, 0.000000000000000000, 1.000000000000000000 ) ) ;
#4095=FACE_OUTER_BOUND ( 'NONE', #26759, .T. ) ;
#4096=AXIS2_PLACEMENT_3D ( 'NONE', #42900, #37955, #37261 ) ;
#4099=ORIENTED_EDGE ( 'NONE', *, *, #15452, .F. ) ;
#4101=PLANE ( 'NONE',  #60614 ) ;
#4105=AXIS2_PLACEMENT_3D ( 'NONE', #28246, #66067, #16254 ) ;
#4110=CIRCLE ( 'NONE', #30025, 0.9999999999999991118 ) ;
#4125=ORIENTED_EDGE ( 'NONE', *, *, #64390, .T. ) ;
#4138=CARTESIAN_POINT ( 'NONE',  ( 7.450000000000004619, -1.336933437520057563E-15, -21.00000000000000000 ) ) ;
#4142=DIRECTION ( 'NONE',  ( -1.000000000000000000, 0.000000000000000000, 0.000000000000000000 ) ) ;
#4144=VECTOR ( 'NONE', #39933, 1000.000000000000000 ) ;
#4150=CARTESIAN_POINT ( 'NONE',  ( -7.250000000000000888, 8.250000000000001776, -11.00000000000000000 ) ) ;
#4152=CARTESIAN_POINT ( 'NONE',  ( 7.250000000000005329, 7.250000000000000888, -11.50000000000000000 ) ) ;
#4154=LINE ( 'NONE', #25360, #24438 ) ;
#4158=CARTESIAN_POINT ( 'NONE',  ( 0.000000000000000000, -7.449999999999998401, -24.50000000000000000 ) ) ;
#4159=LINE ( 'NONE', #64940, #45505 ) ;
#4162=VECTOR ( 'NONE', #3242, 1000.000000000000000 ) ;
#4166=EDGE_LOOP ( 'NONE', ( #8247, #45435, #33540, #69517, #60919, #30958, #48425, #39786 ) ) ;
#4169=CARTESIAN_POINT ( 'NONE',  ( -7.450000000000001954, 0.000000000000000000, -15.50000000000000000 ) ) ;
#4177=ORIENTED_EDGE ( 'NONE', *, *, #22780, .T. ) ;
#4184=FACE_BOUND ( 'NONE', #45616, .T. ) ;
#4190=ORIENTED_EDGE ( 'NONE', *, *, #70, .T. ) ;
#4191=VECTOR ( 'NONE', #29938, 1000.000000000000000 ) ;
#4193=DIRECTION ( 'NONE',  ( -1.000000000000000000, 0.000000000000000000, 0.000000000000000000 ) ) ;
#4197=VECTOR ( 'NONE', #21443, 1000.000000000000000 ) ;
#4199=DIRECTION ( 'NONE',  ( 1.000000000000000000, 0.000000000000000000, 0.000000000000000000 ) ) ;
#4211=DIRECTION ( 'NONE',  ( 0.000000000000000000, 0.000000000000000000, 1.000000000000000000 ) ) ;
#4215=FACE_OUTER_BOUND ( 'NONE', #41784, .T. ) ;
#4216=ORIENTED_EDGE ( 'NONE', *, *, #62803, .T. ) ;
#4218=CIRCLE ( 'NONE', #32426, 1.000000000000000000 ) ;
#4226=CARTESIAN_POINT ( 'NONE',  ( 7.250000000000005329, -8.249999999999998224, -26.00000000000001066 ) ) ;
#4232=FACE_OUTER_BOUND ( 'NONE', #2187, .T. ) ;
#4237=FACE_OUTER_BOUND ( 'NONE', #37732, .T. ) ;
#4241=FACE_OUTER_BOUND ( 'NONE', #1790, .T. ) ;
#4259=CIRCLE ( 'NONE', #887, 0.1999999999999987899 ) ;
#4272=DIRECTION ( 'NONE',  ( 1.000000000000000000, 0.000000000000000000, 0.000000000000000000 ) ) ;
#4273=EDGE_CURVE ( 'NONE', #54217, #9481, #36511, .T. ) ;
#4274=EDGE_LOOP ( 'NONE', ( #42183, #28152, #10158, #38515 ) ) ;
#4283=ORIENTED_EDGE ( 'NONE', *, *, #54113, .T. ) ;
#4295=CARTESIAN_POINT ( 'NONE',  ( 7.250000000000005329, -7.249999999999998224, -25.50000000000000355 ) ) ;
#4298=CARTESIAN_POINT ( 'NONE',  ( -7.250000000000000000, -7.449999999999998401, -12.00000000000000000 ) ) ;
#4303=EDGE_CURVE ( 'NONE', #63139, #35171, #11039, .T. ) ;
#4308=CARTESIAN_POINT ( 'NONE',  ( -7.250000000000000888, 8.250000000000001776, -26.00000000000001066 ) ) ;
#4309=ORIENTED_EDGE ( 'NONE', *, *, #42655, .F. ) ;
#4318=CARTESIAN_POINT ( 'NONE',  ( 7.250000000000005329, -7.449999999999998401, -12.50000000000000000 ) ) ;
#4334=LINE ( 'NONE', #25890, #54925 ) ;
#4336=ADVANCED_FACE ( 'NONE', ( #92 ), #48182, .T. ) ;
#4338=ORIENTED_EDGE ( 'NONE', *, *, #51451, .T. ) ;
#4340=ORIENTED_EDGE ( 'NONE', *, *, #41331, .T. ) ;
#4352=ORIENTED_EDGE ( 'NONE', *, *, #30352, .F. ) ;
#4360=EDGE_CURVE ( 'NONE', #43019, #9455, #64110, .T. ) ;
#4364=DIRECTION ( 'NONE',  ( -0.000000000000000000, -0.000000000000000000, -1.000000000000000000 ) ) ;
#4385=CARTESIAN_POINT ( 'NONE',  ( -7.250000000000000000, -7.449999999999998401, -15.50000000000000000 ) ) ;
#4386=EDGE_CURVE ( 'NONE', #30841, #9491, #52662, .T. ) ;
#4389=ORIENTED_EDGE ( 'NONE', *, *, #57376, .F. ) ;
#4392=DIRECTION ( 'NONE',  ( 0.000000000000000000, 0.000000000000000000, -1.000000000000000000 ) ) ;
#4395=ORIENTED_EDGE ( 'NONE', *, *, #37098, .T. ) ;
#4399=CIRCLE ( 'NONE', #48448, 0.2000000000000005107 ) ;
#4402=DIRECTION ( 'NONE',  ( 0.000000000000000000, 0.000000000000000000, -1.000000000000000000 ) ) ;
#4409=CARTESIAN_POINT ( 'NONE',  ( 9.690000000000001279, 10.50000000000000000, -4.250000000000000000 ) ) ;
#4420=DIRECTION ( 'NONE',  ( 0.000000000000000000, 0.000000000000000000, 1.000000000000000000 ) ) ;
#4421=ADVANCED_FACE ( 'NONE', ( #59827 ), #66164, .F. ) ;
#4422=DIRECTION ( 'NONE',  ( -0.000000000000000000, -0.000000000000000000, -1.000000000000000000 ) ) ;
#4429=EDGE_CURVE ( 'NONE', #10667, #39124, #38270, .T. ) ;
#4440=CARTESIAN_POINT ( 'NONE',  ( -7.250000000000001776, -7.249999999999998224, -26.00000000000001066 ) ) ;
#4448=VECTOR ( 'NONE', #14149, 1000.000000000000000 ) ;
#4456=ORIENTED_EDGE ( 'NONE', *, *, #69411, .F. ) ;
#4464=CARTESIAN_POINT ( 'NONE',  ( 7.250000000000005329, -8.249999999999998224, -11.00000000000000000 ) ) ;
#4472=DIRECTION ( 'NONE',  ( -1.000000000000000000, 0.000000000000000000, 0.000000000000000000 ) ) ;
#4475=LINE ( 'NONE', #31698, #58284 ) ;
#4476=FACE_OUTER_BOUND ( 'NONE', #11717, .T. ) ;
#4487=AXIS2_PLACEMENT_3D ( 'NONE', #23184, #27114, #1278 ) ;
#4491=EDGE_CURVE ( 'NONE', #43562, #42042, #29029, .T. ) ;
#4496=CARTESIAN_POINT ( 'NONE',  ( -8.250000000000001776, 0.000000000000000000, -10.00000000000000000 ) ) ;
#4511=EDGE_CURVE ( 'NONE', #34571, #43764, #41326, .T. ) ;
#4512=DIRECTION ( 'NONE',  ( 1.000000000000000000, 0.000000000000000000, 0.000000000000000000 ) ) ;
#4517=CARTESIAN_POINT ( 'NONE',  ( -7.250000000000000000, -7.449999999999998401, -22.50000000000000000 ) ) ;
#4521=ORIENTED_EDGE ( 'NONE', *, *, #37165, .F. ) ;
#4522=DIRECTION ( 'NONE',  ( 0.000000000000000000, 0.000000000000000000, -1.000000000000000000 ) ) ;
#4526=CARTESIAN_POINT ( 'NONE',  ( 7.250000000000005329, -7.249999999999998224, -17.50000000000000000 ) ) ;
#4527=EDGE_LOOP ( 'NONE', ( #11360, #45754, #13267, #67656 ) ) ;
#4528=LINE ( 'NONE', #20776, #35726 ) ;
#4529=DIRECTION ( 'NONE',  ( -1.000000000000000000, 0.000000000000000000, -0.000000000000000000 ) ) ;
#4532=ORIENTED_EDGE ( 'NONE', *, *, #15523, .F. ) ;
#4536=DIRECTION ( 'NONE',  ( -0.000000000000000000, 0.000000000000000000, 1.000000000000000000 ) ) ;
#4547=VECTOR ( 'NONE', #50115, 1000.000000000000000 ) ;
#4550=DIRECTION ( 'NONE',  ( 0.000000000000000000, 0.000000000000000000, -1.000000000000000000 ) ) ;
#4551=ORIENTED_EDGE ( 'NONE', *, *, #8116, .F. ) ;
#4552=EDGE_CURVE ( 'NONE', #10667, #67031, #35359, .T. ) ;
#4558=ORIENTED_EDGE ( 'NONE', *, *, #59813, .T. ) ;
#4564=DIRECTION ( 'NONE',  ( -1.000000000000000000, 0.000000000000000000, 0.000000000000000000 ) ) ;
#4565=ORIENTED_EDGE ( 'NONE', *, *, #34150, .T. ) ;
#4581=LINE ( 'NONE', #26488, #23964 ) ;
#4587=CARTESIAN_POINT ( 'NONE',  ( -8.250000000000001776, -7.249999999999998224, -24.00000000000000000 ) ) ;
#4597=ORIENTED_EDGE ( 'NONE', *, *, #48549, .T. ) ;
#4600=EDGE_CURVE ( 'NONE', #2646, #13864, #49158, .T. ) ;
#4603=CARTESIAN_POINT ( 'NONE',  ( 4.456444791733522252E-16, 7.450000000000002842, -17.00000000000000000 ) ) ;
#4607=CARTESIAN_POINT ( 'NONE',  ( 0.000000000000000000, 0.000000000000000000, -23.00000000000000000 ) ) ;
#4611=DIRECTION ( 'NONE',  ( -0.000000000000000000, 0.000000000000000000, 1.000000000000000000 ) ) ;
#4617=DIRECTION ( 'NONE',  ( 0.000000000000000000, 0.000000000000000000, -1.000000000000000000 ) ) ;
#4619=CARTESIAN_POINT ( 'NONE',  ( 7.250000000000005329, 8.250000000000001776, -14.00000000000000000 ) ) ;
#4628=CARTESIAN_POINT ( 'NONE',  ( -7.250000000000000888, 7.450000000000003730, -14.50000000000000000 ) ) ;
#4629=CIRCLE ( 'NONE', #29428, 0.1999999999999996503 ) ;
#4633=ORIENTED_EDGE ( 'NONE', *, *, #33935, .F. ) ;
#4637=CIRCLE ( 'NONE', #44131, 1.000000000000000000 ) ;
#4640=DIRECTION ( 'NONE',  ( 0.000000000000000000, 0.000000000000000000, 1.000000000000000000 ) ) ;
#4649=FACE_BOUND ( 'NONE', #66272, .T. ) ;
#4669=EDGE_LOOP ( 'NONE', ( #22113, #32249, #4389, #36307 ) ) ;
#4673=ORIENTED_EDGE ( 'NONE', *, *, #15062, .T. ) ;
#4689=VERTEX_POINT ( 'NONE', #45625 ) ;
#4706=VECTOR ( 'NONE', #55627, 1000.000000000000000 ) ;
#4711=AXIS2_PLACEMENT_3D ( 'NONE', #37971, #54234, #32313 ) ;
#4719=DIRECTION ( 'NONE',  ( 0.000000000000000000, 1.000000000000000000, 0.000000000000000000 ) ) ;
#4722=ADVANCED_FACE ( 'NONE', ( #42084 ), #31844, .T. ) ;
#4724=VECTOR ( 'NONE', #24186, 1000.000000000000000 ) ;
#4757=FACE_OUTER_BOUND ( 'NONE', #3325, .T. ) ;
#4759=DIRECTION ( 'NONE',  ( 1.000000000000000000, -5.981805089575196197E-17, 0.000000000000000000 ) ) ;
#4765=EDGE_LOOP ( 'NONE', ( #60610, #67998, #59549, #68943 ) ) ;
#4766=DIRECTION ( 'NONE',  ( 1.000000000000000000, -0.000000000000000000, -0.000000000000000000 ) ) ;
#4771=EDGE_CURVE ( 'NONE', #52692, #63059, #53408, .T. ) ;
#4773=LINE ( 'NONE', #51804, #10255 ) ;
#4777=DIRECTION ( 'NONE',  ( 1.000000000000000000, 0.000000000000000000, 0.000000000000000000 ) ) ;
#4782=CIRCLE ( 'NONE', #2481, 0.1999999999999987899 ) ;
#4784=VERTEX_POINT ( 'NONE', #68620 ) ;
#4786=VECTOR ( 'NONE', #58656, 1000.000000000000000 ) ;
#4788=DIRECTION ( 'NONE',  ( -1.000000000000000000, 0.000000000000000000, 0.000000000000000000 ) ) ;
#4789=CYLINDRICAL_SURFACE ( 'NONE', #57379, 0.2000000000000005107 ) ;
#4795=VERTEX_POINT ( 'NONE', #37490 ) ;
#4797=ORIENTED_EDGE ( 'NONE', *, *, #29392, .F. ) ;
#4803=ADVANCED_FACE ( 'NONE', ( #10603 ), #58709, .T. ) ;
#4805=AXIS2_PLACEMENT_3D ( 'NONE', #5821, #42943, #47897 ) ;
#4806=CARTESIAN_POINT ( 'NONE',  ( 0.000000000000000000, 8.250000000000001776, -19.50000000000000000 ) ) ;
#4813=DIRECTION ( 'NONE',  ( 0.000000000000000000, 1.000000000000000000, 0.000000000000000000 ) ) ;
#4814=EDGE_CURVE ( 'NONE', #20264, #56954, #57998, .T. ) ;
#4817=VECTOR ( 'NONE', #3230, 1000.000000000000000 ) ;
#4820=LINE ( 'NONE', #54922, #51388 ) ;
#4822=CARTESIAN_POINT ( 'NONE',  ( -7.450000000000001954, -7.249999999999998224, -25.50000000000000355 ) ) ;
#4828=DIRECTION ( 'NONE',  ( 0.000000000000000000, 0.000000000000000000, 1.000000000000000000 ) ) ;
#4833=CARTESIAN_POINT ( 'NONE',  ( 7.450000000000006395, 7.250000000000000888, -17.00000000000000000 ) ) ;
#4838=VECTOR ( 'NONE', #14518, 1000.000000000000000 ) ;
#4843=DIRECTION ( 'NONE',  ( -1.000000000000000000, 0.000000000000000000, 0.000000000000000000 ) ) ;
#4853=FACE_BOUND ( 'NONE', #62401, .T. ) ;
#4854=ORIENTED_EDGE ( 'NONE', *, *, #60336, .F. ) ;
#4861=CARTESIAN_POINT ( 'NONE',  ( -7.450000000000001954, 7.250000000000000000, -14.50000000000000000 ) ) ;
#4868=DIRECTION ( 'NONE',  ( -1.000000000000000000, 0.000000000000000000, 0.000000000000000000 ) ) ;
#4874=CARTESIAN_POINT ( 'NONE',  ( -7.250000000000000888, 7.250000000000001776, -21.50000000000000000 ) ) ;
#4877=CIRCLE ( 'NONE', #64679, 1.000000000000002665 ) ;
#4884=EDGE_LOOP ( 'NONE', ( #48792, #45078, #51432, #22386 ) ) ;
#4899=EDGE_CURVE ( 'NONE', #46497, #39124, #22015, .T. ) ;
#4900=EDGE_LOOP ( 'NONE', ( #7180, #16964, #36523, #34985 ) ) ;
#4901=AXIS2_PLACEMENT_3D ( 'NONE', #51732, #3286, #14594 ) ;
#4904=DIRECTION ( 'NONE',  ( 0.000000000000000000, 0.000000000000000000, -1.000000000000000000 ) ) ;
#4914=AXIS2_PLACEMENT_3D ( 'NONE', #16826, #38392, #59950 ) ;
#4920=CARTESIAN_POINT ( 'NONE',  ( -7.250000000000000888, -8.249999999999998224, -17.00000000000000000 ) ) ;
#4921=ORIENTED_EDGE ( 'NONE', *, *, #21919, .T. ) ;
#4923=DIRECTION ( 'NONE',  ( 0.000000000000000000, 0.000000000000000000, -1.000000000000000000 ) ) ;
#4931=LINE ( 'NONE', #26853, #19837 ) ;
#4936=LINE ( 'NONE', #5634, #18296 ) ;
#4942=EDGE_CURVE ( 'NONE', #16354, #53017, #49167, .T. ) ;
#4945=ADVANCED_FACE ( 'NONE', ( #1382, #22943 ), #16625, .T. ) ;
#4946=CARTESIAN_POINT ( 'NONE',  ( -7.450000000000001954, 7.250000000000000000, -11.50000000000000000 ) ) ;
#4958=VERTEX_POINT ( 'NONE', #16960 ) ;
#4960=LINE ( 'NONE', #59742, #68256 ) ;
#4961=DIRECTION ( 'NONE',  ( 0.000000000000000000, 0.000000000000000000, 1.000000000000000000 ) ) ;
#4962=AXIS2_PLACEMENT_3D ( 'NONE', #39357, #27378, #12472 ) ;
#4968=CIRCLE ( 'NONE', #50110, 1.000000000000000000 ) ;
#4972=ORIENTED_EDGE ( 'NONE', *, *, #1163, .T. ) ;
#4996=LINE ( 'NONE', #36839, #63151 ) ;
#4999=ADVANCED_FACE ( 'NONE', ( #56508 ), #7712, .T. ) ;
#5016=AXIS2_PLACEMENT_3D ( 'NONE', #34872, #66713, #18264 ) ;
#5017=AXIS2_PLACEMENT_3D ( 'NONE', #68114, #30295, #45485 ) ;
#5020=EDGE_LOOP ( 'NONE', ( #27987, #6673, #7293, #59754 ) ) ;
#5022=VECTOR ( 'NONE', #5408, 1000.000000000000000 ) ;
#5031=ORIENTED_EDGE ( 'NONE', *, *, #18494, .F. ) ;
#5033=CARTESIAN_POINT ( 'NONE',  ( -8.250000000000001776, -7.249999999999998224, -20.00000000000000000 ) ) ;
#5034=LINE ( 'NONE', #48871, #28661 ) ;
#5041=ORIENTED_EDGE ( 'NONE', *, *, #57692, .T. ) ;
#5045=VERTEX_POINT ( 'NONE', #57559 ) ;
#5048=DIRECTION ( 'NONE',  ( -1.000000000000000000, 0.000000000000000000, 0.000000000000000000 ) ) ;
#5054=ORIENTED_EDGE ( 'NONE', *, *, #54110, .T. ) ;
#5083=DIRECTION ( 'NONE',  ( -8.951101527228104953E-17, -1.000000000000000000, 0.000000000000000000 ) ) ;
#5084=ADVANCED_FACE ( 'NONE', ( #35631, #51202 ), #50515, .F. ) ;
#5090=DIRECTION ( 'NONE',  ( 0.000000000000000000, 0.000000000000000000, -1.000000000000000000 ) ) ;
#5093=CARTESIAN_POINT ( 'NONE',  ( 7.250000000000005329, -7.249999999999998224, -17.50000000000000000 ) ) ;
#5102=ADVANCED_FACE ( 'NONE', ( #23980 ), #62496, .T. ) ;
#5103=CARTESIAN_POINT ( 'NONE',  ( -7.250000000000001776, -7.249999999999998224, -15.50000000000000000 ) ) ;
#5105=ORIENTED_EDGE ( 'NONE', *, *, #9602, .T. ) ;
#5130=EDGE_LOOP ( 'NONE', ( #17385, #55770, #31793, #50830 ) ) ;
#5133=DIRECTION ( 'NONE',  ( 1.000000000000000000, 0.000000000000000000, 0.000000000000000000 ) ) ;
#5136=EDGE_LOOP ( 'NONE', ( #29991, #48536, #26102, #42583 ) ) ;
#5143=EDGE_CURVE ( 'NONE', #17827, #40029, #26440, .T. ) ;
#5145=VERTEX_POINT ( 'NONE', #58622 ) ;
#5149=DIRECTION ( 'NONE',  ( 0.000000000000000000, 0.000000000000000000, -1.000000000000000000 ) ) ;
#5154=VECTOR ( 'NONE', #11247, 1000.000000000000000 ) ;
#5155=VECTOR ( 'NONE', #3663, 1000.000000000000000 ) ;
#5171=CARTESIAN_POINT ( 'NONE',  ( -7.450000000000001954, 0.000000000000000000, -10.50000000000000000 ) ) ;
#5185=ORIENTED_EDGE ( 'NONE', *, *, #5830, .F. ) ;
#5189=LINE ( 'NONE', #47617, #4197 ) ;
#5199=DIRECTION ( 'NONE',  ( -0.000000000000000000, -0.000000000000000000, -1.000000000000000000 ) ) ;
#5201=ORIENTED_EDGE ( 'NONE', *, *, #68435, .T. ) ;
#5203=AXIS2_PLACEMENT_3D ( 'NONE', #59152, #37251, #31942 ) ;
#5206=ORIENTED_EDGE ( 'NONE', *, *, #64188, .T. ) ;
#5209=ORIENTED_EDGE ( 'NONE', *, *, #39436, .T. ) ;
#5213=AXIS2_PLACEMENT_3D ( 'NONE', #20598, #5746, #21997 ) ;
#5214=AXIS2_PLACEMENT_3D ( 'NONE', #42433, #52002, #31842 ) ;
#5215=DIRECTION ( 'NONE',  ( 0.000000000000000000, -1.000000000000000000, 0.000000000000000000 ) ) ;
#5230=ORIENTED_EDGE ( 'NONE', *, *, #69230, .T. ) ;
#5235=ORIENTED_EDGE ( 'NONE', *, *, #8801, .F. ) ;
#5236=ORIENTED_EDGE ( 'NONE', *, *, #52654, .F. ) ;
#5237=EDGE_CURVE ( 'NONE', #67361, #52010, #64617, .T. ) ;
#5238=ORIENTED_EDGE ( 'NONE', *, *, #1057, .T. ) ;
#5241=VERTEX_POINT ( 'NONE', #16176 ) ;
#5244=VERTEX_POINT ( 'NONE', #26100 ) ;
#5246=ORIENTED_EDGE ( 'NONE', *, *, #744, .F. ) ;
#5263=ORIENTED_EDGE ( 'NONE', *, *, #55206, .F. ) ;
#5275=LINE ( 'NONE', #26839, #36826 ) ;
#5279=VECTOR ( 'NONE', #68847, 1000.000000000000000 ) ;
#5283=CARTESIAN_POINT ( 'NONE',  ( -7.450000000000001954, 7.250000000000000000, -23.00000000000000000 ) ) ;
#5309=ORIENTED_EDGE ( 'NONE', *, *, #26315, .T. ) ;
#5314=VERTEX_POINT ( 'NONE', #54024 ) ;
#5317=AXIS2_PLACEMENT_3D ( 'NONE', #49148, #59414, #69688 ) ;
#5336=CIRCLE ( 'NONE', #67395, 0.9999999999999991118 ) ;
#5338=ORIENTED_EDGE ( 'NONE', *, *, #24519, .F. ) ;
#5347=EDGE_CURVE ( 'NONE', #17361, #65338, #25441, .T. ) ;
#5351=CYLINDRICAL_SURFACE ( 'NONE', #5848, 2.500000000000000000 ) ;
#5354=CARTESIAN_POINT ( 'NONE',  ( 7.750000000000001776, 7.750000000000000000, 5.000000000000000000 ) ) ;
#5359=DIRECTION ( 'NONE',  ( 0.000000000000000000, -0.000000000000000000, 1.000000000000000000 ) ) ;
#5361=EDGE_CURVE ( 'NONE', #65486, #10069, #62115, .T. ) ;
#5368=ORIENTED_EDGE ( 'NONE', *, *, #44076, .F. ) ;
#5369=AXIS2_PLACEMENT_3D ( 'NONE', #64508, #20656, #47541 ) ;
#5378=ORIENTED_EDGE ( 'NONE', *, *, #55995, .T. ) ;
#5384=VECTOR ( 'NONE', #30023, 1000.000000000000000 ) ;
#5393=CARTESIAN_POINT ( 'NONE',  ( -7.250000000000000888, -8.249999999999998224, -15.50000000000000000 ) ) ;
#5396=EDGE_CURVE ( 'NONE', #46624, #63930, #28504, .T. ) ;
#5400=VERTEX_POINT ( 'NONE', #38106 ) ;
#5407=PLANE ( 'NONE',  #52606 ) ;
#5408=DIRECTION ( 'NONE',  ( 1.000000000000000000, -0.000000000000000000, 0.000000000000000000 ) ) ;
#5425=EDGE_LOOP ( 'NONE', ( #36136, #69585, #69436, #55041 ) ) ;
#5441=ORIENTED_EDGE ( 'NONE', *, *, #7941, .F. ) ;
#5442=EDGE_CURVE ( 'NONE', #69858, #63180, #67401, .T. ) ;
#5467=DIRECTION ( 'NONE',  ( -1.000000000000000000, 0.000000000000000000, -0.000000000000000000 ) ) ;
#5475=FACE_OUTER_BOUND ( 'NONE', #34502, .T. ) ;
#5482=LINE ( 'NONE', #64870, #10450 ) ;
#5483=ORIENTED_EDGE ( 'NONE', *, *, #6732, .F. ) ;
#5498=CARTESIAN_POINT ( 'NONE',  ( 4.456444791733522252E-16, 7.450000000000002842, -24.50000000000000000 ) ) ;
#5518=DIRECTION ( 'NONE',  ( -0.000000000000000000, -0.000000000000000000, 1.000000000000000000 ) ) ;
#5522=CARTESIAN_POINT ( 'NONE',  ( 9.690000000000001279, 9.750000000000001776, -5.000000000000000000 ) ) ;
#5534=CARTESIAN_POINT ( 'NONE',  ( 8.250000000000005329, -8.249999999999998224, -26.00000000000001066 ) ) ;
#5538=CARTESIAN_POINT ( 'NONE',  ( 7.250000000000005329, -7.449999999999998401, -7.500000000000000000 ) ) ;
#5542=DIRECTION ( 'NONE',  ( 1.000000000000000000, 0.000000000000000000, 0.000000000000000000 ) ) ;
#5543=DIRECTION ( 'NONE',  ( -1.794541526872559352E-16, -1.000000000000000000, 0.000000000000000000 ) ) ;
#5550=CARTESIAN_POINT ( 'NONE',  ( -7.250000000000000888, 7.250000000000001776, -14.50000000000000000 ) ) ;
#5553=CIRCLE ( 'NONE', #37209, 1.000000000000000000 ) ;
#5559=VERTEX_POINT ( 'NONE', #68447 ) ;
#5568=ORIENTED_EDGE ( 'NONE', *, *, #49526, .F. ) ;
#5578=VERTEX_POINT ( 'NONE', #21050 ) ;
#5580=DIRECTION ( 'NONE',  ( 1.000000000000000000, -0.000000000000000000, 0.000000000000000000 ) ) ;
#5587=ORIENTED_EDGE ( 'NONE', *, *, #61652, .F. ) ;
#5592=AXIS2_PLACEMENT_3D ( 'NONE', #9456, #20409, #4512 ) ;
#5594=EDGE_CURVE ( 'NONE', #4689, #10719, #6807, .T. ) ;
#5600=EDGE_CURVE ( 'NONE', #24192, #11455, #20351, .T. ) ;
#5617=DIRECTION ( 'NONE',  ( 0.000000000000000000, 0.000000000000000000, 1.000000000000000000 ) ) ;
#5634=CARTESIAN_POINT ( 'NONE',  ( 0.000000000000000000, -7.449999999999998401, -14.00000000000000000 ) ) ;
#5645=ORIENTED_EDGE ( 'NONE', *, *, #22848, .T. ) ;
#5657=VECTOR ( 'NONE', #23256, 1000.000000000000000 ) ;
#5668=ORIENTED_EDGE ( 'NONE', *, *, #36325, .F. ) ;
#5671=CIRCLE ( 'NONE', #45149, 0.2000000000000005107 ) ;
#5681=DIRECTION ( 'NONE',  ( -1.794541526872559352E-16, -1.000000000000000000, 0.000000000000000000 ) ) ;
#5684=ORIENTED_EDGE ( 'NONE', *, *, #51339, .F. ) ;
#5686=CARTESIAN_POINT ( 'NONE',  ( -7.250000000000001776, -7.249999999999998224, -16.50000000000000000 ) ) ;
#5695=DIRECTION ( 'NONE',  ( 0.000000000000000000, 0.000000000000000000, -1.000000000000000000 ) ) ;
#5696=ADVANCED_FACE ( 'NONE', ( #6537 ), #65246, .T. ) ;
#5697=CARTESIAN_POINT ( 'NONE',  ( -8.689999999999999503, -8.750000000000000000, -7.000000000000000000 ) ) ;
#5702=EDGE_CURVE ( 'NONE', #40029, #44854, #55316, .T. ) ;
#5703=PLANE ( 'NONE',  #45063 ) ;
#5704=ORIENTED_EDGE ( 'NONE', *, *, #69230, .F. ) ;
#5719=LINE ( 'NONE', #42490, #23300 ) ;
#5721=DIRECTION ( 'NONE',  ( 0.000000000000000000, -0.000000000000000000, 1.000000000000000000 ) ) ;
#5724=CARTESIAN_POINT ( 'NONE',  ( 7.250000000000005329, -7.249999999999998224, -19.50000000000000000 ) ) ;
#5725=ORIENTED_EDGE ( 'NONE', *, *, #9775, .F. ) ;
#5730=CIRCLE ( 'NONE', #27170, 0.9999999999999991118 ) ;
#5746=DIRECTION ( 'NONE',  ( -0.000000000000000000, 0.000000000000000000, 1.000000000000000000 ) ) ;
#5753=CARTESIAN_POINT ( 'NONE',  ( 0.000000000000000000, 0.000000000000000000, -1.000000000000000000 ) ) ;
#5754=AXIS2_PLACEMENT_3D ( 'NONE', #17146, #10198, #58294 ) ;
#5757=EDGE_LOOP ( 'NONE', ( #9318, #8855, #67262, #44592 ) ) ;
#5758=ORIENTED_EDGE ( 'NONE', *, *, #11901, .F. ) ;
#5760=CIRCLE ( 'NONE', #15949, 1.000000000000000000 ) ;
#5770=ORIENTED_EDGE ( 'NONE', *, *, #41642, .T. ) ;
#5771=AXIS2_PLACEMENT_3D ( 'NONE', #16771, #54257, #32677 ) ;
#5772=ADVANCED_FACE ( 'NONE', ( #43996 ), #6854, .F. ) ;
#5782=EDGE_CURVE ( 'NONE', #31198, #39723, #28422, .T. ) ;
#5785=EDGE_CURVE ( 'NONE', #61969, #21985, #17473, .T. ) ;
#5804=LINE ( 'NONE', #43628, #23084 ) ;
#5809=DIRECTION ( 'NONE',  ( -0.000000000000000000, -0.000000000000000000, -1.000000000000000000 ) ) ;
#5813=CYLINDRICAL_SURFACE ( 'NONE', #4962, 1.000000000000002665 ) ;
#5821=CARTESIAN_POINT ( 'NONE',  ( 8.250000000000005329, 8.250000000000001776, -26.00000000000001066 ) ) ;
#5822=ORIENTED_EDGE ( 'NONE', *, *, #68272, .F. ) ;
#5830=EDGE_CURVE ( 'NONE', #46964, #43093, #5730, .T. ) ;
#5832=DIRECTION ( 'NONE',  ( 0.000000000000000000, -0.000000000000000000, 1.000000000000000000 ) ) ;
#5833=DIRECTION ( 'NONE',  ( 0.000000000000000000, 0.000000000000000000, 1.000000000000000000 ) ) ;
#5837=ORIENTED_EDGE ( 'NONE', *, *, #46930, .T. ) ;
#5844=CIRCLE ( 'NONE', #53300, 1.000000000000000000 ) ;
#5845=DIRECTION ( 'NONE',  ( -1.000000000000000000, 0.000000000000000000, 0.000000000000000000 ) ) ;
#5848=AXIS2_PLACEMENT_3D ( 'NONE', #48468, #43850, #64728 ) ;
#5855=VERTEX_POINT ( 'NONE', #18869 ) ;
#5887=LINE ( 'NONE', #44381, #66147 ) ;
#5889=CARTESIAN_POINT ( 'NONE',  ( 0.000000000000000000, 8.250000000000001776, -10.00000000000000000 ) ) ;
#5890=CARTESIAN_POINT ( 'NONE',  ( 0.000000000000000000, -7.449999999999998401, -9.500000000000001776 ) ) ;
#5893=ORIENTED_EDGE ( 'NONE', *, *, #27950, .T. ) ;
#5898=LINE ( 'NONE', #12222, #49904 ) ;
#5910=CARTESIAN_POINT ( 'NONE',  ( -7.450000000000001954, 7.250000000000000000, -16.00000000000000000 ) ) ;
#5920=ORIENTED_EDGE ( 'NONE', *, *, #36838, .T. ) ;
#5929=AXIS2_PLACEMENT_3D ( 'NONE', #942, #59627, #32745 ) ;
#5939=ORIENTED_EDGE ( 'NONE', *, *, #29986, .F. ) ;
#5941=AXIS2_PLACEMENT_3D ( 'NONE', #41387, #31144, #62965 ) ;
#5946=DIRECTION ( 'NONE',  ( 0.000000000000000000, 0.000000000000000000, 1.000000000000000000 ) ) ;
#5947=LINE ( 'NONE', #647, #29667 ) ;
#5952=FACE_OUTER_BOUND ( 'NONE', #41701, .T. ) ;
#5958=CARTESIAN_POINT ( 'NONE',  ( 7.250000000000005329, 7.250000000000000888, -26.00000000000001066 ) ) ;
#5966=ORIENTED_EDGE ( 'NONE', *, *, #41780, .T. ) ;
#5971=AXIS2_PLACEMENT_3D ( 'NONE', #67155, #61138, #13054 ) ;
#5987=CIRCLE ( 'NONE', #66939, 1.000000000000000000 ) ;
#5988=DIRECTION ( 'NONE',  ( 0.000000000000000000, -0.000000000000000000, 1.000000000000000000 ) ) ;
#5989=ORIENTED_EDGE ( 'NONE', *, *, #33220, .T. ) ;
#5992=FACE_OUTER_BOUND ( 'NONE', #43451, .T. ) ;
#5993=CARTESIAN_POINT ( 'NONE',  ( -7.250000000000000000, -7.449999999999998401, -22.00000000000000000 ) ) ;
#5999=DIRECTION ( 'NONE',  ( -0.000000000000000000, -0.000000000000000000, 1.000000000000000000 ) ) ;
#6001=ORIENTED_EDGE ( 'NONE', *, *, #58403, .T. ) ;
#6006=EDGE_CURVE ( 'NONE', #14714, #69741, #20609, .T. ) ;
#6010=ORIENTED_EDGE ( 'NONE', *, *, #36765, .T. ) ;
#6016=DIRECTION ( 'NONE',  ( 0.000000000000000000, -1.000000000000000000, 0.000000000000000000 ) ) ;
#6025=DIRECTION ( 'NONE',  ( 0.000000000000000000, 1.000000000000000000, 0.000000000000000000 ) ) ;
#6034=ORIENTED_EDGE ( 'NONE', *, *, #9950, .F. ) ;
#6045=DIRECTION ( 'NONE',  ( 1.000000000000000000, 0.000000000000000000, 0.000000000000000000 ) ) ;
#6051=LINE ( 'NONE', #48143, #22247 ) ;
#6052=CIRCLE ( 'NONE', #38738, 2.500000000000000000 ) ;
#6054=VERTEX_POINT ( 'NONE', #26274 ) ;
#6055=DIRECTION ( 'NONE',  ( -0.000000000000000000, 0.000000000000000000, 1.000000000000000000 ) ) ;
#6059=CARTESIAN_POINT ( 'NONE',  ( 8.250000000000005329, 8.250000000000001776, -26.00000000000001066 ) ) ;
#6060=DIRECTION ( 'NONE',  ( 0.000000000000000000, 0.000000000000000000, 1.000000000000000000 ) ) ;
#6066=ORIENTED_EDGE ( 'NONE', *, *, #61649, .F. ) ;
#6073=AXIS2_PLACEMENT_3D ( 'NONE', #33295, #54871, #27993 ) ;
#6078=VERTEX_POINT ( 'NONE', #14610 ) ;
#6079=ORIENTED_EDGE ( 'NONE', *, *, #21253, .F. ) ;
#6084=ADVANCED_FACE ( 'NONE', ( #22014 ), #21322, .F. ) ;
#6090=VERTEX_POINT ( 'NONE', #69770 ) ;
#6093=DIRECTION ( 'NONE',  ( 0.000000000000000000, 0.000000000000000000, 1.000000000000000000 ) ) ;
#6096=CARTESIAN_POINT ( 'NONE',  ( 7.250000000000005329, -7.449999999999998401, -25.50000000000000355 ) ) ;
#6103=EDGE_CURVE ( 'NONE', #12421, #68065, #56484, .T. ) ;
#6104=VERTEX_POINT ( 'NONE', #26627 ) ;
#6107=VERTEX_POINT ( 'NONE', #27327 ) ;
#6109=AXIS2_PLACEMENT_3D ( 'NONE', #68437, #5832, #54974 ) ;
#6110=LINE ( 'NONE', #49584, #23456 ) ;
#6135=EDGE_LOOP ( 'NONE', ( #23678, #32633, #45265, #20030 ) ) ;
#6139=CARTESIAN_POINT ( 'NONE',  ( -7.250000000000000888, -8.249999999999998224, -26.00000000000001066 ) ) ;
#6144=CARTESIAN_POINT ( 'NONE',  ( 9.750000000000000000, -9.690000000000001279, -5.000000000000000000 ) ) ;
#6146=CARTESIAN_POINT ( 'NONE',  ( -7.250000000000000888, 7.250000000000001776, -26.00000000000001066 ) ) ;
#6150=CARTESIAN_POINT ( 'NONE',  ( 7.250000000000005329, -7.249999999999998224, -21.00000000000000000 ) ) ;
#6152=CARTESIAN_POINT ( 'NONE',  ( -7.250000000000000000, -8.749999999999998224, -30.00000000000001066 ) ) ;
#6160=EDGE_CURVE ( 'NONE', #13636, #39877, #53505, .T. ) ;
#6166=ORIENTED_EDGE ( 'NONE', *, *, #34471, .T. ) ;
#6167=ORIENTED_EDGE ( 'NONE', *, *, #56541, .F. ) ;
#6173=CARTESIAN_POINT ( 'NONE',  ( 8.250000000000005329, 8.250000000000001776, -26.00000000000001066 ) ) ;
#6177=ORIENTED_EDGE ( 'NONE', *, *, #22848, .F. ) ;
#6179=EDGE_LOOP ( 'NONE', ( #57601, #45223, #58071, #58186 ) ) ;
#6182=VERTEX_POINT ( 'NONE', #39551 ) ;
#6192=DIRECTION ( 'NONE',  ( -1.000000000000000000, 0.000000000000000000, -0.000000000000000000 ) ) ;
#6194=ORIENTED_EDGE ( 'NONE', *, *, #38350, .F. ) ;
#6212=ADVANCED_FACE ( 'NONE', ( #61837 ), #36004, .F. ) ;
#6229=DIRECTION ( 'NONE',  ( 0.000000000000000000, 1.000000000000000000, 0.000000000000000000 ) ) ;
#6230=CARTESIAN_POINT ( 'NONE',  ( 7.250000000000005329, 7.250000000000000888, -15.50000000000000000 ) ) ;
#6240=ORIENTED_EDGE ( 'NONE', *, *, #40635, .F. ) ;
#6243=ORIENTED_EDGE ( 'NONE', *, *, #196, .T. ) ;
#6245=DIRECTION ( 'NONE',  ( 1.000000000000000000, -5.981805089575194965E-17, 0.000000000000000000 ) ) ;
#6267=ORIENTED_EDGE ( 'NONE', *, *, #45456, .F. ) ;
#6269=DIRECTION ( 'NONE',  ( 0.000000000000000000, 0.000000000000000000, -1.000000000000000000 ) ) ;
#6271=DIRECTION ( 'NONE',  ( -1.000000000000000000, 0.000000000000000000, 0.000000000000000000 ) ) ;
#6274=VECTOR ( 'NONE', #65439, 1000.000000000000000 ) ;
#6284=VERTEX_POINT ( 'NONE', #50859 ) ;
#6286=CYLINDRICAL_SURFACE ( 'NONE', #40760, 1.000000000000000000 ) ;
#6289=FACE_OUTER_BOUND ( 'NONE', #3897, .T. ) ;
#6292=CIRCLE ( 'NONE', #27749, 1.000000000000000000 ) ;
#6296=DIRECTION ( 'NONE',  ( -0.000000000000000000, -0.000000000000000000, 1.000000000000000000 ) ) ;
#6301=CIRCLE ( 'NONE', #65013, 1.000000000000000000 ) ;
#6307=VECTOR ( 'NONE', #63746, 1000.000000000000000 ) ;
#6309=ORIENTED_EDGE ( 'NONE', *, *, #26893, .T. ) ;
#6315=CIRCLE ( 'NONE', #66113, 1.000000000000000000 ) ;
#6318=DIRECTION ( 'NONE',  ( -1.000000000000000000, 0.000000000000000000, 0.000000000000000000 ) ) ;
#6321=AXIS2_PLACEMENT_3D ( 'NONE', #18639, #61415, #29242 ) ;
#6325=ORIENTED_EDGE ( 'NONE', *, *, #36199, .T. ) ;
#6330=ORIENTED_EDGE ( 'NONE', *, *, #39436, .F. ) ;
#6336=DIRECTION ( 'NONE',  ( -0.000000000000000000, 0.000000000000000000, -1.000000000000000000 ) ) ;
#6339=ADVANCED_FACE ( 'NONE', ( #45553 ), #18687, .T. ) ;
#6344=CARTESIAN_POINT ( 'NONE',  ( 7.250000000000005329, 7.250000000000000888, -26.00000000000001066 ) ) ;
#6348=DIRECTION ( 'NONE',  ( -0.000000000000000000, -0.000000000000000000, -1.000000000000000000 ) ) ;
#6353=EDGE_CURVE ( 'NONE', #18984, #33218, #4629, .T. ) ;
#6355=EDGE_CURVE ( 'NONE', #17879, #43197, #24702, .T. ) ;
#6372=ORIENTED_EDGE ( 'NONE', *, *, #3015, .F. ) ;
#6379=VERTEX_POINT ( 'NONE', #59320 ) ;
#6381=DIRECTION ( 'NONE',  ( -0.000000000000000000, -0.000000000000000000, -1.000000000000000000 ) ) ;
#6390=LINE ( 'NONE', #65776, #38951 ) ;
#6391=ORIENTED_EDGE ( 'NONE', *, *, #23226, .T. ) ;
#6397=DIRECTION ( 'NONE',  ( 0.000000000000000000, 1.000000000000000000, 0.000000000000000000 ) ) ;
#6408=PLANE ( 'NONE',  #47797 ) ;
#6414=EDGE_LOOP ( 'NONE', ( #65391, #65149, #56337, #15100 ) ) ;
#6428=VECTOR ( 'NONE', #9601, 1000.000000000000000 ) ;
#6429=DIRECTION ( 'NONE',  ( 0.000000000000000000, 1.000000000000000000, 0.000000000000000000 ) ) ;
#6430=DIRECTION ( 'NONE',  ( -1.000000000000000000, 0.000000000000000000, 0.000000000000000000 ) ) ;
#6439=ORIENTED_EDGE ( 'NONE', *, *, #32797, .F. ) ;
#6443=LINE ( 'NONE', #50605, #30983 ) ;
#6445=DIRECTION ( 'NONE',  ( -1.794541526872559352E-16, -1.000000000000000000, 0.000000000000000000 ) ) ;
#6447=VERTEX_POINT ( 'NONE', #32103 ) ;
#6450=CARTESIAN_POINT ( 'NONE',  ( -7.250000000000001776, -7.249999999999998224, -14.00000000000000000 ) ) ;
#6459=ORIENTED_EDGE ( 'NONE', *, *, #39229, .T. ) ;
#6461=CIRCLE ( 'NONE', #57273, 0.7499999999999997780 ) ;
#6469=LINE ( 'NONE', #48218, #69606 ) ;
#6479=ORIENTED_EDGE ( 'NONE', *, *, #57259, .T. ) ;
#6493=ORIENTED_EDGE ( 'NONE', *, *, #17658, .F. ) ;
#6511=ORIENTED_EDGE ( 'NONE', *, *, #60640, .T. ) ;
#6518=DIRECTION ( 'NONE',  ( 0.000000000000000000, -1.000000000000000000, 0.000000000000000000 ) ) ;
#6521=AXIS2_PLACEMENT_3D ( 'NONE', #2898, #29763, #51336 ) ;
#6525=VERTEX_POINT ( 'NONE', #626 ) ;
#6528=DIRECTION ( 'NONE',  ( -1.000000000000000000, 0.000000000000000000, 0.000000000000000000 ) ) ;
#6531=FACE_OUTER_BOUND ( 'NONE', #35145, .T. ) ;
#6534=VERTEX_POINT ( 'NONE', #38786 ) ;
#6536=ORIENTED_EDGE ( 'NONE', *, *, #15119, .F. ) ;
#6537=FACE_OUTER_BOUND ( 'NONE', #56877, .T. ) ;
#6539=ORIENTED_EDGE ( 'NONE', *, *, #57894, .F. ) ;
#6549=VERTEX_POINT ( 'NONE', #17216 ) ;
#6550=PLANE ( 'NONE',  #5754 ) ;
#6551=FACE_OUTER_BOUND ( 'NONE', #54617, .T. ) ;
#6555=VECTOR ( 'NONE', #16238, 1000.000000000000000 ) ;
#6560=CARTESIAN_POINT ( 'NONE',  ( -7.250000000000001776, -7.249999999999998224, -21.00000000000000000 ) ) ;
#6566=EDGE_CURVE ( 'NONE', #57899, #2479, #66723, .T. ) ;
#6569=CARTESIAN_POINT ( 'NONE',  ( -8.250000000000001776, -8.249999999999998224, -26.00000000000001066 ) ) ;
#6570=EDGE_CURVE ( 'NONE', #48126, #13530, #43756, .T. ) ;
#6590=CARTESIAN_POINT ( 'NONE',  ( 7.250000000000005329, -8.249999999999998224, -21.50000000000000000 ) ) ;
#6591=ORIENTED_EDGE ( 'NONE', *, *, #51541, .F. ) ;
#6597=DIRECTION ( 'NONE',  ( 1.000000000000000000, 0.000000000000000000, 0.000000000000000000 ) ) ;
#6598=EDGE_LOOP ( 'NONE', ( #22313, #5031, #8604, #40979 ) ) ;
#6603=EDGE_CURVE ( 'NONE', #52415, #32145, #64492, .T. ) ;
#6605=EDGE_LOOP ( 'NONE', ( #39383, #25112, #13655, #32409 ) ) ;
#6619=VERTEX_POINT ( 'NONE', #50440 ) ;
#6626=ORIENTED_EDGE ( 'NONE', *, *, #60490, .T. ) ;
#6632=AXIS2_PLACEMENT_3D ( 'NONE', #15042, #4094, #53241 ) ;
#6643=DIRECTION ( 'NONE',  ( 0.000000000000000000, 1.000000000000000000, 0.000000000000000000 ) ) ;
#6645=DIRECTION ( 'NONE',  ( -0.000000000000000000, -0.000000000000000000, 1.000000000000000000 ) ) ;
#6650=FACE_OUTER_BOUND ( 'NONE', #57124, .T. ) ;
#6669=ORIENTED_EDGE ( 'NONE', *, *, #27336, .F. ) ;
#6673=ORIENTED_EDGE ( 'NONE', *, *, #26344, .T. ) ;
#6676=PLANE ( 'NONE',  #4105 ) ;
#6677=EDGE_CURVE ( 'NONE', #66827, #49333, #2003, .T. ) ;
#6680=VERTEX_POINT ( 'NONE', #2689 ) ;
#6681=CARTESIAN_POINT ( 'NONE',  ( -7.450000000000001954, 7.250000000000000000, -21.00000000000000000 ) ) ;
#6688=AXIS2_PLACEMENT_3D ( 'NONE', #29023, #3205, #24770 ) ;
#6697=DIRECTION ( 'NONE',  ( 0.000000000000000000, 0.000000000000000000, 1.000000000000000000 ) ) ;
#6704=ORIENTED_EDGE ( 'NONE', *, *, #46232, .F. ) ;
#6711=DIRECTION ( 'NONE',  ( 0.000000000000000000, 0.000000000000000000, 1.000000000000000000 ) ) ;
#6715=DIRECTION ( 'NONE',  ( -1.794541526872559352E-16, -1.000000000000000000, 0.000000000000000000 ) ) ;
#6726=CARTESIAN_POINT ( 'NONE',  ( 8.250000000000005329, 7.250000000000000888, -26.00000000000001066 ) ) ;
#6727=DIRECTION ( 'NONE',  ( -0.000000000000000000, -0.000000000000000000, 1.000000000000000000 ) ) ;
#6729=CYLINDRICAL_SURFACE ( 'NONE', #25600, 0.2000000000000005107 ) ;
#6730=CARTESIAN_POINT ( 'NONE',  ( 7.250000000000005329, 7.250000000000000888, -12.50000000000000000 ) ) ;
#6732=EDGE_CURVE ( 'NONE', #39723, #33795, #39811, .T. ) ;
#6733=CARTESIAN_POINT ( 'NONE',  ( -8.250000000000001776, -7.249999999999998224, -26.00000000000001066 ) ) ;
#6743=LINE ( 'NONE', #28312, #20077 ) ;
#6745=AXIS2_PLACEMENT_3D ( 'NONE', #63802, #57785, #41529 ) ;
#6753=VECTOR ( 'NONE', #2558, 1000.000000000000000 ) ;
#6756=CARTESIAN_POINT ( 'NONE',  ( -8.250000000000001776, -8.249999999999998224, -26.00000000000001066 ) ) ;
#6764=ORIENTED_EDGE ( 'NONE', *, *, #6778, .F. ) ;
#6767=CARTESIAN_POINT ( 'NONE',  ( -8.250000000000001776, -7.249999999999998224, -26.00000000000001066 ) ) ;
#6770=ORIENTED_EDGE ( 'NONE', *, *, #28912, .F. ) ;
#6776=EDGE_LOOP ( 'NONE', ( #40063, #55180, #40792, #33571 ) ) ;
#6778=EDGE_CURVE ( 'NONE', #54080, #29125, #29486, .T. ) ;
#6782=CIRCLE ( 'NONE', #65553, 0.1999999999999996503 ) ;
#6795=DIRECTION ( 'NONE',  ( -1.000000000000000000, 1.794541526872559352E-16, 0.000000000000000000 ) ) ;
#6797=CARTESIAN_POINT ( 'NONE',  ( 8.250000000000005329, -7.249999999999998224, -26.00000000000001066 ) ) ;
#6801=DIRECTION ( 'NONE',  ( 1.000000000000000000, 0.000000000000000000, 0.000000000000000000 ) ) ;
#6807=CIRCLE ( 'NONE', #35017, 1.000000000000000000 ) ;
#6809=ORIENTED_EDGE ( 'NONE', *, *, #52798, .T. ) ;
#6829=EDGE_LOOP ( 'NONE', ( #3905, #1059, #27044, #21559 ) ) ;
#6833=PLANE ( 'NONE',  #18340 ) ;
#6838=ORIENTED_EDGE ( 'NONE', *, *, #43361, .F. ) ;
#6846=EDGE_CURVE ( 'NONE', #3987, #7713, #64212, .T. ) ;
#6853=AXIS2_PLACEMENT_3D ( 'NONE', #31791, #69260, #53359 ) ;
#6854=PLANE ( 'NONE',  #42961 ) ;
#6858=ORIENTED_EDGE ( 'NONE', *, *, #37352, .T. ) ;
#6861=EDGE_CURVE ( 'NONE', #6534, #35816, #69502, .T. ) ;
#6871=EDGE_CURVE ( 'NONE', #24957, #55829, #63511, .T. ) ;
#6875=EDGE_CURVE ( 'NONE', #34406, #28873, #52110, .T. ) ;
#6880=DIRECTION ( 'NONE',  ( 0.000000000000000000, 0.000000000000000000, 1.000000000000000000 ) ) ;
#6885=EDGE_CURVE ( 'NONE', #29779, #3392, #25686, .T. ) ;
#6888=CARTESIAN_POINT ( 'NONE',  ( -7.250000000000000888, -8.249999999999998224, -26.00000000000001066 ) ) ;
#6889=CARTESIAN_POINT ( 'NONE',  ( 7.450000000000006395, 7.250000000000000888, -22.50000000000000000 ) ) ;
#6896=EDGE_CURVE ( 'NONE', #33218, #381, #63854, .T. ) ;
#6901=PLANE ( 'NONE',  #1071 ) ;
#6904=AXIS2_PLACEMENT_3D ( 'NONE', #41866, #63441, #36559 ) ;
#6908=CARTESIAN_POINT ( 'NONE',  ( 8.250000000000005329, 8.250000000000001776, -26.00000000000001066 ) ) ;
#6911=CARTESIAN_POINT ( 'NONE',  ( 7.450000000000003730, -7.249999999999997335, -17.50000000000000000 ) ) ;
#6915=FACE_OUTER_BOUND ( 'NONE', #18829, .T. ) ;
#6920=VERTEX_POINT ( 'NONE', #9768 ) ;
#6922=ORIENTED_EDGE ( 'NONE', *, *, #65268, .T. ) ;
#6951=ORIENTED_EDGE ( 'NONE', *, *, #55273, .T. ) ;
#6955=DIRECTION ( 'NONE',  ( -1.000000000000000000, 0.000000000000000000, 0.000000000000000000 ) ) ;
#6966=CARTESIAN_POINT ( 'NONE',  ( 7.250000000000005329, 8.250000000000001776, -26.00000000000001066 ) ) ;
#6972=EDGE_CURVE ( 'NONE', #35692, #2415, #59594, .T. ) ;
#6976=EDGE_CURVE ( 'NONE', #24784, #64534, #32381, .T. ) ;
#6991=DIRECTION ( 'NONE',  ( 0.000000000000000000, 0.000000000000000000, 1.000000000000000000 ) ) ;
#6993=VERTEX_POINT ( 'NONE', #50006 ) ;
#6997=ORIENTED_EDGE ( 'NONE', *, *, #6896, .T. ) ;
#6999=AXIS2_PLACEMENT_3D ( 'NONE', #48751, #25800, #21191 ) ;
#7021=TOROIDAL_SURFACE ( 'NONE', #5929, 0.06000000000000080963, 0.7500000000000000000 ) ;
#7022=VERTEX_POINT ( 'NONE', #28104 ) ;
#7026=LINE ( 'NONE', #50167, #59253 ) ;
#7052=CARTESIAN_POINT ( 'NONE',  ( 8.250000000000005329, -8.249999999999998224, -26.00000000000001066 ) ) ;
#7058=DIRECTION ( 'NONE',  ( 1.000000000000000000, 0.000000000000000000, 0.000000000000000000 ) ) ;
#7062=DIRECTION ( 'NONE',  ( 0.000000000000000000, 0.000000000000000000, 1.000000000000000000 ) ) ;
#7063=VECTOR ( 'NONE', #46353, 1000.000000000000000 ) ;
#7070=AXIS2_PLACEMENT_3D ( 'NONE', #17871, #13955, #60991 ) ;
#7072=ORIENTED_EDGE ( 'NONE', *, *, #54508, .F. ) ;
#7073=DIRECTION ( 'NONE',  ( 0.000000000000000000, 0.000000000000000000, 1.000000000000000000 ) ) ;
#7089=ORIENTED_EDGE ( 'NONE', *, *, #11221, .F. ) ;
#7091=EDGE_LOOP ( 'NONE', ( #44941, #6704, #46570, #48537 ) ) ;
#7097=FACE_OUTER_BOUND ( 'NONE', #30050, .T. ) ;
#7098=CARTESIAN_POINT ( 'NONE',  ( 7.250000000000005329, 7.250000000000000888, -12.00000000000000000 ) ) ;
#7105=CIRCLE ( 'NONE', #43263, 0.1999999999999996503 ) ;
#7109=VECTOR ( 'NONE', #43486, 1000.000000000000000 ) ;
#7112=ORIENTED_EDGE ( 'NONE', *, *, #12025, .F. ) ;
#7114=ORIENTED_EDGE ( 'NONE', *, *, #58238, .F. ) ;
#7119=ORIENTED_EDGE ( 'NONE', *, *, #61058, .F. ) ;
#7124=VERTEX_POINT ( 'NONE', #50700 ) ;
#7125=DIRECTION ( 'NONE',  ( -0.000000000000000000, -0.000000000000000000, -1.000000000000000000 ) ) ;
#7129=ORIENTED_EDGE ( 'NONE', *, *, #19563, .T. ) ;
#7130=CARTESIAN_POINT ( 'NONE',  ( -7.750000000000001776, -7.348062532927999158, 5.000000000000000000 ) ) ;
#7131=DIRECTION ( 'NONE',  ( -1.000000000000000000, 0.000000000000000000, 0.000000000000000000 ) ) ;
#7141=AXIS2_PLACEMENT_3D ( 'NONE', #65782, #6055, #55181 ) ;
#7142=VECTOR ( 'NONE', #34137, 1000.000000000000000 ) ;
#7149=AXIS2_PLACEMENT_3D ( 'NONE', #30175, #3653, #61632 ) ;
#7150=VERTEX_POINT ( 'NONE', #19575 ) ;
#7151=EDGE_CURVE ( 'NONE', #31478, #51178, #13576, .T. ) ;
#7156=LINE ( 'NONE', #39683, #24385 ) ;
#7163=FACE_OUTER_BOUND ( 'NONE', #11478, .T. ) ;
#7170=ORIENTED_EDGE ( 'NONE', *, *, #12463, .T. ) ;
#7173=DIRECTION ( 'NONE',  ( 1.000000000000000000, 0.000000000000000000, 0.000000000000000000 ) ) ;
#7180=ORIENTED_EDGE ( 'NONE', *, *, #1238, .F. ) ;
#7181=ORIENTED_EDGE ( 'NONE', *, *, #67951, .T. ) ;
#7186=SHAPE_REPRESENTATION_RELATIONSHIP ( 'NONE' , 'NONE' ,  #25847, #25951 ) ;
#7192=VERTEX_POINT ( 'NONE', #18172 ) ;
#7195=AXIS2_PLACEMENT_3D ( 'NONE', #2572, #24498, #35794 ) ;
#7204=VECTOR ( 'NONE', #49894, 1000.000000000000000 ) ;
#7209=EDGE_CURVE ( 'NONE', #17361, #8765, #29485, .T. ) ;
#7212=CARTESIAN_POINT ( 'NONE',  ( -7.250000000000001776, -7.249999999999998224, -10.00000000000000000 ) ) ;
#7213=CARTESIAN_POINT ( 'NONE',  ( -7.250000000000001776, -7.249999999999998224, -26.00000000000001066 ) ) ;
#7217=DIRECTION ( 'NONE',  ( -0.000000000000000000, -0.000000000000000000, -1.000000000000000000 ) ) ;
#7219=ORIENTED_EDGE ( 'NONE', *, *, #23038, .F. ) ;
#7231=EDGE_LOOP ( 'NONE', ( #37845, #3062, #64497, #58324 ) ) ;
#7234=CARTESIAN_POINT ( 'NONE',  ( -7.450000000000001954, 0.000000000000000000, -13.50000000000000178 ) ) ;
#7240=LINE ( 'NONE', #45074, #67045 ) ;
#7252=DIRECTION ( 'NONE',  ( 0.000000000000000000, 0.000000000000000000, 1.000000000000000000 ) ) ;
#7270=LINE ( 'NONE', #28493, #45552 ) ;
#7272=CARTESIAN_POINT ( 'NONE',  ( 6.500000000000000888, -6.500000000000002665, 0.000000000000000000 ) ) ;
#7276=AXIS2_PLACEMENT_3D ( 'NONE', #4607, #30768, #21552 ) ;
#7277=ORIENTED_EDGE ( 'NONE', *, *, #5785, .F. ) ;
#7287=ORIENTED_EDGE ( 'NONE', *, *, #51239, .F. ) ;
#7288=ADVANCED_FACE ( 'NONE', ( #46794, #36186 ), #20277, .T. ) ;
#7293=ORIENTED_EDGE ( 'NONE', *, *, #34820, .F. ) ;
#7295=ADVANCED_FACE ( 'NONE', ( #47843 ), #63421, .T. ) ;
#7297=DIRECTION ( 'NONE',  ( -0.000000000000000000, -0.000000000000000000, 1.000000000000000000 ) ) ;
#7302=FACE_OUTER_BOUND ( 'NONE', #57459, .T. ) ;
#7304=ORIENTED_EDGE ( 'NONE', *, *, #12600, .F. ) ;
#7313=DIRECTION ( 'NONE',  ( 0.000000000000000000, 0.000000000000000000, -1.000000000000000000 ) ) ;
#7314=FACE_OUTER_BOUND ( 'NONE', #29015, .T. ) ;
#7318=CARTESIAN_POINT ( 'NONE',  ( -6.749999999999998224, -7.348062532927999158, -5.000000000000000000 ) ) ;
#7320=EDGE_CURVE ( 'NONE', #63385, #55203, #69423, .T. ) ;
#7327=ORIENTED_EDGE ( 'NONE', *, *, #22311, .F. ) ;
#7333=DIRECTION ( 'NONE',  ( 0.000000000000000000, 0.000000000000000000, -1.000000000000000000 ) ) ;
#7334=EDGE_LOOP ( 'NONE', ( #47679, #1629, #62047, #11974, #13571, #39295, #43893, #49096 ) ) ;
#7348=VECTOR ( 'NONE', #49235, 1000.000000000000000 ) ;
#7349=FACE_OUTER_BOUND ( 'NONE', #58254, .T. ) ;
#7350=ORIENTED_EDGE ( 'NONE', *, *, #32909, .F. ) ;
#7382=LINE ( 'NONE', #34609, #51535 ) ;
#7390=FACE_BOUND ( 'NONE', #47949, .T. ) ;
#7403=LINE ( 'NONE', #28979, #25147 ) ;
#7405=CARTESIAN_POINT ( 'NONE',  ( 7.250000000000005329, -7.249999999999998224, -7.500000000000000000 ) ) ;
#7408=EDGE_CURVE ( 'NONE', #27819, #52415, #8508, .T. ) ;
#7411=AXIS2_PLACEMENT_3D ( 'NONE', #44465, #34196, #39177 ) ;
#7415=ADVANCED_FACE ( 'NONE', ( #12753 ), #61911, .T. ) ;
#7420=EDGE_CURVE ( 'NONE', #22431, #11380, #8157, .T. ) ;
#7428=DIRECTION ( 'NONE',  ( -1.794541526872559352E-16, -1.000000000000000000, 0.000000000000000000 ) ) ;
#7429=ADVANCED_FACE ( 'NONE', ( #13819 ), #45285, .T. ) ;
#7430=ORIENTED_EDGE ( 'NONE', *, *, #4273, .F. ) ;
#7441=ORIENTED_EDGE ( 'NONE', *, *, #41456, .T. ) ;
#7449=PLANE ( 'NONE',  #21802 ) ;
#7452=VECTOR ( 'NONE', #8145, 1000.000000000000000 ) ;
#7463=EDGE_CURVE ( 'NONE', #43093, #37823, #51299, .T. ) ;
#7475=CYLINDRICAL_SURFACE ( 'NONE', #50354, 0.2000000000000005107 ) ;
#7486=CARTESIAN_POINT ( 'NONE',  ( 9.690000000000001279, -8.750000000000000000, -7.000000000000000000 ) ) ;
#7493=LINE ( 'NONE', #66885, #8914 ) ;
#7497=CIRCLE ( 'NONE', #33453, 1.000000000000000000 ) ;
#7502=CARTESIAN_POINT ( 'NONE',  ( -7.250000000000000888, 7.250000000000001776, -11.50000000000000000 ) ) ;
#7506=CARTESIAN_POINT ( 'NONE',  ( -7.250000000000001776, -7.249999999999998224, -20.50000000000000000 ) ) ;
#7511=ADVANCED_FACE ( 'NONE', ( #24788 ), #58379, .T. ) ;
#7525=LINE ( 'NONE', #40032, #65907 ) ;
#7526=CARTESIAN_POINT ( 'NONE',  ( -7.250000000000000888, 7.450000000000003730, -7.000000000000000000 ) ) ;
#7535=FACE_OUTER_BOUND ( 'NONE', #49072, .T. ) ;
#7542=VECTOR ( 'NONE', #15538, 1000.000000000000000 ) ;
#7543=VECTOR ( 'NONE', #32120, 1000.000000000000000 ) ;
#7553=ORIENTED_EDGE ( 'NONE', *, *, #34487, .F. ) ;
#7554=EDGE_CURVE ( 'NONE', #67025, #52765, #26192, .T. ) ;
#7559=AXIS2_PLACEMENT_3D ( 'NONE', #42078, #59390, #63661 ) ;
#7566=DIRECTION ( 'NONE',  ( 1.000000000000000000, 0.000000000000000000, 0.000000000000000000 ) ) ;
#7570=AXIS2_PLACEMENT_3D ( 'NONE', #7052, #16655, #17677 ) ;
#7576=CYLINDRICAL_SURFACE ( 'NONE', #39581, 1.000000000000000000 ) ;
#7579=VERTEX_POINT ( 'NONE', #25848 ) ;
#7584=ORIENTED_EDGE ( 'NONE', *, *, #37136, .T. ) ;
#7586=DIRECTION ( 'NONE',  ( 0.000000000000000000, 0.000000000000000000, -1.000000000000000000 ) ) ;
#7590=AXIS2_PLACEMENT_3D ( 'NONE', #41591, #41231, #14379 ) ;
#7595=AXIS2_PLACEMENT_3D ( 'NONE', #14661, #48242, #5467 ) ;
#7596=VECTOR ( 'NONE', #56360, 1000.000000000000000 ) ;
#7601=EDGE_CURVE ( 'NONE', #31478, #6447, #30790, .T. ) ;
#7608=CARTESIAN_POINT ( 'NONE',  ( 7.250000000000005329, -7.249999999999998224, -13.00000000000000178 ) ) ;
#7611=EDGE_CURVE ( 'NONE', #9455, #66129, #3923, .T. ) ;
#7617=ORIENTED_EDGE ( 'NONE', *, *, #50070, .F. ) ;
#7621=ORIENTED_EDGE ( 'NONE', *, *, #11353, .T. ) ;
#7623=VERTEX_POINT ( 'NONE', #4628 ) ;
#7627=CARTESIAN_POINT ( 'NONE',  ( -7.450000000000001954, 0.000000000000000000, -18.50000000000000000 ) ) ;
#7629=DIRECTION ( 'NONE',  ( 0.000000000000000000, 1.000000000000000000, -0.000000000000000000 ) ) ;
#7644=DIRECTION ( 'NONE',  ( 1.000000000000000000, -5.981805089575194965E-17, 0.000000000000000000 ) ) ;
#7656=FACE_OUTER_BOUND ( 'NONE', #43311, .T. ) ;
#7657=CARTESIAN_POINT ( 'NONE',  ( -7.250000000000000888, 7.250000000000001776, -26.00000000000001066 ) ) ;
#7658=EDGE_CURVE ( 'NONE', #7150, #46624, #15927, .T. ) ;
#7663=LINE ( 'NONE', #44792, #68016 ) ;
#7664=DIRECTION ( 'NONE',  ( -0.000000000000000000, -0.000000000000000000, -1.000000000000000000 ) ) ;
#7668=CARTESIAN_POINT ( 'NONE',  ( -6.500000000000002665, -6.500000000000002665, 0.000000000000000000 ) ) ;
#7669=FACE_OUTER_BOUND ( 'NONE', #33048, .T. ) ;
#7670=DIRECTION ( 'NONE',  ( 0.000000000000000000, 0.000000000000000000, 1.000000000000000000 ) ) ;
#7693=ORIENTED_EDGE ( 'NONE', *, *, #66040, .T. ) ;
#7694=CARTESIAN_POINT ( 'NONE',  ( 7.250000000000005329, -7.249999999999998224, -7.500000000000000000 ) ) ;
#7699=ORIENTED_EDGE ( 'NONE', *, *, #17158, .F. ) ;
#7710=DIRECTION ( 'NONE',  ( 0.000000000000000000, -0.000000000000000000, 1.000000000000000000 ) ) ;
#7712=CYLINDRICAL_SURFACE ( 'NONE', #34440, 0.2000000000000005107 ) ;
#7713=VERTEX_POINT ( 'NONE', #17558 ) ;
#7719=FACE_OUTER_BOUND ( 'NONE', #55457, .T. ) ;
#7733=FACE_OUTER_BOUND ( 'NONE', #36382, .T. ) ;
#7738=LINE ( 'NONE', #61474, #47085 ) ;
#7750=ADVANCED_FACE ( 'NONE', ( #28171 ), #67037, .F. ) ;
#7752=CARTESIAN_POINT ( 'NONE',  ( 7.450000000000004619, -1.336933437520057563E-15, -11.50000000000000000 ) ) ;
#7753=CARTESIAN_POINT ( 'NONE',  ( 0.000000000000000000, 8.250000000000001776, -17.50000000000000000 ) ) ;
#7754=ORIENTED_EDGE ( 'NONE', *, *, #32880, .T. ) ;
#7793=AXIS2_PLACEMENT_3D ( 'NONE', #13500, #19852, #62634 ) ;
#7794=DIRECTION ( 'NONE',  ( -1.000000000000000000, 0.000000000000000000, -0.000000000000000000 ) ) ;
#7798=DIRECTION ( 'NONE',  ( 1.000000000000000000, 0.000000000000000000, 0.000000000000000000 ) ) ;
#7801=ORIENTED_EDGE ( 'NONE', *, *, #3359, .T. ) ;
#7806=EDGE_CURVE ( 'NONE', #6525, #31517, #36616, .T. ) ;
#7809=ORIENTED_EDGE ( 'NONE', *, *, #4058, .T. ) ;
#7816=ORIENTED_EDGE ( 'NONE', *, *, #64884, .T. ) ;
#7821=CARTESIAN_POINT ( 'NONE',  ( 7.250000000000005329, -8.249999999999998224, -16.50000000000000000 ) ) ;
#7822=DIRECTION ( 'NONE',  ( 0.000000000000000000, 0.000000000000000000, 1.000000000000000000 ) ) ;
#7826=CARTESIAN_POINT ( 'NONE',  ( -7.250000000000000888, 8.250000000000001776, -26.00000000000001066 ) ) ;
#7827=LINE ( 'NONE', #55934, #53817 ) ;
#7830=DIRECTION ( 'NONE',  ( -1.794541526872559352E-16, -1.000000000000000000, 0.000000000000000000 ) ) ;
#7833=VERTEX_POINT ( 'NONE', #19299 ) ;
#7839=CARTESIAN_POINT ( 'NONE',  ( 8.250000000000005329, 7.250000000000000888, -26.00000000000001066 ) ) ;
#7840=CARTESIAN_POINT ( 'NONE',  ( 7.250000000000005329, 7.250000000000000888, -24.00000000000000000 ) ) ;
#7843=AXIS2_PLACEMENT_3D ( 'NONE', #66117, #39580, #7058 ) ;
#7845=VERTEX_POINT ( 'NONE', #20356 ) ;
#7847=ORIENTED_EDGE ( 'NONE', *, *, #4942, .F. ) ;
#7851=DIRECTION ( 'NONE',  ( 1.000000000000000000, 0.000000000000000000, 0.000000000000000000 ) ) ;
#7862=CARTESIAN_POINT ( 'NONE',  ( 7.250000000000005329, 7.250000000000000888, -26.00000000000001066 ) ) ;
#7863=VERTEX_POINT ( 'NONE', #45825 ) ;
#7865=FACE_OUTER_BOUND ( 'NONE', #40559, .T. ) ;
#7872=CARTESIAN_POINT ( 'NONE',  ( 7.250000000000005329, 7.250000000000000888, -15.00000000000000000 ) ) ;
#7876=CARTESIAN_POINT ( 'NONE',  ( -7.450000000000001954, 0.000000000000000000, -18.50000000000000000 ) ) ;
#7880=VERTEX_POINT ( 'NONE', #35922 ) ;
#7881=VERTEX_POINT ( 'NONE', #51126 ) ;
#7892=AXIS2_PLACEMENT_3D ( 'NONE', #45147, #35226, #28885 ) ;
#7897=ADVANCED_FACE ( 'NONE', ( #51839 ), #63502, .T. ) ;
#7907=AXIS2_PLACEMENT_3D ( 'NONE', #24134, #13521, #29429 ) ;
#7910=EDGE_CURVE ( 'NONE', #32512, #38612, #3743, .T. ) ;
#7924=AXIS2_PLACEMENT_3D ( 'NONE', #40258, #2774, #51929 ) ;
#7927=CARTESIAN_POINT ( 'NONE',  ( 0.000000000000000000, 0.000000000000000000, -14.00000000000000000 ) ) ;
#7928=DIRECTION ( 'NONE',  ( 0.000000000000000000, 0.000000000000000000, 1.000000000000000000 ) ) ;
#7941=EDGE_CURVE ( 'NONE', #27762, #9056, #15056, .T. ) ;
#7949=CARTESIAN_POINT ( 'NONE',  ( -7.250000000000001776, -7.249999999999998224, -26.00000000000001066 ) ) ;
#7950=EDGE_CURVE ( 'NONE', #52765, #43546, #19196, .T. ) ;
#7951=CARTESIAN_POINT ( 'NONE',  ( 7.250000000000005329, 7.250000000000000888, -7.500000000000000000 ) ) ;
#7955=LINE ( 'NONE', #29880, #10400 ) ;
#7956=ORIENTED_EDGE ( 'NONE', *, *, #45108, .T. ) ;
#7962=FACE_OUTER_BOUND ( 'NONE', #1558, .T. ) ;
#7966=VERTEX_POINT ( 'NONE', #37674 ) ;
#7969=CARTESIAN_POINT ( 'NONE',  ( 0.000000000000000000, 8.250000000000001776, -21.00000000000000000 ) ) ;
#7977=ORIENTED_EDGE ( 'NONE', *, *, #14557, .T. ) ;
#7980=EDGE_CURVE ( 'NONE', #7863, #30319, #36154, .T. ) ;
#7987=EDGE_CURVE ( 'NONE', #29792, #56057, #31633, .T. ) ;
#7989=ORIENTED_EDGE ( 'NONE', *, *, #58161, .T. ) ;
#7994=FACE_OUTER_BOUND ( 'NONE', #21298, .T. ) ;
#8003=ORIENTED_EDGE ( 'NONE', *, *, #2282, .T. ) ;
#8010=ORIENTED_EDGE ( 'NONE', *, *, #8666, .F. ) ;
#8021=CARTESIAN_POINT ( 'NONE',  ( -7.250000000000001776, -7.249999999999998224, -22.00000000000000000 ) ) ;
#8023=LINE ( 'NONE', #29597, #26724 ) ;
#8028=CARTESIAN_POINT ( 'NONE',  ( 8.250000000000005329, 7.250000000000000888, -16.00000000000000000 ) ) ;
#8036=DIRECTION ( 'NONE',  ( -0.000000000000000000, -0.000000000000000000, 1.000000000000000000 ) ) ;
#8048=AXIS2_PLACEMENT_3D ( 'NONE', #52426, #8924, #20588 ) ;
#8070=VERTEX_POINT ( 'NONE', #22104 ) ;
#8089=ORIENTED_EDGE ( 'NONE', *, *, #34965, .F. ) ;
#8097=LINE ( 'NONE', #23668, #30801 ) ;
#8116=EDGE_CURVE ( 'NONE', #9056, #31600, #59926, .T. ) ;
#8119=ORIENTED_EDGE ( 'NONE', *, *, #17853, .T. ) ;
#8121=ORIENTED_EDGE ( 'NONE', *, *, #67934, .F. ) ;
#8127=EDGE_CURVE ( 'NONE', #24527, #69756, #50350, .T. ) ;
#8137=CARTESIAN_POINT ( 'NONE',  ( -8.250000000000001776, 7.250000000000000888, -26.00000000000001066 ) ) ;
#8138=CARTESIAN_POINT ( 'NONE',  ( -9.690000000000001279, 8.750000000000000000, -7.000000000000000000 ) ) ;
#8144=DIRECTION ( 'NONE',  ( 0.000000000000000000, 0.000000000000000000, 1.000000000000000000 ) ) ;
#8145=DIRECTION ( 'NONE',  ( 1.000000000000000000, -0.000000000000000000, 0.000000000000000000 ) ) ;
#8149=EDGE_CURVE ( 'NONE', #35485, #35045, #34415, .T. ) ;
#8157=LINE ( 'NONE', #50608, #45072 ) ;
#8159=EDGE_CURVE ( 'NONE', #32818, #67039, #13569, .T. ) ;
#8162=ADVANCED_FACE ( 'NONE', ( #49336 ), #18168, .T. ) ;
#8171=ORIENTED_EDGE ( 'NONE', *, *, #41775, .F. ) ;
#8178=DIRECTION ( 'NONE',  ( -1.000000000000000000, 0.000000000000000000, 0.000000000000000000 ) ) ;
#8181=VECTOR ( 'NONE', #47970, 1000.000000000000000 ) ;
#8182=CARTESIAN_POINT ( 'NONE',  ( 0.000000000000000000, -8.249999999999998224, -9.000000000000001776 ) ) ;
#8193=DIRECTION ( 'NONE',  ( -0.000000000000000000, -0.000000000000000000, 1.000000000000000000 ) ) ;
#8195=CARTESIAN_POINT ( 'NONE',  ( 8.250000000000005329, 0.000000000000000000, -14.00000000000000000 ) ) ;
#8207=ORIENTED_EDGE ( 'NONE', *, *, #1848, .F. ) ;
#8214=CARTESIAN_POINT ( 'NONE',  ( 7.250000000000005329, -7.249999999999998224, -26.00000000000001066 ) ) ;
#8217=LINE ( 'NONE', #35084, #59164 ) ;
#8220=DIRECTION ( 'NONE',  ( -1.000000000000000000, 0.000000000000000000, 0.000000000000000000 ) ) ;
#8234=VERTEX_POINT ( 'NONE', #61648 ) ;
#8247=ORIENTED_EDGE ( 'NONE', *, *, #35254, .F. ) ;
#8256=LINE ( 'NONE', #29832, #32372 ) ;
#8273=DIRECTION ( 'NONE',  ( -1.000000000000000000, 0.000000000000000000, 0.000000000000000000 ) ) ;
#8274=CARTESIAN_POINT ( 'NONE',  ( -8.250000000000001776, 0.000000000000000000, -13.50000000000000178 ) ) ;
#8285=EDGE_LOOP ( 'NONE', ( #2956, #31235, #12427, #6001 ) ) ;
#8296=EDGE_CURVE ( 'NONE', #1150, #23929, #23708, .T. ) ;
#8298=CARTESIAN_POINT ( 'NONE',  ( -7.250000000000000888, -8.249999999999998224, -10.00000000000000000 ) ) ;
#8300=EDGE_CURVE ( 'NONE', #47005, #21718, #67320, .T. ) ;
#8303=ORIENTED_EDGE ( 'NONE', *, *, #57259, .F. ) ;
#8311=ORIENTED_EDGE ( 'NONE', *, *, #31074, .T. ) ;
#8317=VECTOR ( 'NONE', #3992, 1000.000000000000000 ) ;
#8321=CYLINDRICAL_SURFACE ( 'NONE', #10301, 1.000000000000000000 ) ;
#8324=DIRECTION ( 'NONE',  ( -0.000000000000000000, -0.000000000000000000, -1.000000000000000000 ) ) ;
#8325=ORIENTED_EDGE ( 'NONE', *, *, #11548, .T. ) ;
#8327=FACE_OUTER_BOUND ( 'NONE', #30881, .T. ) ;
#8334=EDGE_LOOP ( 'NONE', ( #61610, #11368, #39362, #5758, #30982, #22450, #5236, #28060 ) ) ;
#8343=EDGE_CURVE ( 'NONE', #29056, #23638, #20969, .T. ) ;
#8346=LINE ( 'NONE', #40877, #54120 ) ;
#8352=ORIENTED_EDGE ( 'NONE', *, *, #3767, .T. ) ;
#8355=PLANE ( 'NONE',  #16622 ) ;
#8363=PLANE ( 'NONE',  #7892 ) ;
#8374=CARTESIAN_POINT ( 'NONE',  ( -8.250000000000001776, -7.249999999999998224, -26.00000000000001066 ) ) ;
#8376=CARTESIAN_POINT ( 'NONE',  ( 7.250000000000005329, -8.249999999999998224, -26.00000000000001066 ) ) ;
#8377=CARTESIAN_POINT ( 'NONE',  ( -7.250000000000000888, -8.249999999999998224, -14.50000000000000000 ) ) ;
#8385=EDGE_CURVE ( 'NONE', #13221, #39386, #23763, .T. ) ;
#8390=CIRCLE ( 'NONE', #42330, 1.000000000000000000 ) ;
#8404=DIRECTION ( 'NONE',  ( -1.000000000000000000, 0.000000000000000000, 0.000000000000000000 ) ) ;
#8411=DIRECTION ( 'NONE',  ( -1.000000000000000000, 0.000000000000000000, 0.000000000000000000 ) ) ;
#8412=VERTEX_POINT ( 'NONE', #14978 ) ;
#8438=DIRECTION ( 'NONE',  ( 0.000000000000000000, -1.000000000000000000, 0.000000000000000000 ) ) ;
#8443=CARTESIAN_POINT ( 'NONE',  ( 0.000000000000000000, 8.250000000000001776, -16.50000000000000000 ) ) ;
#8444=LINE ( 'NONE', #30024, #27169 ) ;
#8445=EDGE_CURVE ( 'NONE', #3293, #26867, #43235, .T. ) ;
#8446=LINE ( 'NONE', #7753, #27420 ) ;
#8453=AXIS2_PLACEMENT_3D ( 'NONE', #11298, #32878, #54453 ) ;
#8455=AXIS2_PLACEMENT_3D ( 'NONE', #35019, #13809, #56595 ) ;
#8463=DIRECTION ( 'NONE',  ( 0.000000000000000000, 0.000000000000000000, 1.000000000000000000 ) ) ;
#8467=EDGE_CURVE ( 'NONE', #9839, #63180, #36905, .T. ) ;
#8469=VECTOR ( 'NONE', #18987, 1000.000000000000000 ) ;
#8476=ORIENTED_EDGE ( 'NONE', *, *, #27950, .F. ) ;
#8477=DIRECTION ( 'NONE',  ( -1.000000000000000000, 0.000000000000000000, 0.000000000000000000 ) ) ;
#8484=ADVANCED_FACE ( 'NONE', ( #55921 ), #22711, .F. ) ;
#8486=DIRECTION ( 'NONE',  ( -0.000000000000000000, -0.000000000000000000, 1.000000000000000000 ) ) ;
#8488=ORIENTED_EDGE ( 'NONE', *, *, #65667, .T. ) ;
#8502=EDGE_LOOP ( 'NONE', ( #27662, #41831, #11526, #23538 ) ) ;
#8508=LINE ( 'NONE', #2859, #19140 ) ;
#8515=EDGE_LOOP ( 'NONE', ( #13883, #6267, #57039, #64298 ) ) ;
#8518=VECTOR ( 'NONE', #53680, 1000.000000000000000 ) ;
#8527=DIRECTION ( 'NONE',  ( 0.000000000000000000, 0.000000000000000000, -1.000000000000000000 ) ) ;
#8529=DIRECTION ( 'NONE',  ( 0.000000000000000000, 0.000000000000000000, 1.000000000000000000 ) ) ;
#8531=DIRECTION ( 'NONE',  ( -1.000000000000000000, 0.000000000000000000, 0.000000000000000000 ) ) ;
#8534=CARTESIAN_POINT ( 'NONE',  ( 7.749999999999998224, -7.348062532928000934, -5.000000000000000000 ) ) ;
#8542=AXIS2_PLACEMENT_3D ( 'NONE', #58207, #26040, #47597 ) ;
#8545=DIRECTION ( 'NONE',  ( -1.000000000000000000, 0.000000000000000000, 0.000000000000000000 ) ) ;
#8554=AXIS2_PLACEMENT_3D ( 'NONE', #14619, #24882, #35837 ) ;
#8562=ORIENTED_EDGE ( 'NONE', *, *, #14633, .F. ) ;
#8564=CIRCLE ( 'NONE', #46987, 0.1999999999999987899 ) ;
#8574=DIRECTION ( 'NONE',  ( 0.000000000000000000, 0.000000000000000000, 1.000000000000000000 ) ) ;
#8583=FACE_BOUND ( 'NONE', #35696, .T. ) ;
#8588=EDGE_CURVE ( 'NONE', #7713, #31930, #21501, .T. ) ;
#8595=ORIENTED_EDGE ( 'NONE', *, *, #6160, .F. ) ;
#8601=VECTOR ( 'NONE', #37727, 1000.000000000000000 ) ;
#8604=ORIENTED_EDGE ( 'NONE', *, *, #50935, .T. ) ;
#8619=ADVANCED_FACE ( 'NONE', ( #60869 ), #12417, .F. ) ;
#8643=EDGE_CURVE ( 'NONE', #34571, #15298, #56956, .T. ) ;
#8644=EDGE_CURVE ( 'NONE', #17879, #42683, #41402, .T. ) ;
#8648=EDGE_CURVE ( 'NONE', #5578, #27416, #56619, .T. ) ;
#8650=ORIENTED_EDGE ( 'NONE', *, *, #11174, .T. ) ;
#8666=EDGE_CURVE ( 'NONE', #34716, #47806, #35266, .T. ) ;
#8668=LINE ( 'NONE', #41184, #17062 ) ;
#8677=VECTOR ( 'NONE', #47772, 1000.000000000000000 ) ;
#8679=DIRECTION ( 'NONE',  ( 1.000000000000000000, 0.000000000000000000, 0.000000000000000000 ) ) ;
#8684=FACE_OUTER_BOUND ( 'NONE', #11055, .T. ) ;
#8690=ORIENTED_EDGE ( 'NONE', *, *, #38049, .F. ) ;
#8701=CARTESIAN_POINT ( 'NONE',  ( 8.250000000000005329, -7.249999999999998224, -11.00000000000000000 ) ) ;
#8705=EDGE_CURVE ( 'NONE', #40067, #43546, #56268, .T. ) ;
#8717=AXIS2_PLACEMENT_3D ( 'NONE', #43681, #16810, #6192 ) ;
#8721=ORIENTED_EDGE ( 'NONE', *, *, #46386, .F. ) ;
#8725=CIRCLE ( 'NONE', #57282, 0.1999999999999996503 ) ;
#8731=LINE ( 'NONE', #35583, #4191 ) ;
#8740=DIRECTION ( 'NONE',  ( -1.000000000000000000, 0.000000000000000000, 0.000000000000000000 ) ) ;
#8745=LINE ( 'NONE', #4158, #53603 ) ;
#8759=CIRCLE ( 'NONE', #43747, 0.2000000000000005107 ) ;
#8762=ORIENTED_EDGE ( 'NONE', *, *, #12600, .T. ) ;
#8765=VERTEX_POINT ( 'NONE', #4298 ) ;
#8771=DIRECTION ( 'NONE',  ( -1.794541526872559352E-16, -1.000000000000000000, 0.000000000000000000 ) ) ;
#8778=ORIENTED_EDGE ( 'NONE', *, *, #42655, .T. ) ;
#8788=LINE ( 'NONE', #45550, #41584 ) ;
#8794=EDGE_CURVE ( 'NONE', #41582, #15537, #47754, .T. ) ;
#8799=EDGE_CURVE ( 'NONE', #25281, #40029, #45469, .T. ) ;
#8800=DIRECTION ( 'NONE',  ( 0.000000000000000000, 0.000000000000000000, 1.000000000000000000 ) ) ;
#8801=EDGE_CURVE ( 'NONE', #34713, #3293, #68638, .T. ) ;
#8807=ORIENTED_EDGE ( 'NONE', *, *, #24679, .T. ) ;
#8812=CARTESIAN_POINT ( 'NONE',  ( -7.250000000000001776, -7.249999999999998224, -24.00000000000000000 ) ) ;
#8829=DIRECTION ( 'NONE',  ( 0.000000000000000000, 0.000000000000000000, -1.000000000000000000 ) ) ;
#8834=VERTEX_POINT ( 'NONE', #26199 ) ;
#8836=ORIENTED_EDGE ( 'NONE', *, *, #65005, .T. ) ;
#8844=LINE ( 'NONE', #4946, #62625 ) ;
#8850=ORIENTED_EDGE ( 'NONE', *, *, #52435, .F. ) ;
#8855=ORIENTED_EDGE ( 'NONE', *, *, #59425, .F. ) ;
#8865=AXIS2_PLACEMENT_3D ( 'NONE', #7872, #2932, #18843 ) ;
#8873=ORIENTED_EDGE ( 'NONE', *, *, #42578, .T. ) ;
#8874=CARTESIAN_POINT ( 'NONE',  ( 8.250000000000005329, 7.250000000000000888, -26.00000000000001066 ) ) ;
#8875=DIRECTION ( 'NONE',  ( 0.000000000000000000, 0.000000000000000000, 1.000000000000000000 ) ) ;
#8892=EDGE_CURVE ( 'NONE', #14806, #39018, #52311, .T. ) ;
#8894=ORIENTED_EDGE ( 'NONE', *, *, #24471, .T. ) ;
#8911=FACE_OUTER_BOUND ( 'NONE', #1105, .T. ) ;
#8914=VECTOR ( 'NONE', #49597, 1000.000000000000000 ) ;
#8918=EDGE_CURVE ( 'NONE', #47489, #33326, #23312, .T. ) ;
#8921=CARTESIAN_POINT ( 'NONE',  ( 8.250000000000005329, -8.249999999999998224, -26.00000000000001066 ) ) ;
#8922=ORIENTED_EDGE ( 'NONE', *, *, #10008, .T. ) ;
#8924=DIRECTION ( 'NONE',  ( -0.000000000000000000, -0.000000000000000000, 1.000000000000000000 ) ) ;
#8931=DIRECTION ( 'NONE',  ( -0.000000000000000000, -0.000000000000000000, 1.000000000000000000 ) ) ;
#8946=ORIENTED_EDGE ( 'NONE', *, *, #50529, .T. ) ;
#8947=EDGE_LOOP ( 'NONE', ( #5966, #13, #68988, #35731 ) ) ;
#8953=EDGE_CURVE ( 'NONE', #57125, #28928, #33909, .T. ) ;
#8962=AXIS2_PLACEMENT_3D ( 'NONE', #54778, #6336, #33547 ) ;
#8967=CARTESIAN_POINT ( 'NONE',  ( 7.250000000000005329, -7.249999999999998224, -15.50000000000000000 ) ) ;
#8974=AXIS2_PLACEMENT_3D ( 'NONE', #25628, #31631, #25977 ) ;
#8975=DIRECTION ( 'NONE',  ( 0.000000000000000000, 0.000000000000000000, 1.000000000000000000 ) ) ;
#8976=EDGE_CURVE ( 'NONE', #7863, #21985, #17305, .T. ) ;
#8979=EDGE_CURVE ( 'NONE', #26426, #19122, #66444, .T. ) ;
#8984=DIRECTION ( 'NONE',  ( -1.000000000000000000, 0.000000000000000000, 0.000000000000000000 ) ) ;
#8987=DIRECTION ( 'NONE',  ( 0.000000000000000000, 1.000000000000000000, -0.000000000000000000 ) ) ;
#8988=ORIENTED_EDGE ( 'NONE', *, *, #22127, .F. ) ;
#8993=AXIS2_PLACEMENT_3D ( 'NONE', #37500, #59055, #63680 ) ;
#8997=DIRECTION ( 'NONE',  ( 1.000000000000000000, 0.000000000000000000, 0.000000000000000000 ) ) ;
#8999=EDGE_LOOP ( 'NONE', ( #1053, #19055, #69925, #11746 ) ) ;
#9002=LINE ( 'NONE', #25276, #20987 ) ;
#9006=ORIENTED_EDGE ( 'NONE', *, *, #63531, .T. ) ;
#9011=EDGE_CURVE ( 'NONE', #49703, #22032, #39560, .T. ) ;
#9012=AXIS2_PLACEMENT_3D ( 'NONE', #8021, #46211, #35236 ) ;
#9014=CARTESIAN_POINT ( 'NONE',  ( -7.250000000000001776, -7.249999999999998224, -25.50000000000000355 ) ) ;
#9016=VERTEX_POINT ( 'NONE', #16640 ) ;
#9028=PLANE ( 'NONE',  #6109 ) ;
#9030=CARTESIAN_POINT ( 'NONE',  ( 7.250000000000005329, -7.249999999999998224, -24.50000000000000000 ) ) ;
#9042=ORIENTED_EDGE ( 'NONE', *, *, #65667, .F. ) ;
#9046=ORIENTED_EDGE ( 'NONE', *, *, #19743, .F. ) ;
#9056=VERTEX_POINT ( 'NONE', #28960 ) ;
#9062=PLANE ( 'NONE',  #41682 ) ;
#9064=VERTEX_POINT ( 'NONE', #61121 ) ;
#9065=EDGE_CURVE ( 'NONE', #18073, #6054, #2438, .T. ) ;
#9086=CYLINDRICAL_SURFACE ( 'NONE', #38015, 0.2000000000000005107 ) ;
#9093=LINE ( 'NONE', #30662, #5279 ) ;
#9095=DIRECTION ( 'NONE',  ( 1.000000000000000000, 0.000000000000000000, 0.000000000000000000 ) ) ;
#9098=ORIENTED_EDGE ( 'NONE', *, *, #24940, .T. ) ;
#9117=AXIS2_PLACEMENT_3D ( 'NONE', #30367, #14809, #2784 ) ;
#9118=EDGE_LOOP ( 'NONE', ( #56618, #11410, #57057, #11860 ) ) ;
#9122=VECTOR ( 'NONE', #46018, 1000.000000000000000 ) ;
#9128=DIRECTION ( 'NONE',  ( -0.000000000000000000, -0.000000000000000000, -1.000000000000000000 ) ) ;
#9134=ADVANCED_FACE ( 'NONE', ( #61470 ), #29297, .F. ) ;
#9143=VERTEX_POINT ( 'NONE', #23650 ) ;
#9149=CARTESIAN_POINT ( 'NONE',  ( -8.750000000000003553, -7.348062532927999158, 0.000000000000000000 ) ) ;
#9158=EDGE_CURVE ( 'NONE', #48640, #21736, #51669, .T. ) ;
#9159=ORIENTED_EDGE ( 'NONE', *, *, #8976, .T. ) ;
#9160=CARTESIAN_POINT ( 'NONE',  ( 0.000000000000000000, 8.250000000000001776, -19.00000000000000000 ) ) ;
#9191=AXIS2_PLACEMENT_3D ( 'NONE', #57594, #40281, #19063 ) ;
#9195=DIRECTION ( 'NONE',  ( 0.000000000000000000, 0.000000000000000000, 1.000000000000000000 ) ) ;
#9202=CARTESIAN_POINT ( 'NONE',  ( 7.250000000000005329, -8.249999999999998224, -10.50000000000000000 ) ) ;
#9203=FACE_BOUND ( 'NONE', #49730, .T. ) ;
#9208=LINE ( 'NONE', #40671, #56671 ) ;
#9232=ORIENTED_EDGE ( 'NONE', *, *, #33138, .F. ) ;
#9235=EDGE_LOOP ( 'NONE', ( #7181, #491, #48697, #13238 ) ) ;
#9240=ADVANCED_FACE ( 'NONE', ( #57582 ), #63598, .T. ) ;
#9242=LINE ( 'NONE', #39989, #9122 ) ;
#9249=DIRECTION ( 'NONE',  ( 0.000000000000000000, 0.000000000000000000, -1.000000000000000000 ) ) ;
#9251=LINE ( 'NONE', #36464, #6428 ) ;
#9253=EDGE_CURVE ( 'NONE', #26084, #50433, #21202, .T. ) ;
#9256=DIRECTION ( 'NONE',  ( 0.000000000000000000, 0.000000000000000000, 1.000000000000000000 ) ) ;
#9259=DIRECTION ( 'NONE',  ( -1.794541526872559352E-16, -1.000000000000000000, 0.000000000000000000 ) ) ;
#9260=ORIENTED_EDGE ( 'NONE', *, *, #50619, .T. ) ;
#9280=VECTOR ( 'NONE', #43021, 1000.000000000000000 ) ;
#9284=ORIENTED_EDGE ( 'NONE', *, *, #2100, .F. ) ;
#9287=ORIENTED_EDGE ( 'NONE', *, *, #7209, .F. ) ;
#9301=ORIENTED_EDGE ( 'NONE', *, *, #725, .F. ) ;
#9309=DIRECTION ( 'NONE',  ( 0.000000000000000000, 0.000000000000000000, 1.000000000000000000 ) ) ;
#9318=ORIENTED_EDGE ( 'NONE', *, *, #20893, .T. ) ;
#9321=AXIS2_PLACEMENT_3D ( 'NONE', #62191, #13755, #35306 ) ;
#9325=DIRECTION ( 'NONE',  ( -1.000000000000000000, 0.000000000000000000, -0.000000000000000000 ) ) ;
#9327=AXIS2_PLACEMENT_3D ( 'NONE', #64792, #16705, #11041 ) ;
#9328=LINE ( 'NONE', #46797, #48175 ) ;
#9344=VECTOR ( 'NONE', #55695, 1000.000000000000000 ) ;
#9346=EDGE_CURVE ( 'NONE', #14806, #39001, #11228, .T. ) ;
#9347=DIRECTION ( 'NONE',  ( 0.000000000000000000, 0.000000000000000000, -1.000000000000000000 ) ) ;
#9349=ADVANCED_FACE ( 'NONE', ( #27155 ), #17221, .F. ) ;
#9355=DIRECTION ( 'NONE',  ( -5.981805089575196197E-17, -1.000000000000000000, 0.000000000000000000 ) ) ;
#9359=CARTESIAN_POINT ( 'NONE',  ( -7.250000000000001776, -7.249999999999998224, -26.00000000000001066 ) ) ;
#9363=VECTOR ( 'NONE', #9719, 1000.000000000000000 ) ;
#9390=CIRCLE ( 'NONE', #39838, 0.2000000000000005107 ) ;
#9395=DIRECTION ( 'NONE',  ( -0.000000000000000000, -0.000000000000000000, 1.000000000000000000 ) ) ;
#9401=DIRECTION ( 'NONE',  ( -0.000000000000000000, -0.000000000000000000, -1.000000000000000000 ) ) ;
#9406=DIRECTION ( 'NONE',  ( -1.000000000000000000, 0.000000000000000000, 0.000000000000000000 ) ) ;
#9419=DIRECTION ( 'NONE',  ( 1.000000000000000000, 0.000000000000000000, 0.000000000000000000 ) ) ;
#9422=FACE_OUTER_BOUND ( 'NONE', #37927, .T. ) ;
#9430=CARTESIAN_POINT ( 'NONE',  ( 7.250000000000004441, 7.450000000000001954, -14.00000000000000000 ) ) ;
#9431=CARTESIAN_POINT ( 'NONE',  ( 7.250000000000005329, 8.250000000000001776, -22.00000000000000000 ) ) ;
#9432=VECTOR ( 'NONE', #60815, 1000.000000000000000 ) ;
#9448=CARTESIAN_POINT ( 'NONE',  ( -7.250000000000000888, 7.250000000000001776, -26.00000000000001066 ) ) ;
#9451=VECTOR ( 'NONE', #65161, 1000.000000000000000 ) ;
#9452=DIRECTION ( 'NONE',  ( 1.000000000000000000, 0.000000000000000000, 0.000000000000000000 ) ) ;
#9455=VERTEX_POINT ( 'NONE', #2693 ) ;
#9456=CARTESIAN_POINT ( 'NONE',  ( -7.250000000000001776, -7.249999999999998224, -26.00000000000001066 ) ) ;
#9471=EDGE_CURVE ( 'NONE', #33973, #15671, #66367, .T. ) ;
#9473=CARTESIAN_POINT ( 'NONE',  ( -7.250000000000000888, 8.250000000000001776, -26.00000000000001066 ) ) ;
#9474=LINE ( 'NONE', #41286, #58154 ) ;
#9475=EDGE_LOOP ( 'NONE', ( #43140, #32942, #24178, #29793 ) ) ;
#9481=VERTEX_POINT ( 'NONE', #23220 ) ;
#9491=VERTEX_POINT ( 'NONE', #1646 ) ;
#9492=VECTOR ( 'NONE', #49627, 1000.000000000000000 ) ;
#9501=ORIENTED_EDGE ( 'NONE', *, *, #13183, .T. ) ;
#9504=CARTESIAN_POINT ( 'NONE',  ( 8.250000000000005329, 0.000000000000000000, -20.00000000000000000 ) ) ;
#9508=VERTEX_POINT ( 'NONE', #61038 ) ;
#9512=DIRECTION ( 'NONE',  ( 1.000000000000000000, 0.000000000000000000, 0.000000000000000000 ) ) ;
#9529=DIRECTION ( 'NONE',  ( -1.000000000000000000, 0.000000000000000000, 0.000000000000000000 ) ) ;
#9544=VERTEX_POINT ( 'NONE', #53524 ) ;
#9545=ORIENTED_EDGE ( 'NONE', *, *, #24016, .F. ) ;
#9551=VECTOR ( 'NONE', #63438, 1000.000000000000000 ) ;
#9556=VERTEX_POINT ( 'NONE', #69788 ) ;
#9559=EDGE_LOOP ( 'NONE', ( #11605, #19806, #2655, #30807 ) ) ;
#9565=AXIS2_PLACEMENT_3D ( 'NONE', #30459, #62275, #62989 ) ;
#9567=VECTOR ( 'NONE', #38527, 1000.000000000000000 ) ;
#9568=LINE ( 'NONE', #37143, #11988 ) ;
#9573=EDGE_LOOP ( 'NONE', ( #52611, #39795, #27333, #38460 ) ) ;
#9580=CARTESIAN_POINT ( 'NONE',  ( 7.250000000000004441, 7.450000000000001954, -16.50000000000000000 ) ) ;
#9600=EDGE_CURVE ( 'NONE', #25515, #28299, #11413, .T. ) ;
#9601=DIRECTION ( 'NONE',  ( -1.000000000000000000, 0.000000000000000000, 0.000000000000000000 ) ) ;
#9602=EDGE_CURVE ( 'NONE', #41191, #58562, #48556, .T. ) ;
#9645=AXIS2_PLACEMENT_3D ( 'NONE', #14828, #51609, #30032 ) ;
#9650=EDGE_CURVE ( 'NONE', #29479, #48363, #16377, .T. ) ;
#9660=EDGE_CURVE ( 'NONE', #58661, #53780, #15336, .T. ) ;
#9668=ORIENTED_EDGE ( 'NONE', *, *, #39635, .T. ) ;
#9674=FACE_OUTER_BOUND ( 'NONE', #169, .T. ) ;
#9682=CARTESIAN_POINT ( 'NONE',  ( -7.250000000000001776, -7.249999999999998224, -13.50000000000000178 ) ) ;
#9685=LINE ( 'NONE', #52468, #37982 ) ;
#9697=DIRECTION ( 'NONE',  ( 0.000000000000000000, 0.000000000000000000, -1.000000000000000000 ) ) ;
#9698=AXIS2_PLACEMENT_3D ( 'NONE', #37025, #9798, #58923 ) ;
#9702=ADVANCED_FACE ( 'NONE', ( #831 ), #28705, .F. ) ;
#9703=CARTESIAN_POINT ( 'NONE',  ( -7.250000000000000888, 7.450000000000003730, -21.50000000000000000 ) ) ;
#9704=FACE_OUTER_BOUND ( 'NONE', #12138, .T. ) ;
#9706=AXIS2_PLACEMENT_3D ( 'NONE', #62483, #3462, #62139 ) ;
#9708=CARTESIAN_POINT ( 'NONE',  ( 7.250000000000005329, 7.250000000000000888, -18.50000000000000000 ) ) ;
#9710=VECTOR ( 'NONE', #21193, 1000.000000000000000 ) ;
#9712=DIRECTION ( 'NONE',  ( -1.000000000000000000, 0.000000000000000000, 0.000000000000000000 ) ) ;
#9719=DIRECTION ( 'NONE',  ( 0.000000000000000000, 0.000000000000000000, 1.000000000000000000 ) ) ;
#9722=DIRECTION ( 'NONE',  ( -1.000000000000000000, 0.000000000000000000, -0.000000000000000000 ) ) ;
#9729=CARTESIAN_POINT ( 'NONE',  ( 7.450000000000006395, 7.250000000000000888, -10.50000000000000000 ) ) ;
#9746=DIRECTION ( 'NONE',  ( -0.000000000000000000, 0.000000000000000000, 1.000000000000000000 ) ) ;
#9754=AXIS2_PLACEMENT_3D ( 'NONE', #13846, #60879, #66543 ) ;
#9758=ORIENTED_EDGE ( 'NONE', *, *, #66000, .F. ) ;
#9761=VECTOR ( 'NONE', #40447, 1000.000000000000000 ) ;
#9762=DIRECTION ( 'NONE',  ( 1.000000000000000000, 0.000000000000000000, 0.000000000000000000 ) ) ;
#9767=VECTOR ( 'NONE', #51882, 1000.000000000000000 ) ;
#9768=CARTESIAN_POINT ( 'NONE',  ( -7.450000000000001954, -7.249999999999998224, -17.50000000000000000 ) ) ;
#9772=DIRECTION ( 'NONE',  ( 0.000000000000000000, 0.000000000000000000, 1.000000000000000000 ) ) ;
#9775=EDGE_CURVE ( 'NONE', #20378, #15085, #22028, .T. ) ;
#9782=DIRECTION ( 'NONE',  ( 0.000000000000000000, -0.000000000000000000, 1.000000000000000000 ) ) ;
#9786=VECTOR ( 'NONE', #6518, 1000.000000000000000 ) ;
#9792=EDGE_CURVE ( 'NONE', #22032, #41339, #66009, .T. ) ;
#9798=DIRECTION ( 'NONE',  ( 0.000000000000000000, 0.000000000000000000, -1.000000000000000000 ) ) ;
#9802=CARTESIAN_POINT ( 'NONE',  ( 7.750000000000001776, 7.750000000000000000, 0.000000000000000000 ) ) ;
#9804=AXIS2_PLACEMENT_3D ( 'NONE', #56285, #23759, #7830 ) ;
#9806=AXIS2_PLACEMENT_3D ( 'NONE', #24252, #29901, #34846 ) ;
#9809=DIRECTION ( 'NONE',  ( 0.000000000000000000, -0.000000000000000000, 1.000000000000000000 ) ) ;
#9810=CARTESIAN_POINT ( 'NONE',  ( 0.000000000000000000, -7.449999999999998401, -12.50000000000000000 ) ) ;
#9813=DIRECTION ( 'NONE',  ( -0.000000000000000000, -0.000000000000000000, 1.000000000000000000 ) ) ;
#9814=FACE_OUTER_BOUND ( 'NONE', #2851, .T. ) ;
#9824=VERTEX_POINT ( 'NONE', #45306 ) ;
#9836=CARTESIAN_POINT ( 'NONE',  ( -8.250000000000001776, -8.249999999999998224, -26.00000000000001066 ) ) ;
#9839=VERTEX_POINT ( 'NONE', #29058 ) ;
#9840=EDGE_LOOP ( 'NONE', ( #623, #64209, #59837, #68782 ) ) ;
#9851=LINE ( 'NONE', #21153, #43566 ) ;
#9853=ORIENTED_EDGE ( 'NONE', *, *, #21924, .T. ) ;
#9858=CARTESIAN_POINT ( 'NONE',  ( 0.000000000000000000, -7.449999999999998401, -10.50000000000000000 ) ) ;
#9869=ADVANCED_FACE ( 'NONE', ( #41059 ), #35048, .F. ) ;
#9877=DIRECTION ( 'NONE',  ( 1.000000000000000000, 0.000000000000000000, 0.000000000000000000 ) ) ;
#9879=ADVANCED_FACE ( 'NONE', ( #41412, #62623 ), #52381, .F. ) ;
#9880=EDGE_LOOP ( 'NONE', ( #44268, #35848, #181, #50187, #48867, #47394, #15245, #27653 ) ) ;
#9882=FACE_OUTER_BOUND ( 'NONE', #60358, .T. ) ;
#9886=FACE_BOUND ( 'NONE', #43062, .T. ) ;
#9889=CYLINDRICAL_SURFACE ( 'NONE', #21715, 0.2000000000000005107 ) ;
#9890=DIRECTION ( 'NONE',  ( -0.000000000000000000, -0.000000000000000000, 1.000000000000000000 ) ) ;
#9897=AXIS2_PLACEMENT_3D ( 'NONE', #45926, #56530, #55834 ) ;
#9903=DIRECTION ( 'NONE',  ( 0.000000000000000000, 1.000000000000000000, 0.000000000000000000 ) ) ;
#9908=ORIENTED_EDGE ( 'NONE', *, *, #68668, .T. ) ;
#9909=ORIENTED_EDGE ( 'NONE', *, *, #14601, .F. ) ;
#9915=ORIENTED_EDGE ( 'NONE', *, *, #26053, .F. ) ;
#9917=CYLINDRICAL_SURFACE ( 'NONE', #67985, 1.000000000000000000 ) ;
#9922=DIRECTION ( 'NONE',  ( 0.000000000000000000, 1.000000000000000000, 0.000000000000000000 ) ) ;
#9925=EDGE_CURVE ( 'NONE', #23182, #54436, #2775, .T. ) ;
#9936=CARTESIAN_POINT ( 'NONE',  ( -7.450000000000001954, 0.000000000000000000, -22.00000000000000000 ) ) ;
#9937=EDGE_LOOP ( 'NONE', ( #21589, #10608, #66683, #26598, #47506, #14145, #58563, #66167 ) ) ;
#9938=EDGE_CURVE ( 'NONE', #17140, #64203, #29400, .T. ) ;
#9944=EDGE_CURVE ( 'NONE', #57776, #12173, #67942, .T. ) ;
#9947=DIRECTION ( 'NONE',  ( -0.000000000000000000, -0.000000000000000000, 1.000000000000000000 ) ) ;
#9948=CARTESIAN_POINT ( 'NONE',  ( -7.450000000000001954, 0.000000000000000000, -19.50000000000000000 ) ) ;
#9950=EDGE_CURVE ( 'NONE', #40124, #59933, #42935, .T. ) ;
#9956=CARTESIAN_POINT ( 'NONE',  ( -2.500000000000000000, 0.000000000000000000, -29.90000000000000924 ) ) ;
#9957=EDGE_LOOP ( 'NONE', ( #61449, #8476, #42620, #27165 ) ) ;
#9978=DIRECTION ( 'NONE',  ( -0.000000000000000000, -0.000000000000000000, -1.000000000000000000 ) ) ;
#9984=DIRECTION ( 'NONE',  ( 0.000000000000000000, -0.000000000000000000, 1.000000000000000000 ) ) ;
#9993=ORIENTED_EDGE ( 'NONE', *, *, #40140, .F. ) ;
#9996=VERTEX_POINT ( 'NONE', #20898 ) ;
#9997=EDGE_LOOP ( 'NONE', ( #67891, #33109, #61245, #29905 ) ) ;
#10005=CARTESIAN_POINT ( 'NONE',  ( 8.689999999999999503, 9.750000000000001776, -7.000000000000000000 ) ) ;
#10008=EDGE_CURVE ( 'NONE', #55374, #16718, #31526, .T. ) ;
#10016=AXIS2_PLACEMENT_3D ( 'NONE', #7506, #12797, #1182 ) ;
#10029=EDGE_LOOP ( 'NONE', ( #56562, #5338, #68921, #66696 ) ) ;
#10043=ORIENTED_EDGE ( 'NONE', *, *, #19700, .F. ) ;
#10045=VECTOR ( 'NONE', #1528, 1000.000000000000000 ) ;
#10048=DIRECTION ( 'NONE',  ( -0.000000000000000000, -0.000000000000000000, 1.000000000000000000 ) ) ;
#10049=CARTESIAN_POINT ( 'NONE',  ( -8.250000000000001776, -8.249999999999998224, -26.00000000000001066 ) ) ;
#10054=CARTESIAN_POINT ( 'NONE',  ( 8.250000000000005329, 7.250000000000000888, -13.00000000000000178 ) ) ;
#10058=DIRECTION ( 'NONE',  ( -1.000000000000000000, 2.602085213965213008E-15, 0.000000000000000000 ) ) ;
#10066=CYLINDRICAL_SURFACE ( 'NONE', #62931, 1.000000000000000000 ) ;
#10069=VERTEX_POINT ( 'NONE', #26557 ) ;
#10087=ADVANCED_FACE ( 'NONE', ( #58029 ), #53437, .T. ) ;
#10088=AXIS2_PLACEMENT_3D ( 'NONE', #40057, #66599, #60939 ) ;
#10094=FACE_OUTER_BOUND ( 'NONE', #48016, .T. ) ;
#10102=ORIENTED_EDGE ( 'NONE', *, *, #22660, .F. ) ;
#10124=FACE_OUTER_BOUND ( 'NONE', #65370, .T. ) ;
#10129=EDGE_CURVE ( 'NONE', #11705, #66129, #22301, .T. ) ;
#10139=DIRECTION ( 'NONE',  ( -1.000000000000000000, 0.000000000000000000, 0.000000000000000000 ) ) ;
#10144=LINE ( 'NONE', #9810, #68939 ) ;
#10149=EDGE_LOOP ( 'NONE', ( #59284, #49268, #31663, #19293 ) ) ;
#10158=ORIENTED_EDGE ( 'NONE', *, *, #52280, .T. ) ;
#10162=CYLINDRICAL_SURFACE ( 'NONE', #19310, 1.000000000000000000 ) ;
#10172=ORIENTED_EDGE ( 'NONE', *, *, #66369, .T. ) ;
#10174=LINE ( 'NONE', #48701, #59825 ) ;
#10177=ORIENTED_EDGE ( 'NONE', *, *, #12930, .F. ) ;
#10182=LINE ( 'NONE', #31763, #49157 ) ;
#10184=EDGE_CURVE ( 'NONE', #6447, #12885, #39237, .T. ) ;
#10195=VECTOR ( 'NONE', #23953, 1000.000000000000000 ) ;
#10198=DIRECTION ( 'NONE',  ( 0.000000000000000000, 0.000000000000000000, -1.000000000000000000 ) ) ;
#10219=DIRECTION ( 'NONE',  ( 1.000000000000000000, -5.981805089575196197E-17, 0.000000000000000000 ) ) ;
#10225=CARTESIAN_POINT ( 'NONE',  ( -7.250000000000000888, -8.249999999999998224, -26.00000000000001066 ) ) ;
#10227=LINE ( 'NONE', #26489, #9710 ) ;
#10228=ORIENTED_EDGE ( 'NONE', *, *, #9471, .T. ) ;
#10235=AXIS2_PLACEMENT_3D ( 'NONE', #16288, #25868, #15950 ) ;
#10249=FACE_OUTER_BOUND ( 'NONE', #9957, .T. ) ;
#10255=VECTOR ( 'NONE', #3364, 1000.000000000000000 ) ;
#10256=VERTEX_POINT ( 'NONE', #12342 ) ;
#10259=DIRECTION ( 'NONE',  ( 8.951101527228104953E-17, -1.000000000000000000, 0.000000000000000000 ) ) ;
#10264=CARTESIAN_POINT ( 'NONE',  ( 7.450000000000004619, -1.336933437520057563E-15, -22.00000000000000000 ) ) ;
#10266=CARTESIAN_POINT ( 'NONE',  ( -7.250000000000001776, -7.249999999999998224, -23.50000000000000000 ) ) ;
#10268=ORIENTED_EDGE ( 'NONE', *, *, #16454, .T. ) ;
#10277=VERTEX_POINT ( 'NONE', #2107 ) ;
#10283=DIRECTION ( 'NONE',  ( -1.000000000000000000, 0.000000000000000000, 0.000000000000000000 ) ) ;
#10294=ORIENTED_EDGE ( 'NONE', *, *, #11574, .F. ) ;
#10295=AXIS2_PLACEMENT_3D ( 'NONE', #36396, #45593, #40299 ) ;
#10301=AXIS2_PLACEMENT_3D ( 'NONE', #68078, #45447, #40850 ) ;
#10304=LINE ( 'NONE', #58407, #14596 ) ;
#10307=VECTOR ( 'NONE', #168, 1000.000000000000000 ) ;
#10326=EDGE_CURVE ( 'NONE', #57771, #6619, #30634, .T. ) ;
#10331=EDGE_CURVE ( 'NONE', #56057, #59106, #39915, .T. ) ;
#10334=CARTESIAN_POINT ( 'NONE',  ( 8.250000000000005329, 7.250000000000000888, -25.00000000000000000 ) ) ;
#10342=ORIENTED_EDGE ( 'NONE', *, *, #4814, .T. ) ;
#10347=EDGE_CURVE ( 'NONE', #3392, #67717, #36025, .T. ) ;
#10351=VERTEX_POINT ( 'NONE', #34962 ) ;
#10369=DIRECTION ( 'NONE',  ( -0.000000000000000000, -0.000000000000000000, 1.000000000000000000 ) ) ;
#10370=ORIENTED_EDGE ( 'NONE', *, *, #61991, .F. ) ;
#10378=CARTESIAN_POINT ( 'NONE',  ( -8.250000000000000000, 7.250000000000001776, -17.00000000000000000 ) ) ;
#10386=CYLINDRICAL_SURFACE ( 'NONE', #12397, 0.7500000000000006661 ) ;
#10387=CIRCLE ( 'NONE', #16043, 1.000000000000000000 ) ;
#10390=EDGE_CURVE ( 'NONE', #55788, #60123, #3508, .T. ) ;
#10391=VERTEX_POINT ( 'NONE', #18708 ) ;
#10392=CARTESIAN_POINT ( 'NONE',  ( 7.250000000000004441, 7.450000000000001954, -8.500000000000000000 ) ) ;
#10400=VECTOR ( 'NONE', #67372, 1000.000000000000000 ) ;
#10405=ORIENTED_EDGE ( 'NONE', *, *, #52968, .T. ) ;
#10412=FACE_OUTER_BOUND ( 'NONE', #21768, .T. ) ;
#10413=ORIENTED_EDGE ( 'NONE', *, *, #31999, .T. ) ;
#10417=ADVANCED_FACE ( 'NONE', ( #37093 ), #58994, .T. ) ;
#10419=DIRECTION ( 'NONE',  ( 0.000000000000000000, 0.000000000000000000, -1.000000000000000000 ) ) ;
#10424=CARTESIAN_POINT ( 'NONE',  ( -8.250000000000001776, 0.000000000000000000, -9.000000000000001776 ) ) ;
#10432=VECTOR ( 'NONE', #49766, 1000.000000000000000 ) ;
#10434=CARTESIAN_POINT ( 'NONE',  ( -8.250000000000001776, -7.249999999999998224, -15.00000000000000000 ) ) ;
#10436=CARTESIAN_POINT ( 'NONE',  ( 7.250000000000005329, -7.249999999999998224, -26.00000000000001066 ) ) ;
#10442=EDGE_LOOP ( 'NONE', ( #16356, #46252, #61479, #21055 ) ) ;
#10443=AXIS2_PLACEMENT_3D ( 'NONE', #2585, #67645, #45711 ) ;
#10450=VECTOR ( 'NONE', #48953, 1000.000000000000000 ) ;
#10452=DIRECTION ( 'NONE',  ( 1.000000000000000000, 0.000000000000000000, 0.000000000000000000 ) ) ;
#10453=ORIENTED_EDGE ( 'NONE', *, *, #26374, .T. ) ;
#10470=AXIS2_PLACEMENT_3D ( 'NONE', #62385, #1597, #39427 ) ;
#10472=DIRECTION ( 'NONE',  ( -1.000000000000000000, 0.000000000000000000, 0.000000000000000000 ) ) ;
#10479=PLANE ( 'NONE',  #15347 ) ;
#10497=DIRECTION ( 'NONE',  ( 0.000000000000000000, -0.000000000000000000, 1.000000000000000000 ) ) ;
#10501=AXIS2_PLACEMENT_3D ( 'NONE', #2045, #17949, #49459 ) ;
#10507=VERTEX_POINT ( 'NONE', #42032 ) ;
#10508=PLANE ( 'NONE',  #30629 ) ;
#10514=VECTOR ( 'NONE', #6697, 1000.000000000000000 ) ;
#10516=ORIENTED_EDGE ( 'NONE', *, *, #35897, .F. ) ;
#10531=ORIENTED_EDGE ( 'NONE', *, *, #9950, .T. ) ;
#10532=CARTESIAN_POINT ( 'NONE',  ( 7.250000000000005329, 8.250000000000001776, -26.00000000000001066 ) ) ;
#10540=LINE ( 'NONE', #36724, #30134 ) ;
#10545=CARTESIAN_POINT ( 'NONE',  ( 0.000000000000000000, -7.449999999999998401, -13.50000000000000178 ) ) ;
#10572=CARTESIAN_POINT ( 'NONE',  ( 8.250000000000005329, 7.250000000000000888, -26.00000000000001066 ) ) ;
#10574=CARTESIAN_POINT ( 'NONE',  ( -7.450000000000001954, -7.249999999999998224, -8.500000000000000000 ) ) ;
#10581=ORIENTED_EDGE ( 'NONE', *, *, #68969, .T. ) ;
#10583=ORIENTED_EDGE ( 'NONE', *, *, #37235, .T. ) ;
#10584=ORIENTED_EDGE ( 'NONE', *, *, #45741, .T. ) ;
#10591=DIRECTION ( 'NONE',  ( 0.000000000000000000, 1.000000000000000000, 0.000000000000000000 ) ) ;
#10592=ORIENTED_EDGE ( 'NONE', *, *, #9471, .F. ) ;
#10603=FACE_OUTER_BOUND ( 'NONE', #65006, .T. ) ;
#10605=VECTOR ( 'NONE', #3685, 1000.000000000000000 ) ;
#10608=ORIENTED_EDGE ( 'NONE', *, *, #52280, .F. ) ;
#10610=EDGE_CURVE ( 'NONE', #60691, #39415, #28336, .T. ) ;
#10617=CARTESIAN_POINT ( 'NONE',  ( -7.250000000000000888, 7.250000000000001776, -17.00000000000000000 ) ) ;
#10637=CYLINDRICAL_SURFACE ( 'NONE', #21510, 1.000000000000000000 ) ;
#10638=FACE_OUTER_BOUND ( 'NONE', #6776, .T. ) ;
#10645=ORIENTED_EDGE ( 'NONE', *, *, #8644, .F. ) ;
#10650=ADVANCED_FACE ( 'NONE', ( #38473 ), #6286, .T. ) ;
#10658=CARTESIAN_POINT ( 'NONE',  ( -7.250000000000000888, -8.249999999999998224, -9.500000000000001776 ) ) ;
#10660=DIRECTION ( 'NONE',  ( 0.000000000000000000, 0.000000000000000000, -1.000000000000000000 ) ) ;
#10667=VERTEX_POINT ( 'NONE', #33504 ) ;
#10677=ORIENTED_EDGE ( 'NONE', *, *, #49535, .T. ) ;
#10681=CARTESIAN_POINT ( 'NONE',  ( 7.250000000000005329, 8.250000000000001776, -25.00000000000000000 ) ) ;
#10682=CARTESIAN_POINT ( 'NONE',  ( 7.250000000000004441, 7.450000000000001954, -10.00000000000000000 ) ) ;
#10683=CARTESIAN_POINT ( 'NONE',  ( -10.50000000000000178, 9.690000000000001279, -5.000000000000000000 ) ) ;
#10686=CARTESIAN_POINT ( 'NONE',  ( -6.500000000000002665, 6.500000000000002665, -1.000000000000000000 ) ) ;
#10688=EDGE_LOOP ( 'NONE', ( #25559, #36257, #56461, #31130, #5368, #17904, #27748, #56006 ) ) ;
#10694=LINE ( 'NONE', #54194, #7348 ) ;
#10697=CIRCLE ( 'NONE', #28708, 1.000000000000000000 ) ;
#10712=ADVANCED_FACE ( 'NONE', ( #50103 ), #22553, .F. ) ;
#10719=VERTEX_POINT ( 'NONE', #45845 ) ;
#10723=CARTESIAN_POINT ( 'NONE',  ( -8.250000000000001776, -7.249999999999998224, -26.00000000000001066 ) ) ;
#10734=DIRECTION ( 'NONE',  ( 0.000000000000000000, 0.000000000000000000, 1.000000000000000000 ) ) ;
#10749=DIRECTION ( 'NONE',  ( 0.000000000000000000, -0.000000000000000000, 1.000000000000000000 ) ) ;
#10753=ADVANCED_FACE ( 'NONE', ( #39829 ), #29929, .F. ) ;
#10767=LINE ( 'NONE', #59904, #13816 ) ;
#10769=VERTEX_POINT ( 'NONE', #19663 ) ;
#10774=DIRECTION ( 'NONE',  ( -1.000000000000000000, 0.000000000000000000, 0.000000000000000000 ) ) ;
#10775=VERTEX_POINT ( 'NONE', #34174 ) ;
#10787=ADVANCED_FACE ( 'NONE', ( #13321 ), #12958, .T. ) ;
#10794=DIRECTION ( 'NONE',  ( -0.000000000000000000, -0.000000000000000000, 1.000000000000000000 ) ) ;
#10814=DIRECTION ( 'NONE',  ( 0.000000000000000000, -0.000000000000000000, 1.000000000000000000 ) ) ;
#10817=DIRECTION ( 'NONE',  ( -0.000000000000000000, -0.000000000000000000, -1.000000000000000000 ) ) ;
#10820=EDGE_CURVE ( 'NONE', #36321, #19554, #14381, .T. ) ;
#10822=LINE ( 'NONE', #36652, #39053 ) ;
#10826=AXIS2_PLACEMENT_3D ( 'NONE', #37005, #20375, #20720 ) ;
#10829=LINE ( 'NONE', #43346, #63530 ) ;
#10833=VECTOR ( 'NONE', #10497, 1000.000000000000000 ) ;
#10835=CARTESIAN_POINT ( 'NONE',  ( 8.250000000000005329, 7.250000000000000888, -10.50000000000000000 ) ) ;
#10839=ORIENTED_EDGE ( 'NONE', *, *, #11353, .F. ) ;
#10840=AXIS2_PLACEMENT_3D ( 'NONE', #28021, #11739, #45298 ) ;
#10842=VECTOR ( 'NONE', #66863, 1000.000000000000000 ) ;
#10847=CYLINDRICAL_SURFACE ( 'NONE', #21299, 0.1999999999999996503 ) ;
#10877=EDGE_CURVE ( 'NONE', #12501, #56941, #36291, .T. ) ;
#10878=EDGE_CURVE ( 'NONE', #62127, #15601, #27160, .T. ) ;
#10884=EDGE_LOOP ( 'NONE', ( #43916, #69405, #52532, #22424 ) ) ;
#10904=AXIS2_PLACEMENT_3D ( 'NONE', #28165, #53666, #32448 ) ;
#10916=ADVANCED_FACE ( 'NONE', ( #10124 ), #41947, .F. ) ;
#10917=AXIS2_PLACEMENT_3D ( 'NONE', #39999, #29064, #30461 ) ;
#10925=CARTESIAN_POINT ( 'NONE',  ( -9.690000000000001279, -9.750000000000001776, -7.000000000000000000 ) ) ;
#10927=LINE ( 'NONE', #10574, #68402 ) ;
#10929=CARTESIAN_POINT ( 'NONE',  ( 9.690000000000001279, 10.50000000000000000, 0.000000000000000000 ) ) ;
#10937=ORIENTED_EDGE ( 'NONE', *, *, #26223, .T. ) ;
#10939=AXIS2_PLACEMENT_3D ( 'NONE', #46185, #68108, #24279 ) ;
#10955=VERTEX_POINT ( 'NONE', #4822 ) ;
#10958=DIRECTION ( 'NONE',  ( 1.000000000000000000, 0.000000000000000000, 0.000000000000000000 ) ) ;
#10982=DIRECTION ( 'NONE',  ( 1.000000000000000000, 0.000000000000000000, 0.000000000000000000 ) ) ;
#10989=LINE ( 'NONE', #380, #52699 ) ;
#10998=DIRECTION ( 'NONE',  ( 1.000000000000000000, -0.000000000000000000, 0.000000000000000000 ) ) ;
#11004=CARTESIAN_POINT ( 'NONE',  ( 0.000000000000000000, 0.000000000000000000, -29.90000000000000924 ) ) ;
#11011=VECTOR ( 'NONE', #67561, 1000.000000000000000 ) ;
#11019=CARTESIAN_POINT ( 'NONE',  ( 7.250000000000005329, -8.249999999999998224, -26.00000000000001066 ) ) ;
#11024=ORIENTED_EDGE ( 'NONE', *, *, #6006, .F. ) ;
#11039=LINE ( 'NONE', #63748, #63965 ) ;
#11041=DIRECTION ( 'NONE',  ( 1.000000000000000000, 0.000000000000000000, 0.000000000000000000 ) ) ;
#11043=ORIENTED_EDGE ( 'NONE', *, *, #42356, .T. ) ;
#11044=EDGE_LOOP ( 'NONE', ( #33139, #29185, #43243, #17462 ) ) ;
#11049=AXIS2_PLACEMENT_3D ( 'NONE', #13524, #18467, #56660 ) ;
#11055=EDGE_LOOP ( 'NONE', ( #904, #31758, #23118, #67179, #64780, #68908, #49165, #37648 ) ) ;
#11068=ADVANCED_FACE ( 'NONE', ( #62689 ), #46773, .F. ) ;
#11076=VERTEX_POINT ( 'NONE', #63051 ) ;
#11080=CARTESIAN_POINT ( 'NONE',  ( -7.250000000000001776, -7.249999999999998224, -18.50000000000000000 ) ) ;
#11083=CARTESIAN_POINT ( 'NONE',  ( -7.250000000000000888, 8.250000000000001776, -12.50000000000000000 ) ) ;
#11088=DIRECTION ( 'NONE',  ( 1.000000000000000000, 0.000000000000000000, 0.000000000000000000 ) ) ;
#11093=DIRECTION ( 'NONE',  ( 0.000000000000000000, 0.000000000000000000, 1.000000000000000000 ) ) ;
#11095=AXIS2_PLACEMENT_3D ( 'NONE', #62227, #35339, #8477 ) ;
#11112=ORIENTED_EDGE ( 'NONE', *, *, #26146, .T. ) ;
#11114=CARTESIAN_POINT ( 'NONE',  ( 8.250000000000005329, 7.250000000000000888, -9.500000000000001776 ) ) ;
#11116=DIRECTION ( 'NONE',  ( 0.000000000000000000, 0.000000000000000000, 1.000000000000000000 ) ) ;
#11123=VERTEX_POINT ( 'NONE', #42527 ) ;
#11126=EDGE_CURVE ( 'NONE', #11267, #19554, #58463, .T. ) ;
#11138=EDGE_CURVE ( 'NONE', #17846, #23372, #31587, .T. ) ;
#11139=CARTESIAN_POINT ( 'NONE',  ( 8.250000000000005329, -7.249999999999998224, -21.00000000000000000 ) ) ;
#11143=CARTESIAN_POINT ( 'NONE',  ( -7.250000000000000888, 7.250000000000001776, -24.50000000000000000 ) ) ;
#11144=CARTESIAN_POINT ( 'NONE',  ( 0.000000000000000000, -7.449999999999998401, -11.00000000000000000 ) ) ;
#11153=FACE_OUTER_BOUND ( 'NONE', #1515, .T. ) ;
#11158=CYLINDRICAL_SURFACE ( 'NONE', #30816, 2.500000000000000000 ) ;
#11165=DIRECTION ( 'NONE',  ( 1.000000000000000000, -0.000000000000000000, 0.000000000000000000 ) ) ;
#11170=DIRECTION ( 'NONE',  ( 0.000000000000000000, -1.000000000000000000, -0.000000000000000000 ) ) ;
#11173=CARTESIAN_POINT ( 'NONE',  ( 8.250000000000005329, -7.249999999999998224, -19.00000000000000000 ) ) ;
#11174=EDGE_CURVE ( 'NONE', #51421, #11793, #36522, .T. ) ;
#11177=CIRCLE ( 'NONE', #50691, 0.1999999999999987899 ) ;
#11181=LINE ( 'NONE', #5890, #63346 ) ;
#11191=DIRECTION ( 'NONE',  ( -1.000000000000000000, 0.000000000000000000, -0.000000000000000000 ) ) ;
#11196=CARTESIAN_POINT ( 'NONE',  ( -7.450000000000001954, -7.249999999999998224, -9.500000000000001776 ) ) ;
#11197=ORIENTED_EDGE ( 'NONE', *, *, #44214, .F. ) ;
#11199=DIRECTION ( 'NONE',  ( -0.000000000000000000, -0.000000000000000000, 1.000000000000000000 ) ) ;
#11203=CIRCLE ( 'NONE', #50713, 1.000000000000002665 ) ;
#11210=CARTESIAN_POINT ( 'NONE',  ( 7.250000000000005329, -7.449999999999998401, -24.50000000000000000 ) ) ;
#11212=AXIS2_PLACEMENT_3D ( 'NONE', #3599, #9256, #25168 ) ;
#11221=EDGE_CURVE ( 'NONE', #56334, #53583, #65491, .T. ) ;
#11222=DIRECTION ( 'NONE',  ( 0.000000000000000000, 0.000000000000000000, 1.000000000000000000 ) ) ;
#11226=CYLINDRICAL_SURFACE ( 'NONE', #50453, 1.000000000000000000 ) ;
#11228=LINE ( 'NONE', #49426, #17792 ) ;
#11229=DIRECTION ( 'NONE',  ( -0.000000000000000000, -0.000000000000000000, -1.000000000000000000 ) ) ;
#11235=DIRECTION ( 'NONE',  ( 0.000000000000000000, 0.000000000000000000, -1.000000000000000000 ) ) ;
#11236=AXIS2_PLACEMENT_3D ( 'NONE', #2802, #51957, #35313 ) ;
#11245=VECTOR ( 'NONE', #26319, 1000.000000000000000 ) ;
#11247=DIRECTION ( 'NONE',  ( 1.000000000000000000, -5.981805089575194965E-17, 0.000000000000000000 ) ) ;
#11260=DIRECTION ( 'NONE',  ( 1.000000000000000000, 0.000000000000000000, 0.000000000000000000 ) ) ;
#11264=DIRECTION ( 'NONE',  ( -1.794541526872559352E-16, -1.000000000000000000, 0.000000000000000000 ) ) ;
#11265=DIRECTION ( 'NONE',  ( -0.000000000000000000, -0.000000000000000000, 1.000000000000000000 ) ) ;
#11267=VERTEX_POINT ( 'NONE', #54893 ) ;
#11274=EDGE_CURVE ( 'NONE', #30319, #27517, #65154, .T. ) ;
#11284=DIRECTION ( 'NONE',  ( 1.000000000000000000, 0.000000000000000000, -0.000000000000000000 ) ) ;
#11290=CARTESIAN_POINT ( 'NONE',  ( 8.250000000000005329, 0.000000000000000000, -19.00000000000000000 ) ) ;
#11295=VERTEX_POINT ( 'NONE', #6096 ) ;
#11296=ORIENTED_EDGE ( 'NONE', *, *, #45756, .F. ) ;
#11298=CARTESIAN_POINT ( 'NONE',  ( -7.250000000000000888, 7.250000000000001776, -13.00000000000000178 ) ) ;
#11306=ORIENTED_EDGE ( 'NONE', *, *, #20699, .T. ) ;
#11309=FACE_BOUND ( 'NONE', #39487, .T. ) ;
#11310=CARTESIAN_POINT ( 'NONE',  ( 7.450000000000004619, -1.336933437520057563E-15, -12.50000000000000000 ) ) ;
#11311=ORIENTED_EDGE ( 'NONE', *, *, #19173, .T. ) ;
#11314=LINE ( 'NONE', #42458, #20372 ) ;
#11327=CARTESIAN_POINT ( 'NONE',  ( 6.500000000000000888, -6.500000000000002665, -1.000000000000000000 ) ) ;
#11328=VECTOR ( 'NONE', #56279, 1000.000000000000000 ) ;
#11335=EDGE_CURVE ( 'NONE', #33105, #57275, #55225, .T. ) ;
#11343=ORIENTED_EDGE ( 'NONE', *, *, #59645, .F. ) ;
#11351=DIRECTION ( 'NONE',  ( -1.000000000000000000, 0.000000000000000000, -0.000000000000000000 ) ) ;
#11353=EDGE_CURVE ( 'NONE', #25227, #17131, #66791, .T. ) ;
#11359=CYLINDRICAL_SURFACE ( 'NONE', #22618, 1.000000000000000000 ) ;
#11360=ORIENTED_EDGE ( 'NONE', *, *, #26846, .T. ) ;
#11366=DIRECTION ( 'NONE',  ( 0.000000000000000000, -0.000000000000000000, 1.000000000000000000 ) ) ;
#11368=ORIENTED_EDGE ( 'NONE', *, *, #59715, .F. ) ;
#11376=CARTESIAN_POINT ( 'NONE',  ( 0.000000000000000000, -8.249999999999998224, -22.50000000000000000 ) ) ;
#11380=VERTEX_POINT ( 'NONE', #35301 ) ;
#11384=ORIENTED_EDGE ( 'NONE', *, *, #5237, .T. ) ;
#11385=CYLINDRICAL_SURFACE ( 'NONE', #46882, 0.2000000000000005107 ) ;
#11392=VERTEX_POINT ( 'NONE', #41322 ) ;
#11397=CARTESIAN_POINT ( 'NONE',  ( 7.250000000000005329, -8.249999999999998224, -15.00000000000000000 ) ) ;
#11398=CARTESIAN_POINT ( 'NONE',  ( 7.250000000000005329, -7.449999999999998401, -11.50000000000000000 ) ) ;
#11400=ORIENTED_EDGE ( 'NONE', *, *, #33138, .T. ) ;
#11409=LINE ( 'NONE', #43929, #149 ) ;
#11410=ORIENTED_EDGE ( 'NONE', *, *, #36765, .F. ) ;
#11413=LINE ( 'NONE', #20628, #13421 ) ;
#11414=DIRECTION ( 'NONE',  ( 0.000000000000000000, -1.000000000000000000, 0.000000000000000000 ) ) ;
#11424=FACE_OUTER_BOUND ( 'NONE', #61614, .T. ) ;
#11441=CARTESIAN_POINT ( 'NONE',  ( 7.250000000000005329, -7.249999999999998224, -15.00000000000000000 ) ) ;
#11444=VECTOR ( 'NONE', #6245, 1000.000000000000000 ) ;
#11445=DIRECTION ( 'NONE',  ( 1.000000000000000000, -0.000000000000000000, 0.000000000000000000 ) ) ;
#11446=DIRECTION ( 'NONE',  ( 0.000000000000000000, 0.000000000000000000, 1.000000000000000000 ) ) ;
#11449=ORIENTED_EDGE ( 'NONE', *, *, #56407, .F. ) ;
#11455=VERTEX_POINT ( 'NONE', #34959 ) ;
#11470=ORIENTED_EDGE ( 'NONE', *, *, #6871, .F. ) ;
#11475=CARTESIAN_POINT ( 'NONE',  ( -7.450000000000001954, 7.250000000000000000, -16.50000000000000000 ) ) ;
#11478=EDGE_LOOP ( 'NONE', ( #38495, #25875, #59092, #48845 ) ) ;
#11480=VECTOR ( 'NONE', #22633, 1000.000000000000000 ) ;
#11483=ORIENTED_EDGE ( 'NONE', *, *, #49921, .T. ) ;
#11490=DIRECTION ( 'NONE',  ( 0.000000000000000000, 0.000000000000000000, -1.000000000000000000 ) ) ;
#11505=ORIENTED_EDGE ( 'NONE', *, *, #5442, .T. ) ;
#11507=EDGE_CURVE ( 'NONE', #64155, #32920, #14102, .T. ) ;
#11525=FACE_OUTER_BOUND ( 'NONE', #13133, .T. ) ;
#11526=ORIENTED_EDGE ( 'NONE', *, *, #48604, .T. ) ;
#11545=CARTESIAN_POINT ( 'NONE',  ( 7.250000000000005329, -8.249999999999998224, -26.00000000000001066 ) ) ;
#11548=EDGE_CURVE ( 'NONE', #31253, #25515, #20744, .T. ) ;
#11550=ORIENTED_EDGE ( 'NONE', *, *, #34542, .F. ) ;
#11554=CARTESIAN_POINT ( 'NONE',  ( -7.250000000000000888, 8.250000000000001776, -26.00000000000001066 ) ) ;
#11569=EDGE_CURVE ( 'NONE', #15576, #42345, #15526, .T. ) ;
#11574=EDGE_CURVE ( 'NONE', #2392, #28744, #58047, .T. ) ;
#11575=EDGE_CURVE ( 'NONE', #54414, #66278, #51219, .T. ) ;
#11578=ORIENTED_EDGE ( 'NONE', *, *, #66667, .F. ) ;
#11584=AXIS2_PLACEMENT_3D ( 'NONE', #7876, #66930, #33716 ) ;
#11588=EDGE_CURVE ( 'NONE', #22431, #60745, #52658, .T. ) ;
#11604=LINE ( 'NONE', #17612, #42045 ) ;
#11605=ORIENTED_EDGE ( 'NONE', *, *, #23696, .T. ) ;
#11609=CARTESIAN_POINT ( 'NONE',  ( 7.450000000000003730, -7.249999999999997335, -9.500000000000001776 ) ) ;
#11610=AXIS2_PLACEMENT_3D ( 'NONE', #40028, #49955, #34739 ) ;
#11618=EDGE_LOOP ( 'NONE', ( #38273, #59734, #49805, #16270 ) ) ;
#11628=VERTEX_POINT ( 'NONE', #2627 ) ;
#11639=EDGE_CURVE ( 'NONE', #57216, #58124, #56373, .T. ) ;
#11641=CARTESIAN_POINT ( 'NONE',  ( -8.250000000000001776, 7.250000000000000888, -26.00000000000001066 ) ) ;
#11659=ADVANCED_FACE ( 'NONE', ( #18898 ), #2283, .F. ) ;
#11660=DIRECTION ( 'NONE',  ( 0.000000000000000000, 0.000000000000000000, 1.000000000000000000 ) ) ;
#11661=DIRECTION ( 'NONE',  ( -0.000000000000000000, -0.000000000000000000, 1.000000000000000000 ) ) ;
#11664=CARTESIAN_POINT ( 'NONE',  ( -8.250000000000001776, 7.250000000000000888, -26.00000000000001066 ) ) ;
#11667=FACE_OUTER_BOUND ( 'NONE', #50041, .T. ) ;
#11671=DIRECTION ( 'NONE',  ( -1.000000000000000000, 1.794541526872559352E-16, 0.000000000000000000 ) ) ;
#11683=CARTESIAN_POINT ( 'NONE',  ( -7.450000000000001954, -7.249999999999998224, -20.50000000000000000 ) ) ;
#11695=VECTOR ( 'NONE', #43100, 1000.000000000000000 ) ;
#11700=DIRECTION ( 'NONE',  ( -0.000000000000000000, -0.000000000000000000, 1.000000000000000000 ) ) ;
#11702=AXIS2_PLACEMENT_3D ( 'NONE', #28688, #60864, #56611 ) ;
#11705=VERTEX_POINT ( 'NONE', #50017 ) ;
#11711=CARTESIAN_POINT ( 'NONE',  ( 7.749999999999998224, -7.348062532928000934, 5.000000000000000000 ) ) ;
#11717=EDGE_LOOP ( 'NONE', ( #27457, #49338, #6626, #12140 ) ) ;
#11719=EDGE_LOOP ( 'NONE', ( #14228, #61281, #21722, #54494 ) ) ;
#11722=EDGE_CURVE ( 'NONE', #31382, #25281, #39408, .T. ) ;
#11724=LINE ( 'NONE', #49571, #54558 ) ;
#11726=ORIENTED_EDGE ( 'NONE', *, *, #9792, .F. ) ;
#11730=EDGE_CURVE ( 'NONE', #52010, #66616, #14997, .T. ) ;
#11732=VECTOR ( 'NONE', #60738, 1000.000000000000000 ) ;
#11735=VERTEX_POINT ( 'NONE', #46116 ) ;
#11739=DIRECTION ( 'NONE',  ( 1.000000000000000000, -0.000000000000000000, 0.000000000000000000 ) ) ;
#11746=ORIENTED_EDGE ( 'NONE', *, *, #43729, .F. ) ;
#11754=AXIS2_PLACEMENT_3D ( 'NONE', #24061, #33637, #2149 ) ;
#11775=EDGE_CURVE ( 'NONE', #49332, #31165, #41860, .T. ) ;
#11776=VERTEX_POINT ( 'NONE', #3336 ) ;
#11777=CARTESIAN_POINT ( 'NONE',  ( 8.750000000000000000, -7.348062532928000934, 0.000000000000000000 ) ) ;
#11791=LINE ( 'NONE', #64185, #17639 ) ;
#11793=VERTEX_POINT ( 'NONE', #19946 ) ;
#11798=VERTEX_POINT ( 'NONE', #57424 ) ;
#11806=AXIS2_PLACEMENT_3D ( 'NONE', #7130, #49256, #32983 ) ;
#11807=EDGE_LOOP ( 'NONE', ( #48408, #56240, #6951, #54060 ) ) ;
#11811=DIRECTION ( 'NONE',  ( -5.981805089575196197E-17, -1.000000000000000000, 0.000000000000000000 ) ) ;
#11812=EDGE_CURVE ( 'NONE', #25369, #61156, #39996, .T. ) ;
#11827=VERTEX_POINT ( 'NONE', #30909 ) ;
#11832=ORIENTED_EDGE ( 'NONE', *, *, #41158, .F. ) ;
#11836=CARTESIAN_POINT ( 'NONE',  ( 7.250000000000005329, 7.250000000000000888, -14.50000000000000000 ) ) ;
#11845=DIRECTION ( 'NONE',  ( 0.000000000000000000, 0.000000000000000000, -1.000000000000000000 ) ) ;
#11851=AXIS2_PLACEMENT_3D ( 'NONE', #43932, #66539, #12099 ) ;
#11853=LINE ( 'NONE', #59959, #9344 ) ;
#11860=ORIENTED_EDGE ( 'NONE', *, *, #37158, .T. ) ;
#11863=DIRECTION ( 'NONE',  ( 1.000000000000000000, -0.000000000000000000, 0.000000000000000000 ) ) ;
#11868=DIRECTION ( 'NONE',  ( -1.794541526872559352E-16, -1.000000000000000000, 0.000000000000000000 ) ) ;
#11875=DIRECTION ( 'NONE',  ( -1.000000000000000000, 0.000000000000000000, 0.000000000000000000 ) ) ;
#11884=VECTOR ( 'NONE', #17592, 1000.000000000000000 ) ;
#11891=ORIENTED_EDGE ( 'NONE', *, *, #22371, .T. ) ;
#11893=ORIENTED_EDGE ( 'NONE', *, *, #14237, .T. ) ;
#11898=EDGE_CURVE ( 'NONE', #19769, #5145, #37618, .T. ) ;
#11899=LINE ( 'NONE', #43755, #49234 ) ;
#11901=EDGE_CURVE ( 'NONE', #47075, #35171, #12893, .T. ) ;
#11902=EDGE_LOOP ( 'NONE', ( #43252, #26275, #6539, #29501 ) ) ;
#11912=FACE_OUTER_BOUND ( 'NONE', #48879, .T. ) ;
#11913=AXIS2_PLACEMENT_3D ( 'NONE', #16473, #65599, #32722 ) ;
#11925=PLANE ( 'NONE',  #65166 ) ;
#11927=LINE ( 'NONE', #61773, #46946 ) ;
#11930=AXIS2_PLACEMENT_3D ( 'NONE', #45291, #61552, #13121 ) ;
#11936=ORIENTED_EDGE ( 'NONE', *, *, #64151, .F. ) ;
#11939=VERTEX_POINT ( 'NONE', #48572 ) ;
#11943=DIRECTION ( 'NONE',  ( -0.000000000000000000, 0.000000000000000000, -1.000000000000000000 ) ) ;
#11945=DIRECTION ( 'NONE',  ( -0.000000000000000000, -0.000000000000000000, 1.000000000000000000 ) ) ;
#11951=LINE ( 'NONE', #64678, #6555 ) ;
#11958=DIRECTION ( 'NONE',  ( 0.000000000000000000, 0.000000000000000000, 1.000000000000000000 ) ) ;
#11959=ORIENTED_EDGE ( 'NONE', *, *, #65744, .F. ) ;
#11962=DIRECTION ( 'NONE',  ( 0.000000000000000000, 0.000000000000000000, -1.000000000000000000 ) ) ;
#11970=CARTESIAN_POINT ( 'NONE',  ( 7.250000000000005329, 7.250000000000000888, -11.00000000000000000 ) ) ;
#11974=ORIENTED_EDGE ( 'NONE', *, *, #17667, .T. ) ;
#11988=VECTOR ( 'NONE', #52716, 1000.000000000000000 ) ;
#11995=EDGE_CURVE ( 'NONE', #35620, #53694, #59868, .T. ) ;
#12009=CARTESIAN_POINT ( 'NONE',  ( 0.000000000000000000, 8.250000000000001776, -10.50000000000000000 ) ) ;
#12021=ORIENTED_EDGE ( 'NONE', *, *, #58524, .T. ) ;
#12025=EDGE_CURVE ( 'NONE', #26490, #32586, #845, .T. ) ;
#12031=DIRECTION ( 'NONE',  ( -1.000000000000000000, 0.000000000000000000, 0.000000000000000000 ) ) ;
#12038=DIRECTION ( 'NONE',  ( -1.000000000000000000, 0.000000000000000000, 0.000000000000000000 ) ) ;
#12069=ADVANCED_FACE ( 'NONE', ( #34354 ), #28719, .T. ) ;
#12070=ORIENTED_EDGE ( 'NONE', *, *, #40004, .T. ) ;
#12081=FACE_OUTER_BOUND ( 'NONE', #69531, .T. ) ;
#12082=CARTESIAN_POINT ( 'NONE',  ( 7.250000000000005329, -7.449999999999998401, -23.00000000000000000 ) ) ;
#12086=AXIS2_PLACEMENT_3D ( 'NONE', #2099, #51230, #24364 ) ;
#12088=EDGE_CURVE ( 'NONE', #21685, #55203, #62570, .T. ) ;
#12095=CARTESIAN_POINT ( 'NONE',  ( -7.750000000000001776, 7.750000000000001776, -5.000000000000000000 ) ) ;
#12099=DIRECTION ( 'NONE',  ( -1.000000000000000000, 0.000000000000000000, 0.000000000000000000 ) ) ;
#12104=DIRECTION ( 'NONE',  ( -1.000000000000000000, 0.000000000000000000, 0.000000000000000000 ) ) ;
#12107=ORIENTED_EDGE ( 'NONE', *, *, #14629, .T. ) ;
#12121=EDGE_CURVE ( 'NONE', #30178, #47920, #34719, .T. ) ;
#12129=ORIENTED_EDGE ( 'NONE', *, *, #46488, .F. ) ;
#12133=CIRCLE ( 'NONE', #33593, 0.2000000000000005107 ) ;
#12134=CIRCLE ( 'NONE', #49412, 0.2000000000000005107 ) ;
#12138=EDGE_LOOP ( 'NONE', ( #41684, #19277, #25306, #58295 ) ) ;
#12140=ORIENTED_EDGE ( 'NONE', *, *, #2371, .F. ) ;
#12146=CARTESIAN_POINT ( 'NONE',  ( 7.250000000000005329, 7.250000000000000888, -25.50000000000000355 ) ) ;
#12149=CIRCLE ( 'NONE', #51688, 1.000000000000000000 ) ;
#12153=ORIENTED_EDGE ( 'NONE', *, *, #30029, .F. ) ;
#12156=CARTESIAN_POINT ( 'NONE',  ( -7.250000000000000000, -7.449999999999998401, -8.000000000000000000 ) ) ;
#12160=AXIS2_PLACEMENT_3D ( 'NONE', #12960, #66716, #40540 ) ;
#12163=ORIENTED_EDGE ( 'NONE', *, *, #34557, .T. ) ;
#12165=DIRECTION ( 'NONE',  ( 1.000000000000000000, -5.981805089575194965E-17, 0.000000000000000000 ) ) ;
#12166=EDGE_LOOP ( 'NONE', ( #43579, #14870, #51108, #45714 ) ) ;
#12173=VERTEX_POINT ( 'NONE', #57691 ) ;
#12188=LINE ( 'NONE', #33758, #57109 ) ;
#12202=DIRECTION ( 'NONE',  ( -1.000000000000000000, 0.000000000000000000, 0.000000000000000000 ) ) ;
#12205=PLANE ( 'NONE',  #48208 ) ;
#12222=CARTESIAN_POINT ( 'NONE',  ( -7.250000000000000888, 8.250000000000001776, -26.00000000000001066 ) ) ;
#12228=CARTESIAN_POINT ( 'NONE',  ( 8.250000000000005329, 0.000000000000000000, -23.00000000000000000 ) ) ;
#12237=ORIENTED_EDGE ( 'NONE', *, *, #24619, .F. ) ;
#12244=CIRCLE ( 'NONE', #31472, 0.1999999999999996503 ) ;
#12245=CARTESIAN_POINT ( 'NONE',  ( 7.250000000000005329, 8.250000000000001776, -23.50000000000000000 ) ) ;
#12257=CARTESIAN_POINT ( 'NONE',  ( -7.250000000000000888, 8.250000000000001776, -20.00000000000000000 ) ) ;
#12262=DIRECTION ( 'NONE',  ( -1.000000000000000000, 0.000000000000000000, 0.000000000000000000 ) ) ;
#12264=CIRCLE ( 'NONE', #69886, 0.1999999999999987899 ) ;
#12268=DIRECTION ( 'NONE',  ( -1.000000000000000000, 0.000000000000000000, 0.000000000000000000 ) ) ;
#12284=DIRECTION ( 'NONE',  ( 0.000000000000000000, 0.000000000000000000, 1.000000000000000000 ) ) ;
#12298=DIRECTION ( 'NONE',  ( -1.000000000000000000, -8.951101527228104953E-17, 0.000000000000000000 ) ) ;
#12307=DIRECTION ( 'NONE',  ( -1.000000000000000000, 0.000000000000000000, 0.000000000000000000 ) ) ;
#12309=ORIENTED_EDGE ( 'NONE', *, *, #6353, .T. ) ;
#12312=DIRECTION ( 'NONE',  ( 0.000000000000000000, 0.000000000000000000, -1.000000000000000000 ) ) ;
#12319=PLANE ( 'NONE',  #50204 ) ;
#12321=AXIS2_PLACEMENT_3D ( 'NONE', #59736, #49476, #11284 ) ;
#12342=CARTESIAN_POINT ( 'NONE',  ( 7.250000000000004441, 7.450000000000001954, -14.50000000000000000 ) ) ;
#12351=FACE_OUTER_BOUND ( 'NONE', #16788, .T. ) ;
#12352=LINE ( 'NONE', #50198, #28199 ) ;
#12355=ORIENTED_EDGE ( 'NONE', *, *, #29900, .T. ) ;
#12356=CARTESIAN_POINT ( 'NONE',  ( 7.450000000000006395, 7.250000000000000888, -20.50000000000000000 ) ) ;
#12358=ORIENTED_EDGE ( 'NONE', *, *, #49322, .T. ) ;
#12361=ORIENTED_EDGE ( 'NONE', *, *, #65744, .T. ) ;
#12363=FACE_OUTER_BOUND ( 'NONE', #57902, .T. ) ;
#12380=ADVANCED_FACE ( 'NONE', ( #63709 ), #38235, .F. ) ;
#12397=AXIS2_PLACEMENT_3D ( 'NONE', #53885, #5083, #16741 ) ;
#12403=ORIENTED_EDGE ( 'NONE', *, *, #57376, .T. ) ;
#12417=PLANE ( 'NONE',  #63575 ) ;
#12418=AXIS2_PLACEMENT_3D ( 'NONE', #25158, #46713, #8178 ) ;
#12421=VERTEX_POINT ( 'NONE', #16301 ) ;
#12422=EDGE_CURVE ( 'NONE', #66751, #20472, #33311, .T. ) ;
#12427=ORIENTED_EDGE ( 'NONE', *, *, #50874, .T. ) ;
#12444=VECTOR ( 'NONE', #15079, 1000.000000000000000 ) ;
#12454=EDGE_CURVE ( 'NONE', #62655, #60123, #6390, .T. ) ;
#12458=( NAMED_UNIT ( * ) SI_UNIT ( $, .STERADIAN. ) SOLID_ANGLE_UNIT ( ) );
#12461=ORIENTED_EDGE ( 'NONE', *, *, #37659, .T. ) ;
#12463=EDGE_CURVE ( 'NONE', #27858, #47920, #23338, .T. ) ;
#12472=DIRECTION ( 'NONE',  ( -1.000000000000000000, 0.000000000000000000, 0.000000000000000000 ) ) ;
#12473=VECTOR ( 'NONE', #42469, 1000.000000000000000 ) ;
#12474=DIRECTION ( 'NONE',  ( -0.000000000000000000, -0.000000000000000000, 1.000000000000000000 ) ) ;
#12487=VECTOR ( 'NONE', #9978, 1000.000000000000000 ) ;
#12491=ORIENTED_EDGE ( 'NONE', *, *, #8648, .F. ) ;
#12499=( NAMED_UNIT ( * ) SI_UNIT ( $, .STERADIAN. ) SOLID_ANGLE_UNIT ( ) );
#12501=VERTEX_POINT ( 'NONE', #54833 ) ;
#12524=CARTESIAN_POINT ( 'NONE',  ( -8.250000000000001776, 7.250000000000000888, -10.50000000000000000 ) ) ;
#12529=DIRECTION ( 'NONE',  ( -1.000000000000000000, 0.000000000000000000, 0.000000000000000000 ) ) ;
#12530=VECTOR ( 'NONE', #49586, 1000.000000000000000 ) ;
#12537=CIRCLE ( 'NONE', #2353, 0.9999999999999991118 ) ;
#12541=LINE ( 'NONE', #44365, #28662 ) ;
#12548=CIRCLE ( 'NONE', #6904, 1.000000000000000000 ) ;
#12549=CARTESIAN_POINT ( 'NONE',  ( 0.000000000000000000, -7.449999999999998401, -24.50000000000000000 ) ) ;
#12577=CARTESIAN_POINT ( 'NONE',  ( -7.450000000000001954, 0.000000000000000000, -14.50000000000000000 ) ) ;
#12587=AXIS2_PLACEMENT_3D ( 'NONE', #19793, #8486, #30063 ) ;
#12590=DIRECTION ( 'NONE',  ( 0.000000000000000000, 0.000000000000000000, 1.000000000000000000 ) ) ;
#12600=EDGE_CURVE ( 'NONE', #28426, #66278, #68387, .T. ) ;
#12604=CARTESIAN_POINT ( 'NONE',  ( 8.689999999999999503, 8.750000000000000000, -7.000000000000000000 ) ) ;
#12610=DIRECTION ( 'NONE',  ( -0.000000000000000000, -0.000000000000000000, 1.000000000000000000 ) ) ;
#12615=LINE ( 'NONE', #55096, #56452 ) ;
#12616=VECTOR ( 'NONE', #13843, 1000.000000000000000 ) ;
#12636=EDGE_CURVE ( 'NONE', #16237, #40446, #24023, .T. ) ;
#12637=ORIENTED_EDGE ( 'NONE', *, *, #20451, .T. ) ;
#12638=CARTESIAN_POINT ( 'NONE',  ( -7.250000000000000888, 7.450000000000003730, -13.50000000000000178 ) ) ;
#12644=EDGE_CURVE ( 'NONE', #19811, #63685, #3519, .T. ) ;
#12646=CARTESIAN_POINT ( 'NONE',  ( 8.250000000000005329, 7.250000000000000888, -26.00000000000001066 ) ) ;
#12649=PLANE ( 'NONE',  #14946 ) ;
#12653=LINE ( 'NONE', #34218, #64080 ) ;
#12655=ORIENTED_EDGE ( 'NONE', *, *, #48346, .T. ) ;
#12683=ORIENTED_EDGE ( 'NONE', *, *, #35168, .F. ) ;
#12686=FACE_OUTER_BOUND ( 'NONE', #32234, .T. ) ;
#12700=ORIENTED_EDGE ( 'NONE', *, *, #407, .T. ) ;
#12702=DIRECTION ( 'NONE',  ( 0.000000000000000000, 1.000000000000000000, 0.000000000000000000 ) ) ;
#12705=ORIENTED_EDGE ( 'NONE', *, *, #64533, .T. ) ;
#12706=DIRECTION ( 'NONE',  ( 0.000000000000000000, 0.000000000000000000, 1.000000000000000000 ) ) ;
#12708=CARTESIAN_POINT ( 'NONE',  ( -7.250000000000000888, 7.450000000000003730, -12.50000000000000000 ) ) ;
#12709=ORIENTED_EDGE ( 'NONE', *, *, #68032, .T. ) ;
#12718=DIRECTION ( 'NONE',  ( 0.000000000000000000, 1.000000000000000000, -0.000000000000000000 ) ) ;
#12722=EDGE_LOOP ( 'NONE', ( #5837, #42142, #61794, #41940 ) ) ;
#12729=EDGE_CURVE ( 'NONE', #2339, #9556, #69267, .T. ) ;
#12732=ORIENTED_EDGE ( 'NONE', *, *, #66486, .T. ) ;
#12734=CARTESIAN_POINT ( 'NONE',  ( -7.250000000000000888, 8.250000000000001776, -9.000000000000001776 ) ) ;
#12738=DIRECTION ( 'NONE',  ( -0.000000000000000000, -0.000000000000000000, 1.000000000000000000 ) ) ;
#12748=ORIENTED_EDGE ( 'NONE', *, *, #3354, .T. ) ;
#12749=ORIENTED_EDGE ( 'NONE', *, *, #19568, .F. ) ;
#12753=FACE_OUTER_BOUND ( 'NONE', #5020, .T. ) ;
#12761=VERTEX_POINT ( 'NONE', #4920 ) ;
#12774=DIRECTION ( 'NONE',  ( -1.000000000000000000, 0.000000000000000000, 0.000000000000000000 ) ) ;
#12775=DIRECTION ( 'NONE',  ( 0.000000000000000000, 0.000000000000000000, -1.000000000000000000 ) ) ;
#12780=DIRECTION ( 'NONE',  ( -1.794541526872559352E-16, -1.000000000000000000, 0.000000000000000000 ) ) ;
#12783=CARTESIAN_POINT ( 'NONE',  ( -7.450000000000001954, 0.000000000000000000, -22.50000000000000000 ) ) ;
#12784=ORIENTED_EDGE ( 'NONE', *, *, #16553, .T. ) ;
#12785=DIRECTION ( 'NONE',  ( -0.000000000000000000, -0.000000000000000000, -1.000000000000000000 ) ) ;
#12786=ADVANCED_FACE ( 'NONE', ( #4232 ), #15874, .T. ) ;
#12796=VECTOR ( 'NONE', #50045, 1000.000000000000000 ) ;
#12797=DIRECTION ( 'NONE',  ( 0.000000000000000000, 0.000000000000000000, -1.000000000000000000 ) ) ;
#12802=FACE_OUTER_BOUND ( 'NONE', #1637, .T. ) ;
#12804=CARTESIAN_POINT ( 'NONE',  ( 8.250000000000005329, 7.250000000000000888, -26.00000000000001066 ) ) ;
#12807=DIRECTION ( 'NONE',  ( 1.000000000000000000, 0.000000000000000000, 0.000000000000000000 ) ) ;
#12838=EDGE_LOOP ( 'NONE', ( #39428, #43601, #19082, #53400 ) ) ;
#12839=VERTEX_POINT ( 'NONE', #47348 ) ;
#12851=CIRCLE ( 'NONE', #17357, 0.1999999999999987899 ) ;
#12861=EDGE_LOOP ( 'NONE', ( #58453, #29175, #9, #56231 ) ) ;
#12868=EDGE_CURVE ( 'NONE', #29522, #58319, #22566, .T. ) ;
#12871=EDGE_LOOP ( 'NONE', ( #43806, #18509, #54281, #64863, #23466, #9545, #13626, #8303 ) ) ;
#12872=AXIS2_PLACEMENT_3D ( 'NONE', #43270, #37635, #69809 ) ;
#12875=CARTESIAN_POINT ( 'NONE',  ( -7.250000000000000000, -7.449999999999998401, -14.50000000000000000 ) ) ;
#12876=EDGE_CURVE ( 'NONE', #60406, #16354, #44454, .T. ) ;
#12885=VERTEX_POINT ( 'NONE', #34184 ) ;
#12887=CARTESIAN_POINT ( 'NONE',  ( -7.250000000000000888, 8.250000000000001776, -26.00000000000001066 ) ) ;
#12893=CIRCLE ( 'NONE', #47903, 1.000000000000000000 ) ;
#12894=PLANE ( 'NONE',  #37759 ) ;
#12896=DIRECTION ( 'NONE',  ( -0.000000000000000000, -0.000000000000000000, 1.000000000000000000 ) ) ;
#12921=EDGE_LOOP ( 'NONE', ( #68765, #9668, #24744, #22118, #62463, #46637, #30018, #56943 ) ) ;
#12928=AXIS2_PLACEMENT_3D ( 'NONE', #13693, #19686, #42315 ) ;
#12930=EDGE_CURVE ( 'NONE', #2145, #57928, #39501, .T. ) ;
#12932=EDGE_LOOP ( 'NONE', ( #6479, #54895, #38252, #50652 ) ) ;
#12937=LINE ( 'NONE', #40520, #39065 ) ;
#12945=PLANE ( 'NONE',  #21109 ) ;
#12950=VECTOR ( 'NONE', #48661, 1000.000000000000000 ) ;
#12958=CYLINDRICAL_SURFACE ( 'NONE', #5016, 1.000000000000000000 ) ;
#12960=CARTESIAN_POINT ( 'NONE',  ( -7.250000000000000888, 7.250000000000001776, -16.50000000000000000 ) ) ;
#12964=DIRECTION ( 'NONE',  ( -1.000000000000000000, 1.794541526872559352E-16, 0.000000000000000000 ) ) ;
#12965=DIRECTION ( 'NONE',  ( -1.000000000000000000, 0.000000000000000000, 0.000000000000000000 ) ) ;
#12976=DIRECTION ( 'NONE',  ( -0.000000000000000000, -0.000000000000000000, 1.000000000000000000 ) ) ;
#12977=CARTESIAN_POINT ( 'NONE',  ( 7.250000000000005329, -7.249999999999998224, -20.00000000000000000 ) ) ;
#12979=DIRECTION ( 'NONE',  ( 1.000000000000000000, 0.000000000000000000, 0.000000000000000000 ) ) ;
#12981=ORIENTED_EDGE ( 'NONE', *, *, #53160, .F. ) ;
#12992=AXIS2_PLACEMENT_3D ( 'NONE', #56173, #3130, #50847 ) ;
#12996=VECTOR ( 'NONE', #27656, 1000.000000000000000 ) ;
#13003=ORIENTED_EDGE ( 'NONE', *, *, #38830, .F. ) ;
#13007=DIRECTION ( 'NONE',  ( -0.000000000000000000, -0.000000000000000000, -1.000000000000000000 ) ) ;
#13018=DIRECTION ( 'NONE',  ( 1.000000000000000000, -5.981805089575196197E-17, 0.000000000000000000 ) ) ;
#13024=ORIENTED_EDGE ( 'NONE', *, *, #22491, .T. ) ;
#13029=CARTESIAN_POINT ( 'NONE',  ( -7.250000000000001776, -7.249999999999998224, -7.000000000000000000 ) ) ;
#13030=PLANE ( 'NONE',  #13163 ) ;
#13033=EDGE_CURVE ( 'NONE', #37116, #55879, #57069, .T. ) ;
#13047=AXIS2_PLACEMENT_3D ( 'NONE', #48636, #54296, #65923 ) ;
#13050=FACE_OUTER_BOUND ( 'NONE', #19450, .T. ) ;
#13054=DIRECTION ( 'NONE',  ( 1.000000000000000000, 0.000000000000000000, 0.000000000000000000 ) ) ;
#13056=CYLINDRICAL_SURFACE ( 'NONE', #21083, 0.1999999999999996503 ) ;
#13066=ORIENTED_EDGE ( 'NONE', *, *, #60434, .T. ) ;
#13079=AXIS2_PLACEMENT_3D ( 'NONE', #32392, #1250, #44021 ) ;
#13086=CARTESIAN_POINT ( 'NONE',  ( -7.250000000000000888, 8.250000000000001776, -9.500000000000001776 ) ) ;
#13091=EDGE_LOOP ( 'NONE', ( #13149, #60862, #50717, #60950 ) ) ;
#13107=CARTESIAN_POINT ( 'NONE',  ( 7.250000000000005329, 7.250000000000000888, -24.50000000000000000 ) ) ;
#13117=DIRECTION ( 'NONE',  ( 0.000000000000000000, 0.000000000000000000, 1.000000000000000000 ) ) ;
#13120=DIRECTION ( 'NONE',  ( 0.000000000000000000, 0.000000000000000000, 1.000000000000000000 ) ) ;
#13121=DIRECTION ( 'NONE',  ( -1.000000000000000000, 0.000000000000000000, 0.000000000000000000 ) ) ;
#13124=DIRECTION ( 'NONE',  ( 0.000000000000000000, 0.000000000000000000, 1.000000000000000000 ) ) ;
#13125=DIRECTION ( 'NONE',  ( 1.000000000000000000, 0.000000000000000000, 0.000000000000000000 ) ) ;
#13133=EDGE_LOOP ( 'NONE', ( #62699, #4352, #26310, #24239 ) ) ;
#13141=EDGE_CURVE ( 'NONE', #1276, #14260, #34491, .T. ) ;
#13143=AXIS2_PLACEMENT_3D ( 'NONE', #5354, #52749, #26912 ) ;
#13146=ORIENTED_EDGE ( 'NONE', *, *, #27199, .T. ) ;
#13149=ORIENTED_EDGE ( 'NONE', *, *, #14654, .F. ) ;
#13150=VECTOR ( 'NONE', #36660, 1000.000000000000000 ) ;
#13160=VERTEX_POINT ( 'NONE', #9431 ) ;
#13163=AXIS2_PLACEMENT_3D ( 'NONE', #17998, #61122, #34251 ) ;
#13169=DIRECTION ( 'NONE',  ( -0.000000000000000000, -0.000000000000000000, 1.000000000000000000 ) ) ;
#13178=VERTEX_POINT ( 'NONE', #26748 ) ;
#13180=EDGE_CURVE ( 'NONE', #2734, #30841, #15785, .T. ) ;
#13183=EDGE_CURVE ( 'NONE', #59074, #30760, #10822, .T. ) ;
#13188=DIRECTION ( 'NONE',  ( 1.000000000000000000, 0.000000000000000000, 0.000000000000000000 ) ) ;
#13194=VERTEX_POINT ( 'NONE', #42998 ) ;
#13198=ORIENTED_EDGE ( 'NONE', *, *, #21253, .T. ) ;
#13208=EDGE_LOOP ( 'NONE', ( #5378, #14852, #20083, #51125, #46877, #3228, #14531, #25939 ) ) ;
#13221=VERTEX_POINT ( 'NONE', #21091 ) ;
#13234=DIRECTION ( 'NONE',  ( 1.000000000000000000, 0.000000000000000000, 0.000000000000000000 ) ) ;
#13238=ORIENTED_EDGE ( 'NONE', *, *, #29787, .T. ) ;
#13239=CARTESIAN_POINT ( 'NONE',  ( 7.250000000000005329, -7.249999999999998224, -16.50000000000000000 ) ) ;
#13240=EDGE_CURVE ( 'NONE', #25255, #60406, #41317, .T. ) ;
#13246=AXIS2_PLACEMENT_3D ( 'NONE', #56108, #50455, #18259 ) ;
#13247=ADVANCED_FACE ( 'NONE', ( #58221 ), #10479, .T. ) ;
#13248=CARTESIAN_POINT ( 'NONE',  ( -8.750000000000003553, -7.348062532927999158, 5.000000000000000000 ) ) ;
#13249=DIRECTION ( 'NONE',  ( -0.000000000000000000, -0.000000000000000000, 1.000000000000000000 ) ) ;
#13252=ORIENTED_EDGE ( 'NONE', *, *, #14494, .T. ) ;
#13255=DIRECTION ( 'NONE',  ( 1.000000000000000000, -0.000000000000000000, 0.000000000000000000 ) ) ;
#13267=ORIENTED_EDGE ( 'NONE', *, *, #4007, .T. ) ;
#13276=DIRECTION ( 'NONE',  ( 1.000000000000000000, 0.000000000000000000, 0.000000000000000000 ) ) ;
#13281=ORIENTED_EDGE ( 'NONE', *, *, #69088, .F. ) ;
#13291=FACE_OUTER_BOUND ( 'NONE', #12932, .T. ) ;
#13298=CARTESIAN_POINT ( 'NONE',  ( 8.250000000000005329, 0.000000000000000000, -13.00000000000000178 ) ) ;
#13309=ADVANCED_FACE ( 'NONE', ( #44718 ), #55691, .T. ) ;
#13321=FACE_OUTER_BOUND ( 'NONE', #46303, .T. ) ;
#13322=CARTESIAN_POINT ( 'NONE',  ( 0.000000000000000000, -8.249999999999998224, -12.50000000000000000 ) ) ;
#13332=VECTOR ( 'NONE', #5721, 1000.000000000000000 ) ;
#13334=ADVANCED_FACE ( 'NONE', ( #39080 ), #59621, .F. ) ;
#13336=EDGE_CURVE ( 'NONE', #31143, #69756, #32737, .T. ) ;
#13339=CARTESIAN_POINT ( 'NONE',  ( 7.250000000000005329, -7.449999999999998401, -22.50000000000000000 ) ) ;
#13362=CARTESIAN_POINT ( 'NONE',  ( 8.250000000000005329, 0.000000000000000000, -18.50000000000000000 ) ) ;
#13366=EDGE_CURVE ( 'NONE', #26371, #36344, #18549, .T. ) ;
#13375=CYLINDRICAL_SURFACE ( 'NONE', #14294, 0.8100000000000017186 ) ;
#13382=ORIENTED_EDGE ( 'NONE', *, *, #49864, .T. ) ;
#13386=DIRECTION ( 'NONE',  ( 0.000000000000000000, 0.000000000000000000, 1.000000000000000000 ) ) ;
#13399=EDGE_CURVE ( 'NONE', #63180, #26023, #51471, .T. ) ;
#13400=CARTESIAN_POINT ( 'NONE',  ( 8.250000000000005329, -8.249999999999998224, -26.00000000000001066 ) ) ;
#13409=FACE_OUTER_BOUND ( 'NONE', #10442, .T. ) ;
#13421=VECTOR ( 'NONE', #43592, 1000.000000000000000 ) ;
#13439=ORIENTED_EDGE ( 'NONE', *, *, #65268, .F. ) ;
#13442=VECTOR ( 'NONE', #18246, 1000.000000000000000 ) ;
#13453=LINE ( 'NONE', #25472, #55029 ) ;
#13459=DIRECTION ( 'NONE',  ( -1.794541526872559352E-16, -1.000000000000000000, 0.000000000000000000 ) ) ;
#13472=AXIS2_PLACEMENT_3D ( 'NONE', #68167, #52979, #4529 ) ;
#13474=CARTESIAN_POINT ( 'NONE',  ( 7.250000000000005329, 7.250000000000000888, -12.50000000000000000 ) ) ;
#13475=ORIENTED_EDGE ( 'NONE', *, *, #4065, .F. ) ;
#13476=ORIENTED_EDGE ( 'NONE', *, *, #38350, .T. ) ;
#13478=DIRECTION ( 'NONE',  ( 0.000000000000000000, 0.000000000000000000, -1.000000000000000000 ) ) ;
#13487=EDGE_CURVE ( 'NONE', #65843, #53480, #58054, .T. ) ;
#13492=DIRECTION ( 'NONE',  ( -1.000000000000000000, 0.000000000000000000, 0.000000000000000000 ) ) ;
#13495=LINE ( 'NONE', #46718, #30548 ) ;
#13500=CARTESIAN_POINT ( 'NONE',  ( 7.250000000000005329, -7.249999999999998224, -16.00000000000000000 ) ) ;
#13507=EDGE_CURVE ( 'NONE', #52907, #16354, #4334, .T. ) ;
#13509=LINE ( 'NONE', #20213, #60007 ) ;
#13521=DIRECTION ( 'NONE',  ( -0.000000000000000000, -0.000000000000000000, 1.000000000000000000 ) ) ;
#13524=CARTESIAN_POINT ( 'NONE',  ( 7.250000000000005329, -7.249999999999998224, -9.500000000000001776 ) ) ;
#13527=CARTESIAN_POINT ( 'NONE',  ( 7.250000000000005329, -7.449999999999998401, -18.50000000000000000 ) ) ;
#13528=DIRECTION ( 'NONE',  ( 0.000000000000000000, -0.000000000000000000, 1.000000000000000000 ) ) ;
#13530=VERTEX_POINT ( 'NONE', #15633 ) ;
#13531=ORIENTED_EDGE ( 'NONE', *, *, #37352, .F. ) ;
#13550=AXIS2_PLACEMENT_3D ( 'NONE', #51685, #9249, #2527 ) ;
#13558=ORIENTED_EDGE ( 'NONE', *, *, #66618, .F. ) ;
#13569=CIRCLE ( 'NONE', #58764, 0.1999999999999996503 ) ;
#13571=ORIENTED_EDGE ( 'NONE', *, *, #42443, .T. ) ;
#13574=DIRECTION ( 'NONE',  ( 1.000000000000000000, 0.000000000000000000, 0.000000000000000000 ) ) ;
#13576=LINE ( 'NONE', #2270, #49879 ) ;
#13577=CARTESIAN_POINT ( 'NONE',  ( 7.450000000000003730, -7.249999999999997335, -23.50000000000000000 ) ) ;
#13583=LINE ( 'NONE', #35136, #54349 ) ;
#13599=AXIS2_PLACEMENT_3D ( 'NONE', #47756, #59421, #59762 ) ;
#13601=ADVANCED_FACE ( 'NONE', ( #37892 ), #53121, .F. ) ;
#13608=DIRECTION ( 'NONE',  ( 1.000000000000000000, -0.000000000000000000, 0.000000000000000000 ) ) ;
#13614=AXIS2_PLACEMENT_3D ( 'NONE', #13961, #35170, #66326 ) ;
#13626=ORIENTED_EDGE ( 'NONE', *, *, #58009, .F. ) ;
#13633=DIRECTION ( 'NONE',  ( -1.000000000000000000, 0.000000000000000000, 0.000000000000000000 ) ) ;
#13634=FACE_OUTER_BOUND ( 'NONE', #9880, .T. ) ;
#13636=VERTEX_POINT ( 'NONE', #15972 ) ;
#13638=FACE_BOUND ( 'NONE', #29626, .T. ) ;
#13646=DIRECTION ( 'NONE',  ( 0.000000000000000000, 0.000000000000000000, -1.000000000000000000 ) ) ;
#13653=ORIENTED_EDGE ( 'NONE', *, *, #16992, .T. ) ;
#13655=ORIENTED_EDGE ( 'NONE', *, *, #2247, .T. ) ;
#13660=DIRECTION ( 'NONE',  ( -1.000000000000000000, 0.000000000000000000, 0.000000000000000000 ) ) ;
#13662=EDGE_CURVE ( 'NONE', #65035, #40390, #51521, .T. ) ;
#13665=EDGE_CURVE ( 'NONE', #59933, #60538, #5719, .T. ) ;
#13671=PLANE ( 'NONE',  #19988 ) ;
#13673=DIRECTION ( 'NONE',  ( -1.000000000000000000, 0.000000000000000000, 0.000000000000000000 ) ) ;
#13675=DIRECTION ( 'NONE',  ( 0.000000000000000000, 0.000000000000000000, 1.000000000000000000 ) ) ;
#13687=EDGE_LOOP ( 'NONE', ( #49837, #36996, #37579, #22909, #38124, #23102, #42951, #46408 ) ) ;
#13693=CARTESIAN_POINT ( 'NONE',  ( 7.250000000000005329, 7.250000000000000888, -11.50000000000000000 ) ) ;
#13694=CARTESIAN_POINT ( 'NONE',  ( -7.250000000000000888, -8.249999999999998224, -25.50000000000000355 ) ) ;
#13707=AXIS2_PLACEMENT_3D ( 'NONE', #53830, #48168, #26950 ) ;
#13711=ORIENTED_EDGE ( 'NONE', *, *, #57610, .F. ) ;
#13724=ORIENTED_EDGE ( 'NONE', *, *, #15123, .F. ) ;
#13733=AXIS2_PLACEMENT_3D ( 'NONE', #69066, #41842, #9325 ) ;
#13741=ORIENTED_EDGE ( 'NONE', *, *, #55021, .T. ) ;
#13744=CARTESIAN_POINT ( 'NONE',  ( 7.250000000000004441, 7.450000000000001954, -12.50000000000000000 ) ) ;
#13755=DIRECTION ( 'NONE',  ( 0.000000000000000000, 0.000000000000000000, 1.000000000000000000 ) ) ;
#13763=CARTESIAN_POINT ( 'NONE',  ( -9.689999999999999503, -10.50000000000000178, 0.000000000000000000 ) ) ;
#13769=ORIENTED_EDGE ( 'NONE', *, *, #41480, .F. ) ;
#13774=ORIENTED_EDGE ( 'NONE', *, *, #15210, .T. ) ;
#13781=DIRECTION ( 'NONE',  ( -1.000000000000000000, 0.000000000000000000, 0.000000000000000000 ) ) ;
#13787=ORIENTED_EDGE ( 'NONE', *, *, #7987, .F. ) ;
#13790=EDGE_CURVE ( 'NONE', #46624, #54560, #7497, .T. ) ;
#13792=DIRECTION ( 'NONE',  ( 0.000000000000000000, 0.000000000000000000, -1.000000000000000000 ) ) ;
#13796=CYLINDRICAL_SURFACE ( 'NONE', #1357, 0.2000000000000005107 ) ;
#13797=ORIENTED_EDGE ( 'NONE', *, *, #52975, .F. ) ;
#13798=EDGE_CURVE ( 'NONE', #9544, #48304, #44914, .T. ) ;
#13800=CARTESIAN_POINT ( 'NONE',  ( 8.250000000000005329, 0.000000000000000000, -23.50000000000000000 ) ) ;
#13803=CARTESIAN_POINT ( 'NONE',  ( 7.450000000000004619, -1.336933437520057563E-15, -10.50000000000000000 ) ) ;
#13809=DIRECTION ( 'NONE',  ( 0.000000000000000000, 0.000000000000000000, -1.000000000000000000 ) ) ;
#13812=DIRECTION ( 'NONE',  ( 0.000000000000000000, 0.000000000000000000, -1.000000000000000000 ) ) ;
#13813=ORIENTED_EDGE ( 'NONE', *, *, #11995, .T. ) ;
#13815=VERTEX_POINT ( 'NONE', #65788 ) ;
#13816=VECTOR ( 'NONE', #43981, 1000.000000000000000 ) ;
#13819=FACE_OUTER_BOUND ( 'NONE', #45472, .T. ) ;
#13823=ADVANCED_FACE ( 'NONE', ( #33613 ), #6729, .T. ) ;
#13826=DIRECTION ( 'NONE',  ( 0.000000000000000000, -0.000000000000000000, -1.000000000000000000 ) ) ;
#13831=ORIENTED_EDGE ( 'NONE', *, *, #66754, .T. ) ;
#13841=DIRECTION ( 'NONE',  ( -1.000000000000000000, 0.000000000000000000, -0.000000000000000000 ) ) ;
#13843=DIRECTION ( 'NONE',  ( 1.000000000000000000, -5.981805089575194965E-17, 0.000000000000000000 ) ) ;
#13844=VECTOR ( 'NONE', #18558, 1000.000000000000000 ) ;
#13846=CARTESIAN_POINT ( 'NONE',  ( 7.250000000000005329, 7.250000000000000888, -22.00000000000000000 ) ) ;
#13861=ORIENTED_EDGE ( 'NONE', *, *, #37158, .F. ) ;
#13864=VERTEX_POINT ( 'NONE', #14846 ) ;
#13869=CARTESIAN_POINT ( 'NONE',  ( -7.250000000000000888, 7.250000000000001776, -7.000000000000000000 ) ) ;
#13872=VECTOR ( 'NONE', #10139, 1000.000000000000000 ) ;
#13877=CARTESIAN_POINT ( 'NONE',  ( 7.250000000000005329, -7.249999999999998224, -23.00000000000000000 ) ) ;
#13883=ORIENTED_EDGE ( 'NONE', *, *, #27720, .T. ) ;
#13898=EDGE_CURVE ( 'NONE', #24794, #25369, #51619, .T. ) ;
#13900=EDGE_LOOP ( 'NONE', ( #49965, #67156, #52060, #41916 ) ) ;
#13907=EDGE_LOOP ( 'NONE', ( #61341, #38932, #54987, #54004 ) ) ;
#13909=ORIENTED_EDGE ( 'NONE', *, *, #38950, .T. ) ;
#13919=ORIENTED_EDGE ( 'NONE', *, *, #26624, .T. ) ;
#13921=AXIS2_PLACEMENT_3D ( 'NONE', #12146, #45708, #18846 ) ;
#13925=ORIENTED_EDGE ( 'NONE', *, *, #61452, .F. ) ;
#13937=ADVANCED_FACE ( 'NONE', ( #67883 ), #35687, .F. ) ;
#13947=DIRECTION ( 'NONE',  ( 0.000000000000000000, 1.000000000000000000, -0.000000000000000000 ) ) ;
#13948=DIRECTION ( 'NONE',  ( -1.000000000000000000, 0.000000000000000000, 0.000000000000000000 ) ) ;
#13955=DIRECTION ( 'NONE',  ( 0.000000000000000000, 0.000000000000000000, 1.000000000000000000 ) ) ;
#13961=CARTESIAN_POINT ( 'NONE',  ( -9.690000000000001279, -9.690000000000001279, -4.250000000000000000 ) ) ;
#13963=CYLINDRICAL_SURFACE ( 'NONE', #25080, 0.2000000000000005107 ) ;
#13964=ORIENTED_EDGE ( 'NONE', *, *, #20622, .F. ) ;
#13973=DIRECTION ( 'NONE',  ( 0.000000000000000000, 0.000000000000000000, 1.000000000000000000 ) ) ;
#13985=DIRECTION ( 'NONE',  ( -1.000000000000000000, 0.000000000000000000, -0.000000000000000000 ) ) ;
#13987=VERTEX_POINT ( 'NONE', #15886 ) ;
#14005=LINE ( 'NONE', #19314, #43954 ) ;
#14033=ORIENTED_EDGE ( 'NONE', *, *, #24177, .T. ) ;
#14039=DIRECTION ( 'NONE',  ( 0.000000000000000000, 0.000000000000000000, 1.000000000000000000 ) ) ;
#14042=ORIENTED_EDGE ( 'NONE', *, *, #53456, .F. ) ;
#14049=CIRCLE ( 'NONE', #68271, 0.2000000000000005107 ) ;
#14052=ORIENTED_EDGE ( 'NONE', *, *, #69769, .T. ) ;
#14054=VERTEX_POINT ( 'NONE', #21879 ) ;
#14055=ORIENTED_EDGE ( 'NONE', *, *, #3776, .T. ) ;
#14057=ORIENTED_EDGE ( 'NONE', *, *, #12636, .F. ) ;
#14067=ORIENTED_EDGE ( 'NONE', *, *, #51436, .F. ) ;
#14079=ADVANCED_FACE ( 'NONE', ( #64331 ), #27197, .F. ) ;
#14084=CARTESIAN_POINT ( 'NONE',  ( -7.250000000000001776, -7.249999999999998224, -20.00000000000000000 ) ) ;
#14086=CARTESIAN_POINT ( 'NONE',  ( 7.250000000000005329, 8.250000000000001776, -26.00000000000001066 ) ) ;
#14090=AXIS2_PLACEMENT_3D ( 'NONE', #36796, #349, #10958 ) ;
#14102=LINE ( 'NONE', #9160, #67066 ) ;
#14104=DIRECTION ( 'NONE',  ( -0.000000000000000000, -0.000000000000000000, -1.000000000000000000 ) ) ;
#14115=CARTESIAN_POINT ( 'NONE',  ( 4.456444791733522252E-16, 7.450000000000002842, -12.00000000000000000 ) ) ;
#14117=VECTOR ( 'NONE', #59404, 1000.000000000000000 ) ;
#14126=CARTESIAN_POINT ( 'NONE',  ( -7.450000000000001954, -7.249999999999998224, -9.500000000000001776 ) ) ;
#14130=DIRECTION ( 'NONE',  ( 0.000000000000000000, 0.000000000000000000, -1.000000000000000000 ) ) ;
#14134=STYLED_ITEM ( 'NONE', ( #44990 ), #44754 ) ;
#14135=EDGE_LOOP ( 'NONE', ( #69268, #1617, #37887, #3638 ) ) ;
#14136=DIRECTION ( 'NONE',  ( -1.794541526872559352E-16, -1.000000000000000000, 0.000000000000000000 ) ) ;
#14138=ORIENTED_EDGE ( 'NONE', *, *, #63997, .T. ) ;
#14145=ORIENTED_EDGE ( 'NONE', *, *, #13790, .F. ) ;
#14146=DIRECTION ( 'NONE',  ( 0.000000000000000000, 0.000000000000000000, 1.000000000000000000 ) ) ;
#14149=DIRECTION ( 'NONE',  ( 0.000000000000000000, 1.000000000000000000, 0.000000000000000000 ) ) ;
#14153=CARTESIAN_POINT ( 'NONE',  ( 0.000000000000000000, -7.449999999999998401, -14.50000000000000000 ) ) ;
#14158=ORIENTED_EDGE ( 'NONE', *, *, #40103, .F. ) ;
#14189=FACE_OUTER_BOUND ( 'NONE', #53483, .T. ) ;
#14196=DIRECTION ( 'NONE',  ( 1.000000000000000000, 0.000000000000000000, 0.000000000000000000 ) ) ;
#14197=EDGE_CURVE ( 'NONE', #50347, #40313, #669, .T. ) ;
#14198=DIRECTION ( 'NONE',  ( 1.000000000000000000, -5.981805089575194965E-17, 0.000000000000000000 ) ) ;
#14220=AXIS2_PLACEMENT_3D ( 'NONE', #43923, #38633, #48545 ) ;
#14226=ORIENTED_EDGE ( 'NONE', *, *, #27557, .T. ) ;
#14228=ORIENTED_EDGE ( 'NONE', *, *, #66657, .F. ) ;
#14229=ADVANCED_FACE ( 'NONE', ( #22915, #61416 ), #22578, .T. ) ;
#14237=EDGE_CURVE ( 'NONE', #53541, #57893, #60439, .T. ) ;
#14260=VERTEX_POINT ( 'NONE', #8377 ) ;
#14275=ORIENTED_EDGE ( 'NONE', *, *, #56282, .T. ) ;
#14278=CARTESIAN_POINT ( 'NONE',  ( -7.250000000000001776, -7.249999999999998224, -13.50000000000000178 ) ) ;
#14284=VECTOR ( 'NONE', #7073, 1000.000000000000000 ) ;
#14294=AXIS2_PLACEMENT_3D ( 'NONE', #24337, #55815, #61821 ) ;
#14309=DIRECTION ( 'NONE',  ( -1.000000000000000000, 0.000000000000000000, 0.000000000000000000 ) ) ;
#14315=DIRECTION ( 'NONE',  ( -0.000000000000000000, -0.000000000000000000, 1.000000000000000000 ) ) ;
#14316=VERTEX_POINT ( 'NONE', #61787 ) ;
#14320=LINE ( 'NONE', #56738, #20643 ) ;
#14321=DIRECTION ( 'NONE',  ( 0.000000000000000000, -1.000000000000000000, 0.000000000000000000 ) ) ;
#14361=ORIENTED_EDGE ( 'NONE', *, *, #48744, .F. ) ;
#14370=CARTESIAN_POINT ( 'NONE',  ( -8.250000000000001776, -8.249999999999998224, -26.00000000000001066 ) ) ;
#14373=CARTESIAN_POINT ( 'NONE',  ( 7.250000000000005329, -7.249999999999998224, -20.00000000000000000 ) ) ;
#14374=AXIS2_PLACEMENT_3D ( 'NONE', #3009, #35882, #8997 ) ;
#14377=DIRECTION ( 'NONE',  ( -0.000000000000000000, 0.000000000000000000, 1.000000000000000000 ) ) ;
#14379=DIRECTION ( 'NONE',  ( -1.000000000000000000, 0.000000000000000000, 0.000000000000000000 ) ) ;
#14381=LINE ( 'NONE', #63526, #55891 ) ;
#14384=VECTOR ( 'NONE', #20167, 1000.000000000000000 ) ;
#14390=ADVANCED_FACE ( 'NONE', ( #53296 ), #25724, .T. ) ;
#14392=DIRECTION ( 'NONE',  ( 0.000000000000000000, 0.000000000000000000, -1.000000000000000000 ) ) ;
#14401=FACE_OUTER_BOUND ( 'NONE', #59122, .T. ) ;
#14402=DIRECTION ( 'NONE',  ( 1.000000000000000000, 0.000000000000000000, 0.000000000000000000 ) ) ;
#14410=DIRECTION ( 'NONE',  ( 0.000000000000000000, 0.000000000000000000, -1.000000000000000000 ) ) ;
#14422=CIRCLE ( 'NONE', #36999, 1.000000000000000000 ) ;
#14423=LINE ( 'NONE', #63913, #51478 ) ;
#14439=EDGE_CURVE ( 'NONE', #66152, #52010, #37906, .T. ) ;
#14453=CARTESIAN_POINT ( 'NONE',  ( -7.450000000000001954, 7.250000000000000000, -20.50000000000000000 ) ) ;
#14459=DIRECTION ( 'NONE',  ( 1.000000000000000000, 0.000000000000000000, 0.000000000000000000 ) ) ;
#14460=CARTESIAN_POINT ( 'NONE',  ( 7.250000000000004441, 7.450000000000001954, -8.500000000000000000 ) ) ;
#14461=CARTESIAN_POINT ( 'NONE',  ( -7.450000000000001954, -7.249999999999998224, -13.00000000000000178 ) ) ;
#14464=CARTESIAN_POINT ( 'NONE',  ( 0.000000000000000000, 0.000000000000000000, -16.00000000000000000 ) ) ;
#14471=CARTESIAN_POINT ( 'NONE',  ( 7.450000000000006395, 7.250000000000000888, -20.00000000000000000 ) ) ;
#14480=AXIS2_PLACEMENT_3D ( 'NONE', #47371, #26507, #69653 ) ;
#14483=LINE ( 'NONE', #46644, #60636 ) ;
#14488=CARTESIAN_POINT ( 'NONE',  ( -7.250000000000000888, 7.250000000000001776, -26.00000000000001066 ) ) ;
#14494=EDGE_CURVE ( 'NONE', #9143, #49824, #236, .T. ) ;
#14500=CARTESIAN_POINT ( 'NONE',  ( -7.250000000000000888, 7.250000000000001776, -10.50000000000000000 ) ) ;
#14506=ORIENTED_EDGE ( 'NONE', *, *, #18107, .T. ) ;
#14510=LINE ( 'NONE', #41374, #50746 ) ;
#14518=DIRECTION ( 'NONE',  ( -0.000000000000000000, -0.000000000000000000, -1.000000000000000000 ) ) ;
#14520=EDGE_LOOP ( 'NONE', ( #4338, #34062, #47298, #15387, #55149, #9853, #28215, #59700 ) ) ;
#14529=CARTESIAN_POINT ( 'NONE',  ( 7.250000000000005329, -7.249999999999998224, -13.50000000000000178 ) ) ;
#14531=ORIENTED_EDGE ( 'NONE', *, *, #61585, .T. ) ;
#14540=CARTESIAN_POINT ( 'NONE',  ( 7.250000000000005329, 7.250000000000000888, -10.50000000000000000 ) ) ;
#14552=CARTESIAN_POINT ( 'NONE',  ( 8.250000000000005329, -7.249999999999998224, -9.000000000000001776 ) ) ;
#14553=ORIENTED_EDGE ( 'NONE', *, *, #62355, .F. ) ;
#14557=EDGE_CURVE ( 'NONE', #67314, #69920, #5887, .T. ) ;
#14560=ORIENTED_EDGE ( 'NONE', *, *, #57067, .F. ) ;
#14561=DIRECTION ( 'NONE',  ( 0.000000000000000000, 0.000000000000000000, -1.000000000000000000 ) ) ;
#14563=VERTEX_POINT ( 'NONE', #28471 ) ;
#14565=VECTOR ( 'NONE', #13633, 1000.000000000000000 ) ;
#14574=ORIENTED_EDGE ( 'NONE', *, *, #9346, .T. ) ;
#14584=EDGE_LOOP ( 'NONE', ( #28093, #67191, #28794, #47838, #28017, #56989, #57716, #28423 ) ) ;
#14592=DIRECTION ( 'NONE',  ( -1.000000000000000000, 0.000000000000000000, 0.000000000000000000 ) ) ;
#14594=DIRECTION ( 'NONE',  ( 0.000000000000000000, 0.000000000000000000, 1.000000000000000000 ) ) ;
#14596=VECTOR ( 'NONE', #42474, 1000.000000000000000 ) ;
#14601=EDGE_CURVE ( 'NONE', #33973, #49824, #32750, .T. ) ;
#14610=CARTESIAN_POINT ( 'NONE',  ( -7.250000000000000000, -7.449999999999998401, -11.50000000000000000 ) ) ;
#14613=LINE ( 'NONE', #20266, #62722 ) ;
#14614=ORIENTED_EDGE ( 'NONE', *, *, #1238, .T. ) ;
#14617=DIRECTION ( 'NONE',  ( 0.000000000000000000, 0.000000000000000000, 1.000000000000000000 ) ) ;
#14619=CARTESIAN_POINT ( 'NONE',  ( -7.750000000000001776, -7.348062532927999158, 0.000000000000000000 ) ) ;
#14623=VECTOR ( 'NONE', #32170, 1000.000000000000000 ) ;
#14629=EDGE_CURVE ( 'NONE', #20614, #51641, #31148, .T. ) ;
#14633=EDGE_CURVE ( 'NONE', #69920, #40971, #38410, .T. ) ;
#14634=DIRECTION ( 'NONE',  ( 0.000000000000000000, 1.000000000000000000, 0.000000000000000000 ) ) ;
#14641=CARTESIAN_POINT ( 'NONE',  ( 8.250000000000005329, 0.000000000000000000, -8.500000000000000000 ) ) ;
#14644=EDGE_CURVE ( 'NONE', #36079, #63788, #23237, .T. ) ;
#14650=CARTESIAN_POINT ( 'NONE',  ( 0.000000000000000000, -8.249999999999998224, -16.50000000000000000 ) ) ;
#14654=EDGE_CURVE ( 'NONE', #63930, #28581, #6292, .T. ) ;
#14661=CARTESIAN_POINT ( 'NONE',  ( 0.000000000000000000, 0.000000000000000000, -11.00000000000000000 ) ) ;
#14662=CARTESIAN_POINT ( 'NONE',  ( -7.450000000000001954, 7.250000000000000000, -20.50000000000000000 ) ) ;
#14668=FACE_OUTER_BOUND ( 'NONE', #33696, .T. ) ;
#14677=DIRECTION ( 'NONE',  ( 0.000000000000000000, 0.000000000000000000, -1.000000000000000000 ) ) ;
#14678=VERTEX_POINT ( 'NONE', #3712 ) ;
#14691=ADVANCED_FACE ( 'NONE', ( #30241 ), #50738, .F. ) ;
#14692=CARTESIAN_POINT ( 'NONE',  ( 8.750000000000003553, 7.750000000000000000, 0.000000000000000000 ) ) ;
#14700=ORIENTED_EDGE ( 'NONE', *, *, #52760, .T. ) ;
#14701=EDGE_CURVE ( 'NONE', #15085, #19699, #9002, .T. ) ;
#14713=ORIENTED_EDGE ( 'NONE', *, *, #60023, .T. ) ;
#14714=VERTEX_POINT ( 'NONE', #8298 ) ;
#14718=CARTESIAN_POINT ( 'NONE',  ( 7.250000000000005329, 7.250000000000000888, -24.00000000000000000 ) ) ;
#14720=AXIS2_PLACEMENT_3D ( 'NONE', #62613, #8875, #24797 ) ;
#14721=EDGE_LOOP ( 'NONE', ( #50189, #34148, #66462, #5893 ) ) ;
#14722=ADVANCED_FACE ( 'NONE', ( #29171 ), #35889, .T. ) ;
#14727=ORIENTED_EDGE ( 'NONE', *, *, #2413, .T. ) ;
#14747=VECTOR ( 'NONE', #12165, 1000.000000000000000 ) ;
#14748=LINE ( 'NONE', #52219, #8181 ) ;
#14751=CARTESIAN_POINT ( 'NONE',  ( 7.450000000000004619, -1.336933437520057563E-15, -9.500000000000001776 ) ) ;
#14753=DIRECTION ( 'NONE',  ( 0.000000000000000000, -0.000000000000000000, 1.000000000000000000 ) ) ;
#14760=CARTESIAN_POINT ( 'NONE',  ( -7.450000000000001954, 0.000000000000000000, -16.50000000000000000 ) ) ;
#14763=ORIENTED_EDGE ( 'NONE', *, *, #28192, .T. ) ;
#14776=CARTESIAN_POINT ( 'NONE',  ( -8.250000000000001776, 7.250000000000000888, -25.50000000000000355 ) ) ;
#14780=AXIS2_PLACEMENT_3D ( 'NONE', #758, #54839, #22659 ) ;
#14796=LINE ( 'NONE', #15501, #50030 ) ;
#14799=DIRECTION ( 'NONE',  ( -0.000000000000000000, -0.000000000000000000, -1.000000000000000000 ) ) ;
#14806=VERTEX_POINT ( 'NONE', #30932 ) ;
#14809=DIRECTION ( 'NONE',  ( 0.000000000000000000, 0.000000000000000000, 1.000000000000000000 ) ) ;
#14810=VERTEX_POINT ( 'NONE', #15376 ) ;
#14813=LINE ( 'NONE', #9504, #35978 ) ;
#14822=CARTESIAN_POINT ( 'NONE',  ( -8.250000000000001776, -7.249999999999998224, -12.50000000000000000 ) ) ;
#14828=CARTESIAN_POINT ( 'NONE',  ( 9.690000000000001279, -9.690000000000001279, -5.000000000000000000 ) ) ;
#14832=PLANE ( 'NONE',  #68578 ) ;
#14842=FACE_OUTER_BOUND ( 'NONE', #33458, .T. ) ;
#14844=EDGE_CURVE ( 'NONE', #43562, #64155, #32333, .T. ) ;
#14845=VECTOR ( 'NONE', #3729, 1000.000000000000000 ) ;
#14846=CARTESIAN_POINT ( 'NONE',  ( -7.250000000000000888, 7.450000000000003730, -21.00000000000000000 ) ) ;
#14850=ORIENTED_EDGE ( 'NONE', *, *, #46148, .F. ) ;
#14852=ORIENTED_EDGE ( 'NONE', *, *, #55487, .T. ) ;
#14857=AXIS2_PLACEMENT_3D ( 'NONE', #35412, #3962, #19163 ) ;
#14859=CARTESIAN_POINT ( 'NONE',  ( -7.250000000000000888, 7.250000000000001776, -11.50000000000000000 ) ) ;
#14869=VECTOR ( 'NONE', #20362, 1000.000000000000000 ) ;
#14870=ORIENTED_EDGE ( 'NONE', *, *, #50771, .F. ) ;
#14880=CARTESIAN_POINT ( 'NONE',  ( 4.456444791733522252E-16, 7.450000000000002842, -16.50000000000000000 ) ) ;
#14885=ORIENTED_EDGE ( 'NONE', *, *, #23883, .T. ) ;
#14898=CARTESIAN_POINT ( 'NONE',  ( -7.250000000000000888, 8.250000000000001776, -18.50000000000000000 ) ) ;
#14900=EDGE_LOOP ( 'NONE', ( #6809, #63288, #30938, #61077 ) ) ;
#14901=FACE_OUTER_BOUND ( 'NONE', #26033, .T. ) ;
#14906=FACE_BOUND ( 'NONE', #1666, .T. ) ;
#14908=CARTESIAN_POINT ( 'NONE',  ( -7.250000000000000000, -7.449999999999998401, -25.50000000000000355 ) ) ;
#14918=LINE ( 'NONE', #36847, #24035 ) ;
#14924=CARTESIAN_POINT ( 'NONE',  ( -8.250000000000001776, 7.250000000000000888, -11.50000000000000000 ) ) ;
#14925=CARTESIAN_POINT ( 'NONE',  ( -8.750000000000001776, 7.250000000000000000, -26.00000000000001066 ) ) ;
#14946=AXIS2_PLACEMENT_3D ( 'NONE', #29262, #34573, #61810 ) ;
#14956=ORIENTED_EDGE ( 'NONE', *, *, #7601, .F. ) ;
#14970=VERTEX_POINT ( 'NONE', #16766 ) ;
#14973=CARTESIAN_POINT ( 'NONE',  ( -7.250000000000000888, 7.450000000000003730, -21.50000000000000000 ) ) ;
#14978=CARTESIAN_POINT ( 'NONE',  ( 7.450000000000006395, 7.250000000000000888, -18.50000000000000000 ) ) ;
#14990=ORIENTED_EDGE ( 'NONE', *, *, #2993, .F. ) ;
#14992=CARTESIAN_POINT ( 'NONE',  ( -7.250000000000000888, 7.450000000000003730, -20.00000000000000000 ) ) ;
#14995=ORIENTED_EDGE ( 'NONE', *, *, #63349, .F. ) ;
#14997=LINE ( 'NONE', #20294, #10605 ) ;
#15013=CARTESIAN_POINT ( 'NONE',  ( -7.250000000000000888, 8.250000000000001776, -13.50000000000000178 ) ) ;
#15025=CIRCLE ( 'NONE', #31994, 0.1999999999999987899 ) ;
#15031=CARTESIAN_POINT ( 'NONE',  ( 0.000000000000000000, 0.000000000000000000, -8.000000000000000000 ) ) ;
#15041=PLANE ( 'NONE',  #41073 ) ;
#15042=CARTESIAN_POINT ( 'NONE',  ( -7.250000000000001776, -7.249999999999998224, -25.50000000000000355 ) ) ;
#15051=ORIENTED_EDGE ( 'NONE', *, *, #53665, .T. ) ;
#15052=AXIS2_PLACEMENT_3D ( 'NONE', #16146, #59279, #26766 ) ;
#15056=LINE ( 'NONE', #59589, #27130 ) ;
#15062=EDGE_CURVE ( 'NONE', #15345, #26986, #54919, .T. ) ;
#15063=CARTESIAN_POINT ( 'NONE',  ( -8.250000000000001776, 0.000000000000000000, -23.50000000000000000 ) ) ;
#15070=FACE_OUTER_BOUND ( 'NONE', #25937, .T. ) ;
#15074=DIRECTION ( 'NONE',  ( -1.794541526872559352E-16, -1.000000000000000000, 0.000000000000000000 ) ) ;
#15076=DIRECTION ( 'NONE',  ( 0.000000000000000000, 0.000000000000000000, -1.000000000000000000 ) ) ;
#15079=DIRECTION ( 'NONE',  ( -0.000000000000000000, -0.000000000000000000, -1.000000000000000000 ) ) ;
#15080=CARTESIAN_POINT ( 'NONE',  ( 0.000000000000000000, -7.449999999999998401, -9.500000000000001776 ) ) ;
#15085=VERTEX_POINT ( 'NONE', #58027 ) ;
#15088=CARTESIAN_POINT ( 'NONE',  ( 7.450000000000006395, 7.250000000000000888, -24.50000000000000000 ) ) ;
#15091=VECTOR ( 'NONE', #6397, 1000.000000000000000 ) ;
#15095=CARTESIAN_POINT ( 'NONE',  ( 7.250000000000005329, 8.250000000000001776, -24.50000000000000000 ) ) ;
#15098=FACE_OUTER_BOUND ( 'NONE', #46517, .T. ) ;
#15100=ORIENTED_EDGE ( 'NONE', *, *, #44140, .T. ) ;
#15110=ADVANCED_FACE ( 'NONE', ( #14901 ), #53787, .F. ) ;
#15117=VERTEX_POINT ( 'NONE', #43155 ) ;
#15119=EDGE_CURVE ( 'NONE', #20472, #53691, #64730, .T. ) ;
#15123=EDGE_CURVE ( 'NONE', #48173, #25947, #10989, .T. ) ;
#15124=LINE ( 'NONE', #32079, #69561 ) ;
#15128=ORIENTED_EDGE ( 'NONE', *, *, #60336, .T. ) ;
#15134=DIRECTION ( 'NONE',  ( 0.000000000000000000, -1.000000000000000000, 0.000000000000000000 ) ) ;
#15153=ORIENTED_EDGE ( 'NONE', *, *, #2993, .T. ) ;
#15157=ORIENTED_EDGE ( 'NONE', *, *, #31259, .F. ) ;
#15158=CARTESIAN_POINT ( 'NONE',  ( 7.250000000000005329, -7.249999999999998224, -21.50000000000000000 ) ) ;
#15162=ORIENTED_EDGE ( 'NONE', *, *, #42795, .T. ) ;
#15169=DIRECTION ( 'NONE',  ( -0.000000000000000000, -0.000000000000000000, 1.000000000000000000 ) ) ;
#15171=AXIS2_PLACEMENT_3D ( 'NONE', #45274, #49897, #23379 ) ;
#15179=CARTESIAN_POINT ( 'NONE',  ( 7.250000000000004441, 7.450000000000001954, -19.50000000000000000 ) ) ;
#15192=DIRECTION ( 'NONE',  ( 0.000000000000000000, 0.000000000000000000, 1.000000000000000000 ) ) ;
#15207=CARTESIAN_POINT ( 'NONE',  ( 7.250000000000005329, 8.250000000000001776, -26.00000000000001066 ) ) ;
#15208=AXIS2_PLACEMENT_3D ( 'NONE', #43194, #59116, #54174 ) ;
#15210=EDGE_CURVE ( 'NONE', #51178, #12885, #28971, .T. ) ;
#15216=DIRECTION ( 'NONE',  ( 1.000000000000000000, 0.000000000000000000, 0.000000000000000000 ) ) ;
#15223=AXIS2_PLACEMENT_3D ( 'NONE', #6344, #31843, #33210 ) ;
#15229=ORIENTED_EDGE ( 'NONE', *, *, #8116, .T. ) ;
#15239=CARTESIAN_POINT ( 'NONE',  ( -9.690000000000001279, -9.750000000000001776, -4.250000000000000000 ) ) ;
#15240=CIRCLE ( 'NONE', #547, 1.000000000000000888 ) ;
#15245=ORIENTED_EDGE ( 'NONE', *, *, #39438, .T. ) ;
#15251=ORIENTED_EDGE ( 'NONE', *, *, #68668, .F. ) ;
#15253=EDGE_LOOP ( 'NONE', ( #21842, #21445, #4673, #31944, #402, #2274, #55051, #3224 ) ) ;
#15270=CARTESIAN_POINT ( 'NONE',  ( 7.250000000000005329, -7.449999999999998401, -12.50000000000000000 ) ) ;
#15271=ORIENTED_EDGE ( 'NONE', *, *, #22311, .T. ) ;
#15283=ORIENTED_EDGE ( 'NONE', *, *, #47040, .T. ) ;
#15284=DIRECTION ( 'NONE',  ( 0.000000000000000000, 0.000000000000000000, -1.000000000000000000 ) ) ;
#15285=ORIENTED_EDGE ( 'NONE', *, *, #26980, .T. ) ;
#15290=CIRCLE ( 'NONE', #3980, 0.1999999999999987899 ) ;
#15298=VERTEX_POINT ( 'NONE', #50889 ) ;
#15309=AXIS2_PLACEMENT_3D ( 'NONE', #22192, #16884, #38457 ) ;
#15310=CARTESIAN_POINT ( 'NONE',  ( -6.500000000000002665, -6.500000000000002665, -1.000000000000000000 ) ) ;
#15312=MECHANICAL_DESIGN_GEOMETRIC_PRESENTATION_REPRESENTATION('',(#14134),#48068);
#15317=ADVANCED_FACE ( 'NONE', ( #12351 ), #13056, .T. ) ;
#15329=ORIENTED_EDGE ( 'NONE', *, *, #34464, .T. ) ;
#15336=LINE ( 'NONE', #36919, #34402 ) ;
#15340=CARTESIAN_POINT ( 'NONE',  ( 7.450000000000004619, -1.336933437520057563E-15, -8.500000000000000000 ) ) ;
#15345=VERTEX_POINT ( 'NONE', #44896 ) ;
#15347=AXIS2_PLACEMENT_3D ( 'NONE', #32051, #36301, #57865 ) ;
#15348=CIRCLE ( 'NONE', #17595, 1.000000000000000000 ) ;
#15357=ORIENTED_EDGE ( 'NONE', *, *, #50955, .T. ) ;
#15359=CARTESIAN_POINT ( 'NONE',  ( 7.250000000000005329, -8.249999999999998224, -26.00000000000001066 ) ) ;
#15365=CYLINDRICAL_SURFACE ( 'NONE', #6745, 1.000000000000000000 ) ;
#15367=DIRECTION ( 'NONE',  ( 1.000000000000000000, 0.000000000000000000, 0.000000000000000000 ) ) ;
#15376=CARTESIAN_POINT ( 'NONE',  ( -8.250000000000001776, -7.249999999999998224, -23.50000000000000000 ) ) ;
#15382=ORIENTED_EDGE ( 'NONE', *, *, #26575, .T. ) ;
#15387=ORIENTED_EDGE ( 'NONE', *, *, #69626, .T. ) ;
#15391=AXIS2_PLACEMENT_3D ( 'NONE', #60673, #45092, #67715 ) ;
#15409=ADVANCED_FACE ( 'NONE', ( #45944 ), #18718, .T. ) ;
#15417=CARTESIAN_POINT ( 'NONE',  ( -7.250000000000000888, 7.450000000000003730, -9.000000000000001776 ) ) ;
#15430=DIRECTION ( 'NONE',  ( -1.000000000000000000, 0.000000000000000000, 0.000000000000000000 ) ) ;
#15433=CARTESIAN_POINT ( 'NONE',  ( 7.250000000000005329, 8.250000000000001776, -16.50000000000000000 ) ) ;
#15435=VECTOR ( 'NONE', #67990, 1000.000000000000000 ) ;
#15441=CARTESIAN_POINT ( 'NONE',  ( 0.000000000000000000, 8.250000000000001776, -23.00000000000000000 ) ) ;
#15452=EDGE_CURVE ( 'NONE', #7881, #22866, #40638, .T. ) ;
#15459=CARTESIAN_POINT ( 'NONE',  ( 7.250000000000005329, -8.249999999999998224, -26.00000000000001066 ) ) ;
#15460=DIRECTION ( 'NONE',  ( -1.000000000000000000, 0.000000000000000000, 0.000000000000000000 ) ) ;
#15466=EDGE_CURVE ( 'NONE', #67361, #41194, #63622, .T. ) ;
#15474=ORIENTED_EDGE ( 'NONE', *, *, #34639, .T. ) ;
#15479=LINE ( 'NONE', #52610, #32257 ) ;
#15482=LINE ( 'NONE', #27125, #15956 ) ;
#15484=DIRECTION ( 'NONE',  ( -0.000000000000000000, -0.000000000000000000, 1.000000000000000000 ) ) ;
#15494=EDGE_LOOP ( 'NONE', ( #62575, #38516, #35904, #47473 ) ) ;
#15501=CARTESIAN_POINT ( 'NONE',  ( -9.690000000000001279, -9.750000000000001776, -7.000000000000000000 ) ) ;
#15512=AXIS2_PLACEMENT_3D ( 'NONE', #57853, #56453, #64913 ) ;
#15523=EDGE_CURVE ( 'NONE', #13194, #65447, #52305, .T. ) ;
#15526=LINE ( 'NONE', #42375, #33214 ) ;
#15537=VERTEX_POINT ( 'NONE', #15179 ) ;
#15538=DIRECTION ( 'NONE',  ( -1.000000000000000000, 0.000000000000000000, 0.000000000000000000 ) ) ;
#15547=LINE ( 'NONE', #48402, #25813 ) ;
#15548=DIRECTION ( 'NONE',  ( -0.000000000000000000, -0.000000000000000000, -1.000000000000000000 ) ) ;
#15551=ORIENTED_EDGE ( 'NONE', *, *, #7950, .F. ) ;
#15564=CARTESIAN_POINT ( 'NONE',  ( 4.456444791733522252E-16, 7.450000000000002842, -9.500000000000001776 ) ) ;
#15566=ORIENTED_EDGE ( 'NONE', *, *, #62649, .T. ) ;
#15576=VERTEX_POINT ( 'NONE', #59001 ) ;
#15577=CYLINDRICAL_SURFACE ( 'NONE', #18293, 1.000000000000000000 ) ;
#15580=VECTOR ( 'NONE', #52204, 1000.000000000000000 ) ;
#15581=CARTESIAN_POINT ( 'NONE',  ( -7.450000000000001954, 7.250000000000000000, -11.00000000000000000 ) ) ;
#15595=CARTESIAN_POINT ( 'NONE',  ( -8.250000000000001776, -7.249999999999998224, -26.00000000000001066 ) ) ;
#15599=ADVANCED_FACE ( 'NONE', ( #69623 ), #11925, .F. ) ;
#15601=VERTEX_POINT ( 'NONE', #32819 ) ;
#15603=CARTESIAN_POINT ( 'NONE',  ( 4.456444791733522252E-16, 7.450000000000002842, -19.50000000000000000 ) ) ;
#15609=FACE_OUTER_BOUND ( 'NONE', #14900, .T. ) ;
#15625=AXIS2_PLACEMENT_3D ( 'NONE', #9708, #30914, #14309 ) ;
#15633=CARTESIAN_POINT ( 'NONE',  ( -7.250000000000000888, 8.250000000000001776, -16.50000000000000000 ) ) ;
#15640=ORIENTED_EDGE ( 'NONE', *, *, #54318, .F. ) ;
#15643=LINE ( 'NONE', #59808, #18416 ) ;
#15671=VERTEX_POINT ( 'NONE', #49442 ) ;
#15678=ORIENTED_EDGE ( 'NONE', *, *, #3927, .F. ) ;
#15704=CARTESIAN_POINT ( 'NONE',  ( -8.250000000000001776, -7.249999999999998224, -16.00000000000000000 ) ) ;
#15721=CARTESIAN_POINT ( 'NONE',  ( 7.250000000000005329, -7.449999999999998401, -8.500000000000000000 ) ) ;
#15724=DIRECTION ( 'NONE',  ( 0.000000000000000000, 0.000000000000000000, 1.000000000000000000 ) ) ;
#15736=CARTESIAN_POINT ( 'NONE',  ( -7.250000000000000888, -8.249999999999998224, -12.00000000000000000 ) ) ;
#15739=VERTEX_POINT ( 'NONE', #33845 ) ;
#15740=AXIS2_PLACEMENT_3D ( 'NONE', #6730, #43180, #65113 ) ;
#15750=CARTESIAN_POINT ( 'NONE',  ( 7.250000000000005329, 7.250000000000000888, -8.500000000000000000 ) ) ;
#15757=CARTESIAN_POINT ( 'NONE',  ( -7.250000000000000000, -7.449999999999998401, -15.00000000000000000 ) ) ;
#15762=EDGE_CURVE ( 'NONE', #28788, #16237, #21146, .T. ) ;
#15785=LINE ( 'NONE', #48316, #1797 ) ;
#15788=DIRECTION ( 'NONE',  ( 0.000000000000000000, 0.000000000000000000, -1.000000000000000000 ) ) ;
#15798=VECTOR ( 'NONE', #56906, 1000.000000000000000 ) ;
#15800=LINE ( 'NONE', #69546, #2619 ) ;
#15807=LINE ( 'NONE', #35974, #53698 ) ;
#15825=DIRECTION ( 'NONE',  ( 0.000000000000000000, 0.000000000000000000, -1.000000000000000000 ) ) ;
#15828=VERTEX_POINT ( 'NONE', #7668 ) ;
#15837=AXIS2_PLACEMENT_3D ( 'NONE', #38078, #28138, #21796 ) ;
#15841=EDGE_CURVE ( 'NONE', #6549, #13178, #8731, .T. ) ;
#15844=CARTESIAN_POINT ( 'NONE',  ( 0.000000000000000000, 0.000000000000000000, -17.00000000000000000 ) ) ;
#15847=ADVANCED_FACE ( 'NONE', ( #52576 ), #42298, .F. ) ;
#15869=DIRECTION ( 'NONE',  ( 0.000000000000000000, 0.000000000000000000, -1.000000000000000000 ) ) ;
#15874=CYLINDRICAL_SURFACE ( 'NONE', #41267, 0.1999999999999987899 ) ;
#15877=AXIS2_PLACEMENT_3D ( 'NONE', #454, #50526, #2082 ) ;
#15886=CARTESIAN_POINT ( 'NONE',  ( -7.250000000000000888, 7.450000000000003730, -19.00000000000000000 ) ) ;
#15887=CARTESIAN_POINT ( 'NONE',  ( 8.250000000000005329, -7.249999999999998224, -24.00000000000000000 ) ) ;
#15889=DIRECTION ( 'NONE',  ( -0.000000000000000000, -1.000000000000000000, -0.000000000000000000 ) ) ;
#15891=DIRECTION ( 'NONE',  ( -5.981805089575196197E-17, -1.000000000000000000, 0.000000000000000000 ) ) ;
#15915=ORIENTED_EDGE ( 'NONE', *, *, #58238, .T. ) ;
#15918=CYLINDRICAL_SURFACE ( 'NONE', #15223, 1.000000000000000000 ) ;
#15927=LINE ( 'NONE', #21577, #29268 ) ;
#15930=EDGE_LOOP ( 'NONE', ( #2293, #52319, #51263, #57573, #45000, #27880, #39664, #12070 ) ) ;
#15934=VERTEX_POINT ( 'NONE', #51868 ) ;
#15943=CARTESIAN_POINT ( 'NONE',  ( 8.250000000000005329, -7.249999999999998224, -21.50000000000000000 ) ) ;
#15949=AXIS2_PLACEMENT_3D ( 'NONE', #49870, #6727, #66813 ) ;
#15950=DIRECTION ( 'NONE',  ( 1.000000000000000000, 0.000000000000000000, 0.000000000000000000 ) ) ;
#15952=EDGE_CURVE ( 'NONE', #39001, #44299, #12133, .T. ) ;
#15956=VECTOR ( 'NONE', #42685, 1000.000000000000000 ) ;
#15961=TOROIDAL_SURFACE ( 'NONE', #20492, 0.06000000000000080963, 0.7500000000000000000 ) ;
#15972=CARTESIAN_POINT ( 'NONE',  ( 7.450000000000006395, 7.250000000000000888, -7.500000000000000000 ) ) ;
#15973=CARTESIAN_POINT ( 'NONE',  ( 8.250000000000005329, -7.249999999999998224, -9.500000000000001776 ) ) ;
#15984=EDGE_CURVE ( 'NONE', #34012, #4795, #63877, .T. ) ;
#15995=VECTOR ( 'NONE', #44882, 1000.000000000000000 ) ;
#15997=FACE_OUTER_BOUND ( 'NONE', #16789, .T. ) ;
#16020=ORIENTED_EDGE ( 'NONE', *, *, #59616, .F. ) ;
#16023=ORIENTED_EDGE ( 'NONE', *, *, #4074, .T. ) ;
#16040=DIRECTION ( 'NONE',  ( 0.000000000000000000, -1.000000000000000000, 0.000000000000000000 ) ) ;
#16042=CARTESIAN_POINT ( 'NONE',  ( 7.250000000000005329, -7.449999999999998401, -9.500000000000001776 ) ) ;
#16043=AXIS2_PLACEMENT_3D ( 'NONE', #61133, #49512, #1081 ) ;
#16049=DIRECTION ( 'NONE',  ( 0.000000000000000000, 0.000000000000000000, -1.000000000000000000 ) ) ;
#16050=DIRECTION ( 'NONE',  ( 1.000000000000000000, 0.000000000000000000, 0.000000000000000000 ) ) ;
#16052=AXIS2_PLACEMENT_3D ( 'NONE', #68073, #13973, #8679 ) ;
#16066=DIRECTION ( 'NONE',  ( 0.000000000000000000, 1.000000000000000000, 0.000000000000000000 ) ) ;
#16068=CYLINDRICAL_SURFACE ( 'NONE', #45747, 1.000000000000000000 ) ;
#16079=DIRECTION ( 'NONE',  ( 0.000000000000000000, 0.000000000000000000, 1.000000000000000000 ) ) ;
#16100=ORIENTED_EDGE ( 'NONE', *, *, #6566, .F. ) ;
#16108=CARTESIAN_POINT ( 'NONE',  ( -7.450000000000001954, 7.250000000000000000, -14.50000000000000000 ) ) ;
#16123=DIRECTION ( 'NONE',  ( 1.000000000000000000, 0.000000000000000000, 0.000000000000000000 ) ) ;
#16136=FACE_OUTER_BOUND ( 'NONE', #11618, .T. ) ;
#16138=CARTESIAN_POINT ( 'NONE',  ( 6.500000000000002665, 6.500000000000000888, 0.000000000000000000 ) ) ;
#16140=LINE ( 'NONE', #21104, #511 ) ;
#16142=EDGE_CURVE ( 'NONE', #23540, #51438, #8759, .T. ) ;
#16144=DIRECTION ( 'NONE',  ( 0.000000000000000000, 0.000000000000000000, 1.000000000000000000 ) ) ;
#16146=CARTESIAN_POINT ( 'NONE',  ( 0.000000000000000000, 0.000000000000000000, -12.50000000000000000 ) ) ;
#16148=CARTESIAN_POINT ( 'NONE',  ( 0.000000000000000000, 8.250000000000001776, -25.00000000000000000 ) ) ;
#16162=DIRECTION ( 'NONE',  ( 0.000000000000000000, 0.000000000000000000, -1.000000000000000000 ) ) ;
#16166=FACE_OUTER_BOUND ( 'NONE', #8999, .T. ) ;
#16176=CARTESIAN_POINT ( 'NONE',  ( -7.450000000000001954, 7.250000000000000000, -9.500000000000001776 ) ) ;
#16178=VECTOR ( 'NONE', #55964, 1000.000000000000000 ) ;
#16209=CYLINDRICAL_SURFACE ( 'NONE', #63361, 1.000000000000000000 ) ;
#16224=EDGE_LOOP ( 'NONE', ( #62614, #15157, #44580, #32994 ) ) ;
#16228=LINE ( 'NONE', #63638, #55368 ) ;
#16237=VERTEX_POINT ( 'NONE', #26578 ) ;
#16238=DIRECTION ( 'NONE',  ( -1.794541526872559352E-16, -1.000000000000000000, 0.000000000000000000 ) ) ;
#16248=EDGE_LOOP ( 'NONE', ( #69647, #64944, #21574, #64996 ) ) ;
#16250=CYLINDRICAL_SURFACE ( 'NONE', #7559, 1.000000000000000000 ) ;
#16252=DIRECTION ( 'NONE',  ( 0.000000000000000000, -0.000000000000000000, 1.000000000000000000 ) ) ;
#16254=DIRECTION ( 'NONE',  ( 0.000000000000000000, 0.000000000000000000, -1.000000000000000000 ) ) ;
#16268=DIRECTION ( 'NONE',  ( 0.000000000000000000, -0.000000000000000000, 1.000000000000000000 ) ) ;
#16270=ORIENTED_EDGE ( 'NONE', *, *, #28975, .T. ) ;
#16271=AXIS2_PLACEMENT_3D ( 'NONE', #10686, #437, #32952 ) ;
#16272=CARTESIAN_POINT ( 'NONE',  ( 7.250000000000005329, -7.449999999999998401, -15.50000000000000000 ) ) ;
#16280=EDGE_LOOP ( 'NONE', ( #38035, #11832, #21035, #61258 ) ) ;
#16286=DIRECTION ( 'NONE',  ( -0.000000000000000000, -0.000000000000000000, -1.000000000000000000 ) ) ;
#16288=CARTESIAN_POINT ( 'NONE',  ( -7.250000000000001776, -7.249999999999998224, -8.500000000000000000 ) ) ;
#16295=ADVANCED_FACE ( 'NONE', ( #41782 ), #3964, .F. ) ;
#16300=VERTEX_POINT ( 'NONE', #14924 ) ;
#16301=CARTESIAN_POINT ( 'NONE',  ( -7.450000000000001954, 7.250000000000000000, -10.00000000000000000 ) ) ;
#16316=CARTESIAN_POINT ( 'NONE',  ( -7.450000000000001954, -7.249999999999998224, -14.50000000000000000 ) ) ;
#16325=VECTOR ( 'NONE', #3563, 1000.000000000000000 ) ;
#16328=PLANE ( 'NONE',  #24223 ) ;
#16330=ORIENTED_EDGE ( 'NONE', *, *, #48959, .T. ) ;
#16332=VERTEX_POINT ( 'NONE', #42830 ) ;
#16338=FACE_OUTER_BOUND ( 'NONE', #42606, .T. ) ;
#16339=CARTESIAN_POINT ( 'NONE',  ( -7.250000000000000888, 7.250000000000001776, -17.00000000000000000 ) ) ;
#16343=ORIENTED_EDGE ( 'NONE', *, *, #57969, .F. ) ;
#16344=DIRECTION ( 'NONE',  ( 0.000000000000000000, 0.000000000000000000, 1.000000000000000000 ) ) ;
#16346=VECTOR ( 'NONE', #25362, 1000.000000000000000 ) ;
#16354=VERTEX_POINT ( 'NONE', #37197 ) ;
#16356=ORIENTED_EDGE ( 'NONE', *, *, #67900, .T. ) ;
#16368=EDGE_LOOP ( 'NONE', ( #62412, #37777, #65324, #17471 ) ) ;
#16377=LINE ( 'NONE', #21336, #46844 ) ;
#16383=ADVANCED_FACE ( 'NONE', ( #46732 ), #48846, .T. ) ;
#16396=EDGE_CURVE ( 'NONE', #40390, #60302, #32921, .T. ) ;
#16429=LINE ( 'NONE', #69471, #1402 ) ;
#16435=VERTEX_POINT ( 'NONE', #59449 ) ;
#16438=LINE ( 'NONE', #38692, #59749 ) ;
#16443=VERTEX_POINT ( 'NONE', #38241 ) ;
#16446=AXIS2_PLACEMENT_3D ( 'NONE', #8214, #41093, #62658 ) ;
#16447=ORIENTED_EDGE ( 'NONE', *, *, #62194, .F. ) ;
#16449=ORIENTED_EDGE ( 'NONE', *, *, #17579, .F. ) ;
#16454=EDGE_CURVE ( 'NONE', #42459, #32586, #49186, .T. ) ;
#16461=EDGE_CURVE ( 'NONE', #42683, #46897, #41072, .T. ) ;
#16466=EDGE_CURVE ( 'NONE', #3957, #67695, #38576, .T. ) ;
#16472=AXIS2_PLACEMENT_3D ( 'NONE', #44632, #39342, #60902 ) ;
#16473=CARTESIAN_POINT ( 'NONE',  ( -7.450000000000001954, 0.000000000000000000, -16.50000000000000000 ) ) ;
#16474=CARTESIAN_POINT ( 'NONE',  ( -8.250000000000001776, 0.000000000000000000, -16.50000000000000000 ) ) ;
#16478=FACE_OUTER_BOUND ( 'NONE', #32337, .T. ) ;
#16487=DIRECTION ( 'NONE',  ( 0.000000000000000000, 0.000000000000000000, 1.000000000000000000 ) ) ;
#16490=FACE_OUTER_BOUND ( 'NONE', #61099, .T. ) ;
#16501=EDGE_CURVE ( 'NONE', #25138, #33710, #55709, .T. ) ;
#16505=AXIS2_PLACEMENT_3D ( 'NONE', #68896, #36007, #25408 ) ;
#16508=LINE ( 'NONE', #244, #8601 ) ;
#16522=DIRECTION ( 'NONE',  ( 1.000000000000000000, 0.000000000000000000, 0.000000000000000000 ) ) ;
#16526=EDGE_LOOP ( 'NONE', ( #25562, #1134, #30132, #60537 ) ) ;
#16533=ORIENTED_EDGE ( 'NONE', *, *, #6896, .F. ) ;
#16535=CARTESIAN_POINT ( 'NONE',  ( 7.450000000000003730, -7.249999999999997335, -14.50000000000000000 ) ) ;
#16539=CARTESIAN_POINT ( 'NONE',  ( 7.250000000000005329, -7.249999999999998224, -23.00000000000000000 ) ) ;
#16542=ORIENTED_EDGE ( 'NONE', *, *, #27632, .T. ) ;
#16545=CIRCLE ( 'NONE', #24461, 1.000000000000000000 ) ;
#16552=VECTOR ( 'NONE', #32894, 1000.000000000000000 ) ;
#16553=EDGE_CURVE ( 'NONE', #23324, #20521, #19617, .T. ) ;
#16556=CIRCLE ( 'NONE', #4096, 1.000000000000000000 ) ;
#16559=CARTESIAN_POINT ( 'NONE',  ( 7.250000000000005329, 8.250000000000001776, -12.50000000000000000 ) ) ;
#16577=AXIS2_PLACEMENT_3D ( 'NONE', #5697, #66108, #21607 ) ;
#16590=LINE ( 'NONE', #23264, #48613 ) ;
#16612=EDGE_LOOP ( 'NONE', ( #46337, #55972, #53731, #12129, #30791, #317, #5263, #10516 ) ) ;
#16615=AXIS2_PLACEMENT_3D ( 'NONE', #10617, #43481, #65075 ) ;
#16622=AXIS2_PLACEMENT_3D ( 'NONE', #52202, #22977, #51510 ) ;
#16625=PLANE ( 'NONE',  #38957 ) ;
#16632=CARTESIAN_POINT ( 'NONE',  ( 8.250000000000005329, 0.000000000000000000, -7.500000000000000000 ) ) ;
#16634=DIRECTION ( 'NONE',  ( -1.000000000000000000, 0.000000000000000000, 0.000000000000000000 ) ) ;
#16636=VERTEX_POINT ( 'NONE', #18731 ) ;
#16639=ORIENTED_EDGE ( 'NONE', *, *, #63248, .T. ) ;
#16640=CARTESIAN_POINT ( 'NONE',  ( -7.250000000000000000, -7.449999999999998401, -16.50000000000000000 ) ) ;
#16644=ORIENTED_EDGE ( 'NONE', *, *, #36231, .F. ) ;
#16655=DIRECTION ( 'NONE',  ( -1.000000000000000000, 0.000000000000000000, 0.000000000000000000 ) ) ;
#16657=CARTESIAN_POINT ( 'NONE',  ( 9.689999999999999503, -10.50000000000000178, -4.250000000000000000 ) ) ;
#16659=VECTOR ( 'NONE', #39484, 1000.000000000000000 ) ;
#16664=ORIENTED_EDGE ( 'NONE', *, *, #29456, .T. ) ;
#16665=CIRCLE ( 'NONE', #11049, 1.000000000000000000 ) ;
#16672=VECTOR ( 'NONE', #38722, 1000.000000000000000 ) ;
#16680=DIRECTION ( 'NONE',  ( 0.000000000000000000, 0.000000000000000000, 1.000000000000000000 ) ) ;
#16681=CARTESIAN_POINT ( 'NONE',  ( 7.450000000000003730, -7.249999999999997335, -15.50000000000000000 ) ) ;
#16683=ORIENTED_EDGE ( 'NONE', *, *, #41042, .F. ) ;
#16684=FACE_OUTER_BOUND ( 'NONE', #8515, .T. ) ;
#16691=DIRECTION ( 'NONE',  ( 0.000000000000000000, -1.000000000000000000, 0.000000000000000000 ) ) ;
#16692=VERTEX_POINT ( 'NONE', #53376 ) ;
#16695=ORIENTED_EDGE ( 'NONE', *, *, #1685, .T. ) ;
#16700=AXIS2_PLACEMENT_3D ( 'NONE', #42917, #37280, #64498 ) ;
#16701=ADVANCED_FACE ( 'NONE', ( #31109 ), #62921, .T. ) ;
#16705=DIRECTION ( 'NONE',  ( -0.000000000000000000, 0.000000000000000000, -1.000000000000000000 ) ) ;
#16717=ORIENTED_EDGE ( 'NONE', *, *, #56385, .F. ) ;
#16718=VERTEX_POINT ( 'NONE', #31466 ) ;
#16725=DIRECTION ( 'NONE',  ( -1.000000000000000000, 0.000000000000000000, 0.000000000000000000 ) ) ;
#16741=DIRECTION ( 'NONE',  ( 1.000000000000000000, 0.000000000000000000, 0.000000000000000000 ) ) ;
#16749=AXIS2_PLACEMENT_3D ( 'NONE', #57703, #30834, #3968 ) ;
#16755=AXIS2_PLACEMENT_3D ( 'NONE', #39523, #66746, #61084 ) ;
#16756=ORIENTED_EDGE ( 'NONE', *, *, #34652, .F. ) ;
#16757=CARTESIAN_POINT ( 'NONE',  ( 7.250000000000005329, -7.249999999999998224, -22.50000000000000000 ) ) ;
#16762=CARTESIAN_POINT ( 'NONE',  ( -7.450000000000001954, 7.250000000000000000, -20.00000000000000000 ) ) ;
#16766=CARTESIAN_POINT ( 'NONE',  ( -7.250000000000000888, 7.450000000000003730, -18.50000000000000000 ) ) ;
#16770=VERTEX_POINT ( 'NONE', #58675 ) ;
#16771=CARTESIAN_POINT ( 'NONE',  ( 10.50000000000000178, 9.690000000000001279, -5.000000000000000000 ) ) ;
#16779=CARTESIAN_POINT ( 'NONE',  ( -7.250000000000000888, 8.250000000000001776, -25.50000000000000355 ) ) ;
#16783=EDGE_CURVE ( 'NONE', #62655, #33710, #25444, .T. ) ;
#16784=DIRECTION ( 'NONE',  ( 0.000000000000000000, 0.000000000000000000, -1.000000000000000000 ) ) ;
#16785=DIRECTION ( 'NONE',  ( 1.000000000000000000, 0.000000000000000000, 0.000000000000000000 ) ) ;
#16788=EDGE_LOOP ( 'NONE', ( #41806, #49507, #55560, #4216 ) ) ;
#16789=EDGE_LOOP ( 'NONE', ( #68367, #34776, #51288, #20697 ) ) ;
#16793=DIRECTION ( 'NONE',  ( 1.000000000000000000, 0.000000000000000000, 0.000000000000000000 ) ) ;
#16799=VERTEX_POINT ( 'NONE', #49093 ) ;
#16800=CIRCLE ( 'NONE', #39385, 1.000000000000000000 ) ;
#16802=DIRECTION ( 'NONE',  ( -0.000000000000000000, 0.000000000000000000, -1.000000000000000000 ) ) ;
#16810=DIRECTION ( 'NONE',  ( 0.000000000000000000, 0.000000000000000000, -1.000000000000000000 ) ) ;
#16817=DIRECTION ( 'NONE',  ( 0.000000000000000000, 0.000000000000000000, -1.000000000000000000 ) ) ;
#16819=CARTESIAN_POINT ( 'NONE',  ( 9.689999999999999503, -9.750000000000001776, -4.250000000000000000 ) ) ;
#16826=CARTESIAN_POINT ( 'NONE',  ( 7.250000000000005329, -7.249999999999998224, -9.000000000000001776 ) ) ;
#16843=FACE_OUTER_BOUND ( 'NONE', #67646, .T. ) ;
#16844=DIRECTION ( 'NONE',  ( 0.000000000000000000, 0.000000000000000000, 1.000000000000000000 ) ) ;
#16849=CARTESIAN_POINT ( 'NONE',  ( 7.250000000000005329, -7.449999999999998401, -7.500000000000000000 ) ) ;
#16873=CIRCLE ( 'NONE', #2171, 1.000000000000000000 ) ;
#16880=FACE_OUTER_BOUND ( 'NONE', #55484, .T. ) ;
#16881=CARTESIAN_POINT ( 'NONE',  ( 7.450000000000006395, 7.250000000000000888, -13.50000000000000178 ) ) ;
#16882=ORIENTED_EDGE ( 'NONE', *, *, #41933, .F. ) ;
#16884=DIRECTION ( 'NONE',  ( -0.000000000000000000, -0.000000000000000000, 1.000000000000000000 ) ) ;
#16898=DIRECTION ( 'NONE',  ( 0.000000000000000000, 0.000000000000000000, 1.000000000000000000 ) ) ;
#16930=CARTESIAN_POINT ( 'NONE',  ( -7.450000000000001954, 0.000000000000000000, -17.00000000000000000 ) ) ;
#16931=EDGE_LOOP ( 'NONE', ( #10839, #38297, #41422, #65642, #34575, #10043, #21661, #46452 ) ) ;
#16932=CARTESIAN_POINT ( 'NONE',  ( 7.250000000000005329, 7.250000000000000888, -9.500000000000001776 ) ) ;
#16933=AXIS2_PLACEMENT_3D ( 'NONE', #46171, #24960, #40866 ) ;
#16942=ORIENTED_EDGE ( 'NONE', *, *, #50905, .F. ) ;
#16955=ORIENTED_EDGE ( 'NONE', *, *, #23480, .T. ) ;
#16960=CARTESIAN_POINT ( 'NONE',  ( -8.250000000000000000, 7.250000000000001776, -15.00000000000000000 ) ) ;
#16961=EDGE_LOOP ( 'NONE', ( #64947, #40514, #69053, #4565 ) ) ;
#16964=ORIENTED_EDGE ( 'NONE', *, *, #9938, .F. ) ;
#16966=AXIS2_PLACEMENT_3D ( 'NONE', #55787, #62842, #7333 ) ;
#16975=ORIENTED_EDGE ( 'NONE', *, *, #67861, .T. ) ;
#16981=DIRECTION ( 'NONE',  ( 1.000000000000000000, 0.000000000000000000, 0.000000000000000000 ) ) ;
#16991=LINE ( 'NONE', #11664, #778 ) ;
#16992=EDGE_CURVE ( 'NONE', #28094, #26202, #39174, .T. ) ;
#16993=CARTESIAN_POINT ( 'NONE',  ( -7.250000000000000888, 8.250000000000001776, -26.00000000000001066 ) ) ;
#16997=CYLINDRICAL_SURFACE ( 'NONE', #46206, 1.000000000000000000 ) ;
#17006=DIRECTION ( 'NONE',  ( -1.000000000000000000, 2.602085213965213008E-15, 0.000000000000000000 ) ) ;
#17011=DIRECTION ( 'NONE',  ( 0.000000000000000000, 0.000000000000000000, -1.000000000000000000 ) ) ;
#17015=FACE_OUTER_BOUND ( 'NONE', #37323, .T. ) ;
#17018=VERTEX_POINT ( 'NONE', #13339 ) ;
#17019=ORIENTED_EDGE ( 'NONE', *, *, #17731, .T. ) ;
#17023=CARTESIAN_POINT ( 'NONE',  ( 8.250000000000005329, -8.249999999999998224, -26.00000000000001066 ) ) ;
#17024=CARTESIAN_POINT ( 'NONE',  ( -7.250000000000000888, 7.450000000000003730, -10.50000000000000000 ) ) ;
#17037=FACE_OUTER_BOUND ( 'NONE', #636, .T. ) ;
#17038=DIRECTION ( 'NONE',  ( -0.000000000000000000, -0.000000000000000000, 1.000000000000000000 ) ) ;
#17039=DIRECTION ( 'NONE',  ( 0.000000000000000000, 0.000000000000000000, -1.000000000000000000 ) ) ;
#17043=ORIENTED_EDGE ( 'NONE', *, *, #5237, .F. ) ;
#17062=VECTOR ( 'NONE', #46491, 1000.000000000000000 ) ;
#17064=CARTESIAN_POINT ( 'NONE',  ( 7.250000000000004441, 7.450000000000001954, -22.00000000000000000 ) ) ;
#17076=ORIENTED_EDGE ( 'NONE', *, *, #66513, .F. ) ;
#17089=FACE_OUTER_BOUND ( 'NONE', #46155, .T. ) ;
#17093=DIRECTION ( 'NONE',  ( -1.000000000000000000, 0.000000000000000000, 0.000000000000000000 ) ) ;
#17095=CARTESIAN_POINT ( 'NONE',  ( -7.450000000000001954, 0.000000000000000000, -10.50000000000000000 ) ) ;
#17102=CARTESIAN_POINT ( 'NONE',  ( -7.450000000000001954, 0.000000000000000000, -23.50000000000000000 ) ) ;
#17113=ADVANCED_FACE ( 'NONE', ( #58231 ), #62834, .T. ) ;
#17114=VECTOR ( 'NONE', #18449, 1000.000000000000000 ) ;
#17118=ORIENTED_EDGE ( 'NONE', *, *, #4600, .F. ) ;
#17131=VERTEX_POINT ( 'NONE', #40905 ) ;
#17139=LINE ( 'NONE', #42970, #23198 ) ;
#17140=VERTEX_POINT ( 'NONE', #31722 ) ;
#17146=CARTESIAN_POINT ( 'NONE',  ( 0.000000000000000000, 0.000000000000000000, -20.00000000000000000 ) ) ;
#17153=DIRECTION ( 'NONE',  ( -1.000000000000000000, 0.000000000000000000, 0.000000000000000000 ) ) ;
#17156=LINE ( 'NONE', #6888, #16672 ) ;
#17158=EDGE_CURVE ( 'NONE', #25138, #18463, #58590, .T. ) ;
#17166=CARTESIAN_POINT ( 'NONE',  ( -8.250000000000001776, -8.249999999999998224, -26.00000000000001066 ) ) ;
#17177=EDGE_CURVE ( 'NONE', #39723, #29071, #64867, .T. ) ;
#17189=PLANE ( 'NONE',  #20531 ) ;
#17209=ADVANCED_FACE ( 'NONE', ( #49021 ), #65293, .F. ) ;
#17210=ORIENTED_EDGE ( 'NONE', *, *, #51159, .F. ) ;
#17213=LINE ( 'NONE', #16535, #57918 ) ;
#17216=CARTESIAN_POINT ( 'NONE',  ( 7.450000000000006395, 7.250000000000000888, -14.50000000000000000 ) ) ;
#17217=ORIENTED_EDGE ( 'NONE', *, *, #53069, .T. ) ;
#17221=PLANE ( 'NONE',  #41523 ) ;
#17252=VERTEX_POINT ( 'NONE', #11173 ) ;
#17258=EDGE_CURVE ( 'NONE', #26986, #39386, #32747, .T. ) ;
#17263=AXIS2_PLACEMENT_3D ( 'NONE', #22218, #43780, #59345 ) ;
#17265=EDGE_CURVE ( 'NONE', #17842, #60006, #16140, .T. ) ;
#17266=DIRECTION ( 'NONE',  ( -0.000000000000000000, -0.000000000000000000, 1.000000000000000000 ) ) ;
#17276=ORIENTED_EDGE ( 'NONE', *, *, #4065, .T. ) ;
#17283=DIRECTION ( 'NONE',  ( 0.000000000000000000, 1.000000000000000000, 0.000000000000000000 ) ) ;
#17284=CARTESIAN_POINT ( 'NONE',  ( 8.750000000000005329, 7.250000000000000888, -30.00000000000001066 ) ) ;
#17294=DIRECTION ( 'NONE',  ( -5.981805089575196197E-17, -1.000000000000000000, 0.000000000000000000 ) ) ;
#17298=VERTEX_POINT ( 'NONE', #59275 ) ;
#17301=CARTESIAN_POINT ( 'NONE',  ( 0.000000000000000000, -8.749999999999998224, -30.00000000000001066 ) ) ;
#17303=CARTESIAN_POINT ( 'NONE',  ( 8.250000000000005329, 7.250000000000000888, -26.00000000000001066 ) ) ;
#17305=LINE ( 'NONE', #60437, #7109 ) ;
#17309=CARTESIAN_POINT ( 'NONE',  ( 4.456444791733522252E-16, 7.450000000000002842, -13.50000000000000178 ) ) ;
#17333=ORIENTED_EDGE ( 'NONE', *, *, #2864, .F. ) ;
#17343=DIRECTION ( 'NONE',  ( 1.000000000000000000, 0.000000000000000000, 0.000000000000000000 ) ) ;
#17344=CARTESIAN_POINT ( 'NONE',  ( -8.250000000000001776, -8.249999999999998224, -26.00000000000001066 ) ) ;
#17347=ORIENTED_EDGE ( 'NONE', *, *, #2078, .T. ) ;
#17351=DIRECTION ( 'NONE',  ( -0.000000000000000000, -0.000000000000000000, 1.000000000000000000 ) ) ;
#17357=AXIS2_PLACEMENT_3D ( 'NONE', #26257, #36506, #3640 ) ;
#17358=VECTOR ( 'NONE', #25500, 1000.000000000000000 ) ;
#17360=EDGE_LOOP ( 'NONE', ( #14713, #64245, #4395, #16975, #66475, #2670, #10453, #48347 ) ) ;
#17361=VERTEX_POINT ( 'NONE', #35165 ) ;
#17362=CARTESIAN_POINT ( 'NONE',  ( -8.689999999999999503, -8.750000000000000000, -5.000000000000000000 ) ) ;
#17369=CARTESIAN_POINT ( 'NONE',  ( 7.450000000000003730, -7.249999999999997335, -20.50000000000000000 ) ) ;
#17372=CARTESIAN_POINT ( 'NONE',  ( 0.000000000000000000, -8.249999999999998224, -13.00000000000000178 ) ) ;
#17382=DIRECTION ( 'NONE',  ( -1.000000000000000000, 0.000000000000000000, 0.000000000000000000 ) ) ;
#17385=ORIENTED_EDGE ( 'NONE', *, *, #37772, .F. ) ;
#17386=DIRECTION ( 'NONE',  ( -1.000000000000000000, 0.000000000000000000, -0.000000000000000000 ) ) ;
#17387=DIRECTION ( 'NONE',  ( -0.000000000000000000, -0.000000000000000000, 1.000000000000000000 ) ) ;
#17394=EDGE_CURVE ( 'NONE', #17018, #68958, #65953, .T. ) ;
#17405=EDGE_CURVE ( 'NONE', #46897, #52634, #33781, .T. ) ;
#17407=EDGE_CURVE ( 'NONE', #44960, #17538, #23172, .T. ) ;
#17411=ADVANCED_FACE ( 'NONE', ( #44727 ), #12894, .F. ) ;
#17414=DIRECTION ( 'NONE',  ( 8.951101527228106186E-17, 1.000000000000000000, -0.000000000000000000 ) ) ;
#17428=DIRECTION ( 'NONE',  ( 0.000000000000000000, -1.000000000000000000, -0.000000000000000000 ) ) ;
#17433=DIRECTION ( 'NONE',  ( 0.000000000000000000, 0.000000000000000000, 1.000000000000000000 ) ) ;
#17455=CIRCLE ( 'NONE', #32107, 1.000000000000003553 ) ;
#17462=ORIENTED_EDGE ( 'NONE', *, *, #35862, .F. ) ;
#17465=DIRECTION ( 'NONE',  ( 0.000000000000000000, 0.000000000000000000, 1.000000000000000000 ) ) ;
#17471=ORIENTED_EDGE ( 'NONE', *, *, #5702, .T. ) ;
#17472=AXIS2_PLACEMENT_3D ( 'NONE', #19804, #20171, #30781 ) ;
#17473=LINE ( 'NONE', #39039, #14747 ) ;
#17480=ORIENTED_EDGE ( 'NONE', *, *, #14197, .F. ) ;
#17483=FACE_OUTER_BOUND ( 'NONE', #6605, .T. ) ;
#17489=FACE_OUTER_BOUND ( 'NONE', #53387, .T. ) ;
#17492=DIRECTION ( 'NONE',  ( 0.000000000000000000, 0.000000000000000000, 1.000000000000000000 ) ) ;
#17506=VERTEX_POINT ( 'NONE', #36226 ) ;
#17512=EDGE_CURVE ( 'NONE', #58882, #5244, #10697, .T. ) ;
#17525=DIRECTION ( 'NONE',  ( -0.000000000000000000, -0.000000000000000000, 1.000000000000000000 ) ) ;
#17526=CARTESIAN_POINT ( 'NONE',  ( 7.250000000000005329, -7.249999999999998224, -18.00000000000000000 ) ) ;
#17528=DIRECTION ( 'NONE',  ( 0.000000000000000000, 0.000000000000000000, 1.000000000000000000 ) ) ;
#17529=PLANE ( 'NONE',  #34527 ) ;
#17535=VECTOR ( 'NONE', #62217, 1000.000000000000000 ) ;
#17538=VERTEX_POINT ( 'NONE', #29872 ) ;
#17558=CARTESIAN_POINT ( 'NONE',  ( -7.450000000000001954, 7.250000000000000000, -14.00000000000000000 ) ) ;
#17567=DIRECTION ( 'NONE',  ( 0.000000000000000000, 1.000000000000000000, 0.000000000000000000 ) ) ;
#17577=DIRECTION ( 'NONE',  ( 1.000000000000000000, 0.000000000000000000, 0.000000000000000000 ) ) ;
#17578=LINE ( 'NONE', #38803, #22836 ) ;
#17579=EDGE_CURVE ( 'NONE', #33956, #11076, #31988, .T. ) ;
#17584=AXIS2_PLACEMENT_3D ( 'NONE', #9448, #31012, #64586 ) ;
#17592=DIRECTION ( 'NONE',  ( -0.000000000000000000, -0.000000000000000000, -1.000000000000000000 ) ) ;
#17594=AXIS2_PLACEMENT_3D ( 'NONE', #17166, #11165, #39419 ) ;
#17595=AXIS2_PLACEMENT_3D ( 'NONE', #13474, #17387, #23040 ) ;
#17612=CARTESIAN_POINT ( 'NONE',  ( 0.000000000000000000, -8.249999999999998224, -9.500000000000001776 ) ) ;
#17622=ORIENTED_EDGE ( 'NONE', *, *, #9158, .F. ) ;
#17629=CARTESIAN_POINT ( 'NONE',  ( -7.450000000000001954, 7.250000000000000000, -12.50000000000000000 ) ) ;
#17631=AXIS2_PLACEMENT_3D ( 'NONE', #7840, #66889, #66213 ) ;
#17633=FACE_OUTER_BOUND ( 'NONE', #19547, .T. ) ;
#17639=VECTOR ( 'NONE', #58874, 1000.000000000000000 ) ;
#17654=AXIS2_PLACEMENT_3D ( 'NONE', #27231, #26184, #21235 ) ;
#17658=EDGE_CURVE ( 'NONE', #44658, #4958, #27715, .T. ) ;
#17659=ADVANCED_FACE ( 'NONE', ( #42584 ), #16068, .T. ) ;
#17667=EDGE_CURVE ( 'NONE', #63525, #23322, #869, .T. ) ;
#17671=DIRECTION ( 'NONE',  ( 1.000000000000000000, 0.000000000000000000, 0.000000000000000000 ) ) ;
#17672=ORIENTED_EDGE ( 'NONE', *, *, #34487, .T. ) ;
#17677=DIRECTION ( 'NONE',  ( 0.000000000000000000, 0.000000000000000000, 1.000000000000000000 ) ) ;
#17680=EDGE_CURVE ( 'NONE', #8070, #17836, #15290, .T. ) ;
#17690=DIRECTION ( 'NONE',  ( 0.000000000000000000, 1.000000000000000000, 0.000000000000000000 ) ) ;
#17712=CARTESIAN_POINT ( 'NONE',  ( 8.250000000000005329, 7.250000000000000888, -15.50000000000000000 ) ) ;
#17716=LINE ( 'NONE', #30679, #32959 ) ;
#17718=ORIENTED_EDGE ( 'NONE', *, *, #55206, .T. ) ;
#17724=LINE ( 'NONE', #8137, #18456 ) ;
#17727=CYLINDRICAL_SURFACE ( 'NONE', #62729, 1.000000000000000000 ) ;
#17731=EDGE_CURVE ( 'NONE', #43147, #2261, #50248, .T. ) ;
#17740=ORIENTED_EDGE ( 'NONE', *, *, #31428, .T. ) ;
#17752=VECTOR ( 'NONE', #24495, 1000.000000000000000 ) ;
#17755=DIRECTION ( 'NONE',  ( -0.000000000000000000, -0.000000000000000000, 1.000000000000000000 ) ) ;
#17765=DIRECTION ( 'NONE',  ( 0.000000000000000000, 0.000000000000000000, -1.000000000000000000 ) ) ;
#17768=ORIENTED_EDGE ( 'NONE', *, *, #54033, .T. ) ;
#17773=CIRCLE ( 'NONE', #33568, 0.1999999999999996503 ) ;
#17786=ORIENTED_EDGE ( 'NONE', *, *, #49275, .F. ) ;
#17792=VECTOR ( 'NONE', #50093, 1000.000000000000000 ) ;
#17795=FACE_OUTER_BOUND ( 'NONE', #22051, .T. ) ;
#17799=ORIENTED_EDGE ( 'NONE', *, *, #13141, .F. ) ;
#17802=CIRCLE ( 'NONE', #3120, 0.1999999999999996503 ) ;
#17815=ORIENTED_EDGE ( 'NONE', *, *, #32220, .T. ) ;
#17817=ORIENTED_EDGE ( 'NONE', *, *, #20728, .T. ) ;
#17823=DIRECTION ( 'NONE',  ( 0.000000000000000000, 0.000000000000000000, 1.000000000000000000 ) ) ;
#17827=VERTEX_POINT ( 'NONE', #3629 ) ;
#17830=ORIENTED_EDGE ( 'NONE', *, *, #17680, .F. ) ;
#17831=ORIENTED_EDGE ( 'NONE', *, *, #65904, .F. ) ;
#17836=VERTEX_POINT ( 'NONE', #57005 ) ;
#17837=CARTESIAN_POINT ( 'NONE',  ( 7.250000000000005329, 8.250000000000001776, -13.00000000000000178 ) ) ;
#17842=VERTEX_POINT ( 'NONE', #41800 ) ;
#17845=DIRECTION ( 'NONE',  ( -1.000000000000000000, 0.000000000000000000, 0.000000000000000000 ) ) ;
#17846=VERTEX_POINT ( 'NONE', #13527 ) ;
#17852=ORIENTED_EDGE ( 'NONE', *, *, #51681, .T. ) ;
#17853=EDGE_CURVE ( 'NONE', #69858, #45036, #19527, .T. ) ;
#17854=DIRECTION ( 'NONE',  ( 0.000000000000000000, 0.000000000000000000, -1.000000000000000000 ) ) ;
#17858=CARTESIAN_POINT ( 'NONE',  ( -7.250000000000000888, 7.250000000000001776, -15.00000000000000000 ) ) ;
#17861=CARTESIAN_POINT ( 'NONE',  ( 0.000000000000000000, 8.250000000000001776, -13.50000000000000178 ) ) ;
#17866=VERTEX_POINT ( 'NONE', #2923 ) ;
#17871=CARTESIAN_POINT ( 'NONE',  ( 7.250000000000005329, 7.250000000000000888, -7.500000000000000000 ) ) ;
#17873=CARTESIAN_POINT ( 'NONE',  ( 4.456444791733522252E-16, 7.450000000000002842, -24.00000000000000000 ) ) ;
#17879=VERTEX_POINT ( 'NONE', #57364 ) ;
#17882=CARTESIAN_POINT ( 'NONE',  ( 7.250000000000005329, -7.249999999999998224, -26.00000000000001066 ) ) ;
#17897=ORIENTED_EDGE ( 'NONE', *, *, #34988, .T. ) ;
#17898=ORIENTED_EDGE ( 'NONE', *, *, #38792, .T. ) ;
#17904=ORIENTED_EDGE ( 'NONE', *, *, #45486, .F. ) ;
#17907=ORIENTED_EDGE ( 'NONE', *, *, #42443, .F. ) ;
#17912=VERTEX_POINT ( 'NONE', #20232 ) ;
#17917=CYLINDRICAL_SURFACE ( 'NONE', #13246, 0.2000000000000005107 ) ;
#17945=CARTESIAN_POINT ( 'NONE',  ( -7.250000000000001776, -7.249999999999998224, -22.50000000000000000 ) ) ;
#17949=DIRECTION ( 'NONE',  ( -0.000000000000000000, -0.000000000000000000, 1.000000000000000000 ) ) ;
#17952=AXIS2_PLACEMENT_3D ( 'NONE', #52214, #3777, #20045 ) ;
#17958=DIRECTION ( 'NONE',  ( -1.000000000000000000, 0.000000000000000000, 0.000000000000000000 ) ) ;
#17963=CARTESIAN_POINT ( 'NONE',  ( 7.450000000000006395, 7.250000000000000888, -18.50000000000000000 ) ) ;
#17966=ADVANCED_FACE ( 'NONE', ( #31218 ), #56663, .T. ) ;
#17976=EDGE_LOOP ( 'NONE', ( #9993, #35905, #61168, #5704 ) ) ;
#17991=VERTEX_POINT ( 'NONE', #28227 ) ;
#17998=CARTESIAN_POINT ( 'NONE',  ( 0.000000000000000000, 0.000000000000000000, -19.50000000000000000 ) ) ;
#18001=CIRCLE ( 'NONE', #28160, 1.000000000000000000 ) ;
#18004=CARTESIAN_POINT ( 'NONE',  ( -6.500000000000002665, -6.500000000000002665, -1.000000000000000000 ) ) ;
#18009=AXIS2_PLACEMENT_3D ( 'NONE', #39403, #17845, #2279 ) ;
#18036=VECTOR ( 'NONE', #25005, 1000.000000000000000 ) ;
#18045=CIRCLE ( 'NONE', #42903, 1.000000000000000000 ) ;
#18049=ORIENTED_EDGE ( 'NONE', *, *, #21872, .F. ) ;
#18058=DIRECTION ( 'NONE',  ( -1.000000000000000000, -0.000000000000000000, -0.000000000000000000 ) ) ;
#18073=VERTEX_POINT ( 'NONE', #49109 ) ;
#18076=CARTESIAN_POINT ( 'NONE',  ( 7.450000000000004619, -1.336933437520057563E-15, -17.50000000000000000 ) ) ;
#18079=DIRECTION ( 'NONE',  ( -5.981805089575196197E-17, -1.000000000000000000, 0.000000000000000000 ) ) ;
#18080=FACE_OUTER_BOUND ( 'NONE', #22361, .T. ) ;
#18084=DIRECTION ( 'NONE',  ( -1.000000000000000000, 0.000000000000000000, 0.000000000000000000 ) ) ;
#18087=ORIENTED_EDGE ( 'NONE', *, *, #45756, .T. ) ;
#18091=CARTESIAN_POINT ( 'NONE',  ( -7.250000000000000000, -8.749999999999998224, -26.00000000000001066 ) ) ;
#18093=LINE ( 'NONE', #39660, #35775 ) ;
#18096=CARTESIAN_POINT ( 'NONE',  ( -7.450000000000001954, -7.249999999999998224, -13.50000000000000178 ) ) ;
#18103=ORIENTED_EDGE ( 'NONE', *, *, #66920, .T. ) ;
#18106=DIRECTION ( 'NONE',  ( -1.000000000000000000, 2.602085213965213008E-15, 0.000000000000000000 ) ) ;
#18107=EDGE_CURVE ( 'NONE', #26426, #57275, #33870, .T. ) ;
#18114=ORIENTED_EDGE ( 'NONE', *, *, #61325, .T. ) ;
#18117=FILL_AREA_STYLE ('',( #44293 ) ) ;
#18118=DIRECTION ( 'NONE',  ( -1.000000000000000000, 0.000000000000000000, -0.000000000000000000 ) ) ;
#18121=CARTESIAN_POINT ( 'NONE',  ( 7.250000000000005329, -7.249999999999998224, -26.00000000000001066 ) ) ;
#18133=CARTESIAN_POINT ( 'NONE',  ( -7.250000000000001776, -7.249999999999998224, -19.50000000000000000 ) ) ;
#18134=VERTEX_POINT ( 'NONE', #12638 ) ;
#18140=DIRECTION ( 'NONE',  ( 0.000000000000000000, 0.000000000000000000, 1.000000000000000000 ) ) ;
#18146=LINE ( 'NONE', #66931, #69142 ) ;
#18155=AXIS2_PLACEMENT_3D ( 'NONE', #39017, #37647, #43640 ) ;
#18163=CARTESIAN_POINT ( 'NONE',  ( -7.250000000000000888, 7.250000000000001776, -16.00000000000000000 ) ) ;
#18168=CYLINDRICAL_SURFACE ( 'NONE', #17, 0.2000000000000005107 ) ;
#18171=FACE_OUTER_BOUND ( 'NONE', #22506, .T. ) ;
#18172=CARTESIAN_POINT ( 'NONE',  ( -9.689999999999999503, -10.50000000000000178, -4.250000000000000000 ) ) ;
#18178=CARTESIAN_POINT ( 'NONE',  ( 0.000000000000000000, 8.250000000000001776, -20.00000000000000000 ) ) ;
#18179=CARTESIAN_POINT ( 'NONE',  ( -7.250000000000000888, -8.249999999999998224, -26.00000000000001066 ) ) ;
#18204=CARTESIAN_POINT ( 'NONE',  ( -7.450000000000001954, 0.000000000000000000, -9.000000000000001776 ) ) ;
#18207=DIRECTION ( 'NONE',  ( 0.000000000000000000, 0.000000000000000000, -1.000000000000000000 ) ) ;
#18212=ORIENTED_EDGE ( 'NONE', *, *, #4899, .F. ) ;
#18213=CARTESIAN_POINT ( 'NONE',  ( 7.250000000000005329, -7.449999999999998401, -22.50000000000000000 ) ) ;
#18229=EDGE_LOOP ( 'NONE', ( #24883, #39404, #47727, #4340 ) ) ;
#18246=DIRECTION ( 'NONE',  ( -1.000000000000000000, 0.000000000000000000, 0.000000000000000000 ) ) ;
#18249=DIRECTION ( 'NONE',  ( -1.794541526872559352E-16, -1.000000000000000000, 0.000000000000000000 ) ) ;
#18259=DIRECTION ( 'NONE',  ( 1.000000000000000000, 0.000000000000000000, 0.000000000000000000 ) ) ;
#18262=ORIENTED_EDGE ( 'NONE', *, *, #53131, .T. ) ;
#18264=DIRECTION ( 'NONE',  ( 1.000000000000000000, 0.000000000000000000, 0.000000000000000000 ) ) ;
#18281=AXIS2_PLACEMENT_3D ( 'NONE', #3380, #41198, #65148 ) ;
#18283=ORIENTED_EDGE ( 'NONE', *, *, #8149, .F. ) ;
#18291=DIRECTION ( 'NONE',  ( 1.000000000000000000, -5.981805089575194965E-17, 0.000000000000000000 ) ) ;
#18293=AXIS2_PLACEMENT_3D ( 'NONE', #37477, #4611, #47729 ) ;
#18294=ORIENTED_EDGE ( 'NONE', *, *, #23883, .F. ) ;
#18296=VECTOR ( 'NONE', #37122, 1000.000000000000000 ) ;
#18304=VERTEX_POINT ( 'NONE', #63557 ) ;
#18310=CARTESIAN_POINT ( 'NONE',  ( -7.450000000000001954, 0.000000000000000000, -23.00000000000000000 ) ) ;
#18320=ORIENTED_EDGE ( 'NONE', *, *, #68938, .T. ) ;
#18328=DIRECTION ( 'NONE',  ( -0.000000000000000000, -0.000000000000000000, 1.000000000000000000 ) ) ;
#18330=VERTEX_POINT ( 'NONE', #3454 ) ;
#18335=ORIENTED_EDGE ( 'NONE', *, *, #47040, .F. ) ;
#18337=DIRECTION ( 'NONE',  ( 0.000000000000000000, 0.000000000000000000, -1.000000000000000000 ) ) ;
#18340=AXIS2_PLACEMENT_3D ( 'NONE', #40417, #33378, #49972 ) ;
#18343=ORIENTED_EDGE ( 'NONE', *, *, #61674, .T. ) ;
#18361=VECTOR ( 'NONE', #63325, 1000.000000000000000 ) ;
#18363=EDGE_CURVE ( 'NONE', #43564, #36247, #15807, .T. ) ;
#18381=DIRECTION ( 'NONE',  ( 0.000000000000000000, 0.000000000000000000, -1.000000000000000000 ) ) ;
#18395=FACE_OUTER_BOUND ( 'NONE', #35451, .T. ) ;
#18402=LINE ( 'NONE', #45277, #23943 ) ;
#18410=DIRECTION ( 'NONE',  ( 0.000000000000000000, -0.000000000000000000, 1.000000000000000000 ) ) ;
#18416=VECTOR ( 'NONE', #59113, 1000.000000000000000 ) ;
#18424=DIRECTION ( 'NONE',  ( -1.000000000000000000, 0.000000000000000000, 0.000000000000000000 ) ) ;
#18444=AXIS2_PLACEMENT_3D ( 'NONE', #67027, #62063, #56417 ) ;
#18446=ADVANCED_FACE ( 'NONE', ( #4853, #26419 ), #17529, .T. ) ;
#18449=DIRECTION ( 'NONE',  ( 1.000000000000000000, -0.000000000000000000, 0.000000000000000000 ) ) ;
#18456=VECTOR ( 'NONE', #29359, 1000.000000000000000 ) ;
#18463=VERTEX_POINT ( 'NONE', #6590 ) ;
#18464=CARTESIAN_POINT ( 'NONE',  ( 7.250000000000005329, 7.250000000000000888, -14.00000000000000000 ) ) ;
#18467=DIRECTION ( 'NONE',  ( -0.000000000000000000, -0.000000000000000000, 1.000000000000000000 ) ) ;
#18468=CARTESIAN_POINT ( 'NONE',  ( -7.250000000000001776, -7.249999999999998224, -26.00000000000001066 ) ) ;
#18486=LINE ( 'NONE', #19199, #25133 ) ;
#18494=EDGE_CURVE ( 'NONE', #32668, #69381, #21457, .T. ) ;
#18506=VECTOR ( 'NONE', #12529, 1000.000000000000000 ) ;
#18507=EDGE_CURVE ( 'NONE', #3987, #7623, #68427, .T. ) ;
#18509=ORIENTED_EDGE ( 'NONE', *, *, #35292, .F. ) ;
#18513=EDGE_CURVE ( 'NONE', #30760, #15934, #16508, .T. ) ;
#18519=CARTESIAN_POINT ( 'NONE',  ( 7.450000000000004619, -1.336933437520057563E-15, -7.000000000000000000 ) ) ;
#18529=ADVANCED_FACE ( 'NONE', ( #11525 ), #38088, .F. ) ;
#18533=DIRECTION ( 'NONE',  ( -1.000000000000000000, 0.000000000000000000, 0.000000000000000000 ) ) ;
#18537=ADVANCED_FACE ( 'NONE', ( #45795 ), #61707, .T. ) ;
#18542=CARTESIAN_POINT ( 'NONE',  ( -7.250000000000001776, -7.249999999999998224, -17.50000000000000000 ) ) ;
#18543=CARTESIAN_POINT ( 'NONE',  ( -7.250000000000000888, 8.250000000000001776, -16.00000000000000000 ) ) ;
#18549=LINE ( 'NONE', #18204, #42445 ) ;
#18551=AXIS2_PLACEMENT_3D ( 'NONE', #4152, #53294, #25004 ) ;
#18553=ORIENTED_EDGE ( 'NONE', *, *, #4771, .T. ) ;
#18555=DIRECTION ( 'NONE',  ( -1.000000000000000000, 2.602085213965213008E-15, 0.000000000000000000 ) ) ;
#18558=DIRECTION ( 'NONE',  ( 0.000000000000000000, 1.000000000000000000, 0.000000000000000000 ) ) ;
#18578=ORIENTED_EDGE ( 'NONE', *, *, #19025, .T. ) ;
#18584=CARTESIAN_POINT ( 'NONE',  ( 7.250000000000004441, 8.750000000000001776, -30.00000000000001066 ) ) ;
#18594=VERTEX_POINT ( 'NONE', #50052 ) ;
#18596=EDGE_CURVE ( 'NONE', #37823, #26265, #22149, .T. ) ;
#18601=CIRCLE ( 'NONE', #40040, 0.2000000000000005107 ) ;
#18611=AXIS2_PLACEMENT_3D ( 'NONE', #7234, #28805, #27782 ) ;
#18613=DIRECTION ( 'NONE',  ( 0.000000000000000000, 0.000000000000000000, 1.000000000000000000 ) ) ;
#18616=EDGE_LOOP ( 'NONE', ( #51591, #24862, #56713, #40796 ) ) ;
#18626=CYLINDRICAL_SURFACE ( 'NONE', #34999, 0.7500000000000006661 ) ;
#18630=DIRECTION ( 'NONE',  ( 0.000000000000000000, 0.000000000000000000, 1.000000000000000000 ) ) ;
#18639=CARTESIAN_POINT ( 'NONE',  ( -7.250000000000000888, 7.250000000000001776, -23.50000000000000000 ) ) ;
#18656=CARTESIAN_POINT ( 'NONE',  ( -10.50000000000000178, 9.690000000000001279, -5.000000000000000000 ) ) ;
#18672=DIRECTION ( 'NONE',  ( 0.000000000000000000, 0.000000000000000000, -1.000000000000000000 ) ) ;
#18678=EDGE_CURVE ( 'NONE', #11380, #65843, #44678, .T. ) ;
#18684=ORIENTED_EDGE ( 'NONE', *, *, #61779, .F. ) ;
#18687=CYLINDRICAL_SURFACE ( 'NONE', #7924, 1.000000000000000000 ) ;
#18696=CARTESIAN_POINT ( 'NONE',  ( 9.690000000000001279, -9.690000000000001279, -4.250000000000000000 ) ) ;
#18702=FACE_OUTER_BOUND ( 'NONE', #46839, .T. ) ;
#18705=ORIENTED_EDGE ( 'NONE', *, *, #67934, .T. ) ;
#18708=CARTESIAN_POINT ( 'NONE',  ( 10.50000000000000178, 9.690000000000001279, -4.250000000000000000 ) ) ;
#18717=VERTEX_POINT ( 'NONE', #57805 ) ;
#18718=CYLINDRICAL_SURFACE ( 'NONE', #44775, 0.1999999999999987899 ) ;
#18722=VERTEX_POINT ( 'NONE', #51808 ) ;
#18731=CARTESIAN_POINT ( 'NONE',  ( -8.250000000000000000, 7.250000000000001776, -9.000000000000001776 ) ) ;
#18738=CARTESIAN_POINT ( 'NONE',  ( -7.250000000000000888, 7.250000000000001776, -8.000000000000000000 ) ) ;
#18739=DIRECTION ( 'NONE',  ( -1.000000000000000000, 0.000000000000000000, 0.000000000000000000 ) ) ;
#18743=AXIS2_PLACEMENT_3D ( 'NONE', #5171, #48302, #42985 ) ;
#18749=DIRECTION ( 'NONE',  ( -1.000000000000000000, 0.000000000000000000, 0.000000000000000000 ) ) ;
#18757=ADVANCED_FACE ( 'NONE', ( #52513 ), #46843, .T. ) ;
#18760=LINE ( 'NONE', #35010, #1959 ) ;
#18766=AXIS2_PLACEMENT_3D ( 'NONE', #7098, #28677, #50244 ) ;
#18808=AXIS2_PLACEMENT_3D ( 'NONE', #28811, #45076, #39767 ) ;
#18817=CARTESIAN_POINT ( 'NONE',  ( 7.250000000000005329, 8.250000000000001776, -7.500000000000000000 ) ) ;
#18823=CYLINDRICAL_SURFACE ( 'NONE', #37043, 0.2000000000000005107 ) ;
#18825=VECTOR ( 'NONE', #56283, 1000.000000000000000 ) ;
#18826=CARTESIAN_POINT ( 'NONE',  ( 0.000000000000000000, 0.000000000000000000, -22.00000000000000000 ) ) ;
#18829=EDGE_LOOP ( 'NONE', ( #9908, #20327, #45437, #64449 ) ) ;
#18833=ORIENTED_EDGE ( 'NONE', *, *, #16396, .T. ) ;
#18839=EDGE_LOOP ( 'NONE', ( #17817, #11936, #18114, #59907 ) ) ;
#18843=DIRECTION ( 'NONE',  ( -1.000000000000000000, 0.000000000000000000, 0.000000000000000000 ) ) ;
#18846=DIRECTION ( 'NONE',  ( -1.000000000000000000, 0.000000000000000000, 0.000000000000000000 ) ) ;
#18851=ORIENTED_EDGE ( 'NONE', *, *, #67678, .F. ) ;
#18858=CARTESIAN_POINT ( 'NONE',  ( 7.450000000000006395, 7.250000000000000888, -23.50000000000000000 ) ) ;
#18869=CARTESIAN_POINT ( 'NONE',  ( 7.450000000000003730, -7.249999999999997335, -14.50000000000000000 ) ) ;
#18873=EDGE_CURVE ( 'NONE', #16636, #67323, #43644, .T. ) ;
#18879=AXIS2_PLACEMENT_3D ( 'NONE', #14370, #46881, #23922 ) ;
#18881=ADVANCED_FACE ( 'NONE', ( #43290 ), #59898, .F. ) ;
#18886=CARTESIAN_POINT ( 'NONE',  ( -9.690000000000001279, -9.690000000000001279, -5.000000000000000000 ) ) ;
#18898=FACE_OUTER_BOUND ( 'NONE', #45844, .T. ) ;
#18901=VECTOR ( 'NONE', #42742, 1000.000000000000000 ) ;
#18904=CARTESIAN_POINT ( 'NONE',  ( -7.250000000000000888, 8.250000000000001776, -12.00000000000000000 ) ) ;
#18907=AXIS2_PLACEMENT_3D ( 'NONE', #13029, #56188, #23999 ) ;
#18909=AXIS2_PLACEMENT_3D ( 'NONE', #48303, #27426, #69515 ) ;
#18921=AXIS2_PLACEMENT_3D ( 'NONE', #58616, #20080, #63209 ) ;
#18939=EDGE_CURVE ( 'NONE', #44299, #67897, #11791, .T. ) ;
#18971=PLANE ( 'NONE',  #18879 ) ;
#18975=LINE ( 'NONE', #52198, #50498 ) ;
#18981=CYLINDRICAL_SURFACE ( 'NONE', #12160, 0.2000000000000005107 ) ;
#18983=DIRECTION ( 'NONE',  ( 0.000000000000000000, 0.000000000000000000, -1.000000000000000000 ) ) ;
#18984=VERTEX_POINT ( 'NONE', #65888 ) ;
#18986=CARTESIAN_POINT ( 'NONE',  ( 7.450000000000003730, -7.249999999999997335, -23.50000000000000000 ) ) ;
#18987=DIRECTION ( 'NONE',  ( 0.000000000000000000, 0.000000000000000000, 1.000000000000000000 ) ) ;
#18992=LINE ( 'NONE', #2722, #51072 ) ;
#18993=ADVANCED_FACE ( 'NONE', ( #39366 ), #49971, .F. ) ;
#18999=VERTEX_POINT ( 'NONE', #35095 ) ;
#19006=AXIS2_PLACEMENT_3D ( 'NONE', #20414, #35977, #41980 ) ;
#19008=EDGE_LOOP ( 'NONE', ( #62854, #51867, #31363, #63193 ) ) ;
#19017=ADVANCED_FACE ( 'NONE', ( #29108 ), #50670, .T. ) ;
#19019=DIRECTION ( 'NONE',  ( 0.000000000000000000, 0.000000000000000000, 1.000000000000000000 ) ) ;
#19020=ORIENTED_EDGE ( 'NONE', *, *, #28975, .F. ) ;
#19021=ORIENTED_EDGE ( 'NONE', *, *, #17407, .T. ) ;
#19023=ORIENTED_EDGE ( 'NONE', *, *, #57002, .T. ) ;
#19025=EDGE_CURVE ( 'NONE', #61277, #26426, #59447, .T. ) ;
#19029=CARTESIAN_POINT ( 'NONE',  ( -7.250000000000000888, 7.250000000000001776, -26.00000000000001066 ) ) ;
#19033=CARTESIAN_POINT ( 'NONE',  ( 7.450000000000003730, -7.249999999999997335, -17.50000000000000000 ) ) ;
#19047=ORIENTED_EDGE ( 'NONE', *, *, #49810, .T. ) ;
#19055=ORIENTED_EDGE ( 'NONE', *, *, #22780, .F. ) ;
#19060=VERTEX_POINT ( 'NONE', #55632 ) ;
#19063=DIRECTION ( 'NONE',  ( -1.000000000000000000, 0.000000000000000000, 0.000000000000000000 ) ) ;
#19065=CYLINDRICAL_SURFACE ( 'NONE', #9321, 0.1999999999999987899 ) ;
#19067=PLANE ( 'NONE',  #67781 ) ;
#19082=ORIENTED_EDGE ( 'NONE', *, *, #57067, .T. ) ;
#19085=EDGE_CURVE ( 'NONE', #1911, #54119, #25206, .T. ) ;
#19092=EDGE_CURVE ( 'NONE', #33736, #21660, #16545, .T. ) ;
#19095=ORIENTED_EDGE ( 'NONE', *, *, #39943, .F. ) ;
#19101=PLANE ( 'NONE',  #20847 ) ;
#19108=EDGE_LOOP ( 'NONE', ( #22196, #5483, #3379, #24518 ) ) ;
#19110=CARTESIAN_POINT ( 'NONE',  ( -7.250000000000000888, 8.250000000000001776, -24.50000000000000000 ) ) ;
#19116=CYLINDRICAL_SURFACE ( 'NONE', #29838, 0.2000000000000005107 ) ;
#19119=CYLINDRICAL_SURFACE ( 'NONE', #35232, 1.000000000000000000 ) ;
#19122=VERTEX_POINT ( 'NONE', #51369 ) ;
#19129=ORIENTED_EDGE ( 'NONE', *, *, #25845, .F. ) ;
#19132=FACE_OUTER_BOUND ( 'NONE', #41040, .T. ) ;
#19140=VECTOR ( 'NONE', #57307, 1000.000000000000000 ) ;
#19157=CYLINDRICAL_SURFACE ( 'NONE', #38974, 0.1999999999999996503 ) ;
#19163=DIRECTION ( 'NONE',  ( -1.000000000000000000, 2.602085213965213008E-15, 0.000000000000000000 ) ) ;
#19171=LINE ( 'NONE', #35070, #38151 ) ;
#19173=EDGE_CURVE ( 'NONE', #41194, #56308, #21081, .T. ) ;
#19175=FACE_OUTER_BOUND ( 'NONE', #29721, .T. ) ;
#19185=CARTESIAN_POINT ( 'NONE',  ( 7.250000000000005329, -7.249999999999998224, -26.00000000000001066 ) ) ;
#19191=ORIENTED_EDGE ( 'NONE', *, *, #56623, .T. ) ;
#19194=DIRECTION ( 'NONE',  ( -1.000000000000000000, 0.000000000000000000, 0.000000000000000000 ) ) ;
#19196=CIRCLE ( 'NONE', #66633, 0.2000000000000005107 ) ;
#19199=CARTESIAN_POINT ( 'NONE',  ( 0.000000000000000000, 8.250000000000001776, -21.50000000000000000 ) ) ;
#19203=ORIENTED_EDGE ( 'NONE', *, *, #56623, .F. ) ;
#19215=EDGE_CURVE ( 'NONE', #49394, #48512, #61746, .T. ) ;
#19222=ORIENTED_EDGE ( 'NONE', *, *, #41543, .F. ) ;
#19223=CIRCLE ( 'NONE', #3422, 0.1999999999999987899 ) ;
#19230=CARTESIAN_POINT ( 'NONE',  ( -7.250000000000000000, -7.449999999999998401, -17.50000000000000000 ) ) ;
#19239=CARTESIAN_POINT ( 'NONE',  ( -7.450000000000001954, 7.250000000000000000, -9.000000000000001776 ) ) ;
#19264=CARTESIAN_POINT ( 'NONE',  ( 8.250000000000005329, 0.000000000000000000, -17.50000000000000000 ) ) ;
#19269=DIRECTION ( 'NONE',  ( -0.000000000000000000, 0.000000000000000000, 1.000000000000000000 ) ) ;
#19274=DIRECTION ( 'NONE',  ( -1.000000000000000000, 0.000000000000000000, 0.000000000000000000 ) ) ;
#19277=ORIENTED_EDGE ( 'NONE', *, *, #51890, .F. ) ;
#19293=ORIENTED_EDGE ( 'NONE', *, *, #21032, .F. ) ;
#19299=CARTESIAN_POINT ( 'NONE',  ( 7.250000000000004441, 7.450000000000001954, -12.50000000000000000 ) ) ;
#19305=ORIENTED_EDGE ( 'NONE', *, *, #49266, .F. ) ;
#19310=AXIS2_PLACEMENT_3D ( 'NONE', #53315, #26786, #22172 ) ;
#19314=CARTESIAN_POINT ( 'NONE',  ( 8.250000000000005329, -7.249999999999998224, -26.00000000000001066 ) ) ;
#19321=ORIENTED_EDGE ( 'NONE', *, *, #58543, .F. ) ;
#19326=LINE ( 'NONE', #6966, #47165 ) ;
#19332=CARTESIAN_POINT ( 'NONE',  ( -7.750000000000001776, 7.750000000000001776, 0.000000000000000000 ) ) ;
#19334=CARTESIAN_POINT ( 'NONE',  ( 9.750000000000001776, 9.690000000000001279, -5.000000000000000000 ) ) ;
#19339=PLANE ( 'NONE',  #65509 ) ;
#19348=ORIENTED_EDGE ( 'NONE', *, *, #34222, .T. ) ;
#19360=VECTOR ( 'NONE', #32154, 1000.000000000000000 ) ;
#19374=PLANE ( 'NONE',  #13472 ) ;
#19377=DIRECTION ( 'NONE',  ( 1.000000000000000000, -0.000000000000000000, 0.000000000000000000 ) ) ;
#19386=DIRECTION ( 'NONE',  ( -1.000000000000000000, 0.000000000000000000, 0.000000000000000000 ) ) ;
#19389=VERTEX_POINT ( 'NONE', #55084 ) ;
#19390=EDGE_CURVE ( 'NONE', #68564, #56334, #28193, .T. ) ;
#19406=EDGE_LOOP ( 'NONE', ( #55967, #41903, #56883, #34430 ) ) ;
#19412=VECTOR ( 'NONE', #33794, 1000.000000000000000 ) ;
#19422=DIRECTION ( 'NONE',  ( 0.000000000000000000, 0.000000000000000000, -1.000000000000000000 ) ) ;
#19430=ORIENTED_EDGE ( 'NONE', *, *, #46098, .T. ) ;
#19434=DIRECTION ( 'NONE',  ( 1.000000000000000000, 0.000000000000000000, 0.000000000000000000 ) ) ;
#19436=ADVANCED_FACE ( 'NONE', ( #7656 ), #23924, .T. ) ;
#19442=EDGE_LOOP ( 'NONE', ( #3173, #61125, #60514, #23026 ) ) ;
#19450=EDGE_LOOP ( 'NONE', ( #33484, #52885, #37638, #26643 ) ) ;
#19467=ORIENTED_EDGE ( 'NONE', *, *, #66513, .T. ) ;
#19470=DIRECTION ( 'NONE',  ( 1.000000000000000000, 0.000000000000000000, 0.000000000000000000 ) ) ;
#19473=ORIENTED_EDGE ( 'NONE', *, *, #29456, .F. ) ;
#19475=AXIS2_PLACEMENT_3D ( 'NONE', #40393, #45685, #34030 ) ;
#19476=CARTESIAN_POINT ( 'NONE',  ( -7.450000000000001954, -7.249999999999998224, -12.50000000000000000 ) ) ;
#19491=DIRECTION ( 'NONE',  ( 0.000000000000000000, 0.000000000000000000, 1.000000000000000000 ) ) ;
#19503=CARTESIAN_POINT ( 'NONE',  ( -8.250000000000001776, 7.250000000000000888, -26.00000000000001066 ) ) ;
#19512=CARTESIAN_POINT ( 'NONE',  ( -7.250000000000000888, -8.249999999999998224, -11.50000000000000000 ) ) ;
#19515=ADVANCED_FACE ( 'NONE', ( #3412 ), #24980, .T. ) ;
#19523=ORIENTED_EDGE ( 'NONE', *, *, #6677, .F. ) ;
#19525=LINE ( 'NONE', #24839, #29050 ) ;
#19527=LINE ( 'NONE', #58068, #55903 ) ;
#19532=ORIENTED_EDGE ( 'NONE', *, *, #30133, .T. ) ;
#19547=EDGE_LOOP ( 'NONE', ( #6325, #21469, #38271, #3237 ) ) ;
#19554=VERTEX_POINT ( 'NONE', #52561 ) ;
#19556=ORIENTED_EDGE ( 'NONE', *, *, #59173, .F. ) ;
#19557=ADVANCED_FACE ( 'NONE', ( #53612 ), #58911, .F. ) ;
#19562=CARTESIAN_POINT ( 'NONE',  ( 8.250000000000005329, 7.250000000000000888, -15.00000000000000000 ) ) ;
#19563=EDGE_CURVE ( 'NONE', #6549, #5855, #25696, .T. ) ;
#19565=ORIENTED_EDGE ( 'NONE', *, *, #44226, .F. ) ;
#19567=ADVANCED_FACE ( 'NONE', ( #69861 ), #53268, .F. ) ;
#19568=EDGE_CURVE ( 'NONE', #39415, #19811, #4475, .T. ) ;
#19569=CARTESIAN_POINT ( 'NONE',  ( -8.250000000000001776, 7.250000000000000888, -26.00000000000001066 ) ) ;
#19575=CARTESIAN_POINT ( 'NONE',  ( -7.250000000000000888, -8.249999999999998224, -18.00000000000000000 ) ) ;
#19576=ADVANCED_FACE ( 'NONE', ( #63522 ), #36634, .T. ) ;
#19580=AXIS2_PLACEMENT_3D ( 'NONE', #19961, #4420, #47539 ) ;
#19586=LINE ( 'NONE', #18179, #40154 ) ;
#19592=DIRECTION ( 'NONE',  ( 0.000000000000000000, 0.000000000000000000, 1.000000000000000000 ) ) ;
#19603=DIRECTION ( 'NONE',  ( 0.000000000000000000, 0.000000000000000000, -1.000000000000000000 ) ) ;
#19610=DIRECTION ( 'NONE',  ( -1.000000000000000000, 0.000000000000000000, 0.000000000000000000 ) ) ;
#19617=CIRCLE ( 'NONE', #47841, 1.000000000000002665 ) ;
#19618=AXIS2_PLACEMENT_3D ( 'NONE', #48274, #54620, #16785 ) ;
#19621=DIRECTION ( 'NONE',  ( 1.000000000000000000, 0.000000000000000000, 0.000000000000000000 ) ) ;
#19632=DIRECTION ( 'NONE',  ( -1.000000000000000000, 0.000000000000000000, 0.000000000000000000 ) ) ;
#19633=CYLINDRICAL_SURFACE ( 'NONE', #30284, 0.1999999999999987899 ) ;
#19640=ORIENTED_EDGE ( 'NONE', *, *, #4600, .T. ) ;
#19648=PLANE ( 'NONE',  #68400 ) ;
#19649=DIRECTION ( 'NONE',  ( 0.000000000000000000, 0.000000000000000000, -1.000000000000000000 ) ) ;
#19654=CARTESIAN_POINT ( 'NONE',  ( -7.250000000000000000, -8.749999999999998224, -30.00000000000001066 ) ) ;
#19663=CARTESIAN_POINT ( 'NONE',  ( 8.250000000000005329, 7.250000000000000888, -8.000000000000000000 ) ) ;
#19664=DIRECTION ( 'NONE',  ( 1.000000000000000000, -0.000000000000000000, 0.000000000000000000 ) ) ;
#19679=ORIENTED_EDGE ( 'NONE', *, *, #48709, .T. ) ;
#19683=LINE ( 'NONE', #56821, #9767 ) ;
#19686=DIRECTION ( 'NONE',  ( -0.000000000000000000, -0.000000000000000000, 1.000000000000000000 ) ) ;
#19699=VERTEX_POINT ( 'NONE', #22123 ) ;
#19700=EDGE_CURVE ( 'NONE', #69920, #9064, #42431, .T. ) ;
#19706=EDGE_LOOP ( 'NONE', ( #25263, #35504, #35188, #13003, #46589, #59041, #62212, #53928 ) ) ;
#19715=DIRECTION ( 'NONE',  ( 0.000000000000000000, 0.000000000000000000, 1.000000000000000000 ) ) ;
#19717=CARTESIAN_POINT ( 'NONE',  ( 0.000000000000000000, 0.000000000000000000, -24.00000000000000000 ) ) ;
#19725=ADVANCED_FACE ( 'NONE', ( #11153 ), #924, .F. ) ;
#19731=EDGE_CURVE ( 'NONE', #20521, #10069, #66293, .T. ) ;
#19743=EDGE_CURVE ( 'NONE', #36865, #29168, #12188, .T. ) ;
#19767=AXIS2_PLACEMENT_3D ( 'NONE', #11970, #38854, #28248 ) ;
#19769=VERTEX_POINT ( 'NONE', #67346 ) ;
#19784=CYLINDRICAL_SURFACE ( 'NONE', #32960, 0.2000000000000005107 ) ;
#19792=ORIENTED_EDGE ( 'NONE', *, *, #43218, .F. ) ;
#19793=CARTESIAN_POINT ( 'NONE',  ( -7.250000000000001776, -7.249999999999998224, -12.50000000000000000 ) ) ;
#19794=VERTEX_POINT ( 'NONE', #35492 ) ;
#19796=DIRECTION ( 'NONE',  ( 1.000000000000000000, -0.000000000000000000, 0.000000000000000000 ) ) ;
#19798=CARTESIAN_POINT ( 'NONE',  ( -8.250000000000001776, -7.249999999999998224, -21.50000000000000000 ) ) ;
#19799=FACE_OUTER_BOUND ( 'NONE', #20260, .T. ) ;
#19801=ORIENTED_EDGE ( 'NONE', *, *, #23397, .T. ) ;
#19804=CARTESIAN_POINT ( 'NONE',  ( 7.250000000000005329, 7.250000000000000888, -22.50000000000000000 ) ) ;
#19806=ORIENTED_EDGE ( 'NONE', *, *, #38289, .F. ) ;
#19811=VERTEX_POINT ( 'NONE', #61673 ) ;
#19819=VECTOR ( 'NONE', #30883, 1000.000000000000000 ) ;
#19828=CARTESIAN_POINT ( 'NONE',  ( -8.250000000000001776, 7.250000000000000888, -26.00000000000001066 ) ) ;
#19837=VECTOR ( 'NONE', #26495, 1000.000000000000000 ) ;
#19840=PLANE ( 'NONE',  #36274 ) ;
#19841=ORIENTED_EDGE ( 'NONE', *, *, #3359, .F. ) ;
#19847=FACE_BOUND ( 'NONE', #62365, .T. ) ;
#19852=DIRECTION ( 'NONE',  ( -0.000000000000000000, -0.000000000000000000, 1.000000000000000000 ) ) ;
#19860=ORIENTED_EDGE ( 'NONE', *, *, #60350, .F. ) ;
#19865=DIRECTION ( 'NONE',  ( 0.000000000000000000, 1.000000000000000000, 0.000000000000000000 ) ) ;
#19876=ADVANCED_FACE ( 'NONE', ( #36934 ), #19947, .F. ) ;
#19886=DIRECTION ( 'NONE',  ( -0.000000000000000000, -0.000000000000000000, 1.000000000000000000 ) ) ;
#19892=ORIENTED_EDGE ( 'NONE', *, *, #28231, .F. ) ;
#19902=DIRECTION ( 'NONE',  ( -0.000000000000000000, -0.000000000000000000, 1.000000000000000000 ) ) ;
#19906=EDGE_CURVE ( 'NONE', #21685, #53820, #62724, .T. ) ;
#19914=ORIENTED_EDGE ( 'NONE', *, *, #21388, .T. ) ;
#19924=EDGE_CURVE ( 'NONE', #59933, #41191, #26658, .T. ) ;
#19927=ORIENTED_EDGE ( 'NONE', *, *, #67861, .F. ) ;
#19946=CARTESIAN_POINT ( 'NONE',  ( 7.450000000000003730, -7.249999999999997335, -8.000000000000000000 ) ) ;
#19947=PLANE ( 'NONE',  #58347 ) ;
#19956=FACE_OUTER_BOUND ( 'NONE', #59096, .T. ) ;
#19960=AXIS2_PLACEMENT_3D ( 'NONE', #752, #22652, #22318 ) ;
#19961=CARTESIAN_POINT ( 'NONE',  ( 9.690000000000001279, -9.690000000000001279, -5.000000000000000000 ) ) ;
#19964=DIRECTION ( 'NONE',  ( 1.000000000000000000, 0.000000000000000000, 0.000000000000000000 ) ) ;
#19976=LINE ( 'NONE', #42590, #58862 ) ;
#19979=CARTESIAN_POINT ( 'NONE',  ( -7.250000000000000888, 7.250000000000001776, -22.50000000000000000 ) ) ;
#19981=CIRCLE ( 'NONE', #29001, 1.000000000000000000 ) ;
#19988=AXIS2_PLACEMENT_3D ( 'NONE', #3419, #67764, #61762 ) ;
#19991=FACE_OUTER_BOUND ( 'NONE', #39648, .T. ) ;
#19995=ORIENTED_EDGE ( 'NONE', *, *, #61997, .T. ) ;
#20010=DIRECTION ( 'NONE',  ( -1.794541526872559352E-16, -1.000000000000000000, 0.000000000000000000 ) ) ;
#20012=ORIENTED_EDGE ( 'NONE', *, *, #41454, .F. ) ;
#20016=VECTOR ( 'NONE', #54745, 1000.000000000000000 ) ;
#20017=ORIENTED_EDGE ( 'NONE', *, *, #31999, .F. ) ;
#20019=ORIENTED_EDGE ( 'NONE', *, *, #30195, .F. ) ;
#20030=ORIENTED_EDGE ( 'NONE', *, *, #633, .T. ) ;
#20033=CIRCLE ( 'NONE', #36970, 0.06000000000000102474 ) ;
#20042=DIRECTION ( 'NONE',  ( -1.000000000000000000, 0.000000000000000000, 0.000000000000000000 ) ) ;
#20045=DIRECTION ( 'NONE',  ( 1.000000000000000000, 0.000000000000000000, 0.000000000000000000 ) ) ;
#20048=CARTESIAN_POINT ( 'NONE',  ( 4.456444791733522252E-16, 7.450000000000002842, -18.50000000000000000 ) ) ;
#20053=CARTESIAN_POINT ( 'NONE',  ( -7.250000000000000888, 7.250000000000001776, -15.50000000000000000 ) ) ;
#20077=VECTOR ( 'NONE', #45607, 1000.000000000000000 ) ;
#20080=DIRECTION ( 'NONE',  ( -0.000000000000000000, -0.000000000000000000, 1.000000000000000000 ) ) ;
#20083=ORIENTED_EDGE ( 'NONE', *, *, #16466, .T. ) ;
#20086=AXIS2_PLACEMENT_3D ( 'NONE', #19029, #3122, #40236 ) ;
#20099=LINE ( 'NONE', #20787, #39013 ) ;
#20101=ORIENTED_EDGE ( 'NONE', *, *, #17177, .F. ) ;
#20106=DIRECTION ( 'NONE',  ( -1.000000000000000000, 0.000000000000000000, 0.000000000000000000 ) ) ;
#20109=CARTESIAN_POINT ( 'NONE',  ( 7.750000000000001776, 7.750000000000000000, 0.000000000000000000 ) ) ;
#20112=ORIENTED_EDGE ( 'NONE', *, *, #6603, .T. ) ;
#20124=FACE_OUTER_BOUND ( 'NONE', #4010, .T. ) ;
#20126=ORIENTED_EDGE ( 'NONE', *, *, #13033, .T. ) ;
#20135=ORIENTED_EDGE ( 'NONE', *, *, #46614, .T. ) ;
#20136=DIRECTION ( 'NONE',  ( -0.000000000000000000, -0.000000000000000000, -1.000000000000000000 ) ) ;
#20137=LINE ( 'NONE', #47007, #64506 ) ;
#20163=EDGE_CURVE ( 'NONE', #11939, #31382, #66192, .T. ) ;
#20167=DIRECTION ( 'NONE',  ( 0.000000000000000000, 0.000000000000000000, 1.000000000000000000 ) ) ;
#20170=DIRECTION ( 'NONE',  ( 0.000000000000000000, 0.000000000000000000, -1.000000000000000000 ) ) ;
#20171=DIRECTION ( 'NONE',  ( 0.000000000000000000, 0.000000000000000000, -1.000000000000000000 ) ) ;
#20176=ORIENTED_EDGE ( 'NONE', *, *, #24471, .F. ) ;
#20177=CIRCLE ( 'NONE', #59693, 1.000000000000000000 ) ;
#20181=ORIENTED_EDGE ( 'NONE', *, *, #43320, .T. ) ;
#20184=CARTESIAN_POINT ( 'NONE',  ( 9.690000000000001279, 9.750000000000001776, -7.000000000000000000 ) ) ;
#20195=VERTEX_POINT ( 'NONE', #56295 ) ;
#20197=CARTESIAN_POINT ( 'NONE',  ( -8.250000000000001776, -7.249999999999998224, -26.00000000000001066 ) ) ;
#20205=ORIENTED_EDGE ( 'NONE', *, *, #8892, .T. ) ;
#20211=DIRECTION ( 'NONE',  ( -1.000000000000000000, 0.000000000000000000, -0.000000000000000000 ) ) ;
#20213=CARTESIAN_POINT ( 'NONE',  ( -8.250000000000001776, -7.249999999999998224, -26.00000000000001066 ) ) ;
#20219=AXIS2_PLACEMENT_3D ( 'NONE', #32011, #54274, #60249 ) ;
#20224=ORIENTED_EDGE ( 'NONE', *, *, #26624, .F. ) ;
#20229=CIRCLE ( 'NONE', #60844, 0.1999999999999987899 ) ;
#20232=CARTESIAN_POINT ( 'NONE',  ( 8.250000000000005329, -7.249999999999998224, -16.50000000000000000 ) ) ;
#20233=AXIS2_PLACEMENT_3D ( 'NONE', #52195, #26035, #57148 ) ;
#20234=CARTESIAN_POINT ( 'NONE',  ( -7.250000000000001776, -7.249999999999998224, -18.50000000000000000 ) ) ;
#20247=DIRECTION ( 'NONE',  ( -1.000000000000000000, 2.602085213965213008E-15, 0.000000000000000000 ) ) ;
#20248=CARTESIAN_POINT ( 'NONE',  ( 7.250000000000004441, 8.750000000000001776, -30.00000000000001066 ) ) ;
#20249=AXIS2_PLACEMENT_3D ( 'NONE', #38898, #10998, #28285 ) ;
#20254=ORIENTED_EDGE ( 'NONE', *, *, #8666, .T. ) ;
#20260=EDGE_LOOP ( 'NONE', ( #61680, #50745, #56449, #17768 ) ) ;
#20264=VERTEX_POINT ( 'NONE', #63005 ) ;
#20266=CARTESIAN_POINT ( 'NONE',  ( 0.000000000000000000, -7.449999999999998401, -16.50000000000000000 ) ) ;
#20271=DIRECTION ( 'NONE',  ( -0.000000000000000000, -0.000000000000000000, -1.000000000000000000 ) ) ;
#20272=ORIENTED_EDGE ( 'NONE', *, *, #12868, .T. ) ;
#20274=ORIENTED_EDGE ( 'NONE', *, *, #14844, .T. ) ;
#20277=PLANE ( 'NONE',  #13733 ) ;
#20288=AXIS2_PLACEMENT_3D ( 'NONE', #34286, #61881, #46657 ) ;
#20294=CARTESIAN_POINT ( 'NONE',  ( 8.250000000000005329, 0.000000000000000000, -25.00000000000000000 ) ) ;
#20305=VERTEX_POINT ( 'NONE', #30824 ) ;
#20327=ORIENTED_EDGE ( 'NONE', *, *, #51339, .T. ) ;
#20333=FACE_OUTER_BOUND ( 'NONE', #67655, .T. ) ;
#20337=FACE_OUTER_BOUND ( 'NONE', #23297, .T. ) ;
#20345=DIRECTION ( 'NONE',  ( 1.000000000000000000, 0.000000000000000000, 0.000000000000000000 ) ) ;
#20347=ORIENTED_EDGE ( 'NONE', *, *, #27175, .T. ) ;
#20351=LINE ( 'NONE', #41570, #1181 ) ;
#20355=ORIENTED_EDGE ( 'NONE', *, *, #11569, .T. ) ;
#20356=CARTESIAN_POINT ( 'NONE',  ( -7.250000000000000000, -7.449999999999998401, -9.000000000000001776 ) ) ;
#20362=DIRECTION ( 'NONE',  ( 0.000000000000000000, 0.000000000000000000, 1.000000000000000000 ) ) ;
#20364=DIRECTION ( 'NONE',  ( 0.000000000000000000, 0.000000000000000000, 1.000000000000000000 ) ) ;
#20370=EDGE_CURVE ( 'NONE', #19794, #10769, #49524, .T. ) ;
#20372=VECTOR ( 'NONE', #42104, 1000.000000000000000 ) ;
#20375=DIRECTION ( 'NONE',  ( 1.000000000000000000, -0.000000000000000000, 0.000000000000000000 ) ) ;
#20378=VERTEX_POINT ( 'NONE', #54497 ) ;
#20379=DIRECTION ( 'NONE',  ( 0.000000000000000000, 0.000000000000000000, 1.000000000000000000 ) ) ;
#20382=DIRECTION ( 'NONE',  ( 0.000000000000000000, 0.000000000000000000, 1.000000000000000000 ) ) ;
#20388=DIRECTION ( 'NONE',  ( 0.000000000000000000, 1.000000000000000000, 0.000000000000000000 ) ) ;
#20396=DIRECTION ( 'NONE',  ( 0.000000000000000000, -0.000000000000000000, 1.000000000000000000 ) ) ;
#20407=EDGE_CURVE ( 'NONE', #44854, #14810, #6051, .T. ) ;
#20409=DIRECTION ( 'NONE',  ( -0.000000000000000000, 0.000000000000000000, 1.000000000000000000 ) ) ;
#20414=CARTESIAN_POINT ( 'NONE',  ( -9.690000000000001279, -9.690000000000001279, -4.250000000000000000 ) ) ;
#20418=ORIENTED_EDGE ( 'NONE', *, *, #36371, .T. ) ;
#20426=LINE ( 'NONE', #3473, #63771 ) ;
#20428=ORIENTED_EDGE ( 'NONE', *, *, #10820, .F. ) ;
#20432=CARTESIAN_POINT ( 'NONE',  ( 8.250000000000005329, -7.249999999999998224, -26.00000000000001066 ) ) ;
#20433=VERTEX_POINT ( 'NONE', #60124 ) ;
#20442=ORIENTED_EDGE ( 'NONE', *, *, #29986, .T. ) ;
#20448=VERTEX_POINT ( 'NONE', #27608 ) ;
#20451=EDGE_CURVE ( 'NONE', #27517, #55865, #61743, .T. ) ;
#20472=VERTEX_POINT ( 'NONE', #45586 ) ;
#20480=CARTESIAN_POINT ( 'NONE',  ( 7.250000000000005329, 7.250000000000000888, -15.50000000000000000 ) ) ;
#20482=ORIENTED_EDGE ( 'NONE', *, *, #46930, .F. ) ;
#20485=ORIENTED_EDGE ( 'NONE', *, *, #23734, .F. ) ;
#20492=AXIS2_PLACEMENT_3D ( 'NONE', #52795, #8574, #35439 ) ;
#20493=CARTESIAN_POINT ( 'NONE',  ( -7.250000000000000888, 7.250000000000001776, -25.00000000000000000 ) ) ;
#20497=ORIENTED_EDGE ( 'NONE', *, *, #34594, .F. ) ;
#20499=EDGE_CURVE ( 'NONE', #50, #11776, #29675, .T. ) ;
#20500=DIRECTION ( 'NONE',  ( -0.000000000000000000, -0.000000000000000000, -1.000000000000000000 ) ) ;
#20509=ORIENTED_EDGE ( 'NONE', *, *, #22383, .T. ) ;
#20511=CARTESIAN_POINT ( 'NONE',  ( -8.250000000000000000, 7.250000000000001776, -12.00000000000000000 ) ) ;
#20516=PLANE ( 'NONE',  #49226 ) ;
#20521=VERTEX_POINT ( 'NONE', #60811 ) ;
#20531=AXIS2_PLACEMENT_3D ( 'NONE', #59644, #60316, #11191 ) ;
#20537=EDGE_LOOP ( 'NONE', ( #29260, #4854, #26693, #1091 ) ) ;
#20540=EDGE_CURVE ( 'NONE', #36929, #52415, #49863, .T. ) ;
#20546=CARTESIAN_POINT ( 'NONE',  ( -7.250000000000000888, 7.250000000000001776, -25.50000000000000355 ) ) ;
#20547=ORIENTED_EDGE ( 'NONE', *, *, #45271, .F. ) ;
#20548=AXIS2_PLACEMENT_3D ( 'NONE', #49184, #22988, #2122 ) ;
#20550=LINE ( 'NONE', #46366, #34074 ) ;
#20553=PRODUCT_DEFINITION ( 'UNKNOWN', '', #56169, #29620 ) ;
#20554=DIRECTION ( 'NONE',  ( 8.951101527228104953E-17, 1.000000000000000000, -0.000000000000000000 ) ) ;
#20561=VERTEX_POINT ( 'NONE', #12356 ) ;
#20582=VECTOR ( 'NONE', #64949, 1000.000000000000000 ) ;
#20585=DIRECTION ( 'NONE',  ( 0.000000000000000000, 0.000000000000000000, 1.000000000000000000 ) ) ;
#20587=VERTEX_POINT ( 'NONE', #39586 ) ;
#20588=DIRECTION ( 'NONE',  ( -1.000000000000000000, 0.000000000000000000, 0.000000000000000000 ) ) ;
#20592=DIRECTION ( 'NONE',  ( -0.000000000000000000, -0.000000000000000000, -1.000000000000000000 ) ) ;
#20595=DIRECTION ( 'NONE',  ( 0.000000000000000000, 0.000000000000000000, -1.000000000000000000 ) ) ;
#20598=CARTESIAN_POINT ( 'NONE',  ( -7.250000000000001776, -7.249999999999998224, -26.00000000000001066 ) ) ;
#20602=ADVANCED_FACE ( 'NONE', ( #9886, #31459 ), #14832, .F. ) ;
#20604=CARTESIAN_POINT ( 'NONE',  ( 0.000000000000000000, -8.249999999999998224, -23.00000000000000000 ) ) ;
#20609=LINE ( 'NONE', #47151, #53149 ) ;
#20611=PLANE ( 'NONE',  #44635 ) ;
#20614=VERTEX_POINT ( 'NONE', #62917 ) ;
#20622=EDGE_CURVE ( 'NONE', #15345, #13221, #14483, .T. ) ;
#20624=EDGE_CURVE ( 'NONE', #2477, #29173, #41470, .T. ) ;
#20628=CARTESIAN_POINT ( 'NONE',  ( -7.250000000000000888, 7.450000000000003730, -20.50000000000000000 ) ) ;
#20631=CARTESIAN_POINT ( 'NONE',  ( 9.690000000000001279, -9.690000000000001279, -4.250000000000000000 ) ) ;
#20643=VECTOR ( 'NONE', #46131, 1000.000000000000000 ) ;
#20645=DIRECTION ( 'NONE',  ( 1.000000000000000000, -0.000000000000000000, 0.000000000000000000 ) ) ;
#20648=AXIS2_PLACEMENT_3D ( 'NONE', #38810, #15869, #69956 ) ;
#20656=DIRECTION ( 'NONE',  ( 0.000000000000000000, 0.000000000000000000, -1.000000000000000000 ) ) ;
#20661=VECTOR ( 'NONE', #21012, 1000.000000000000000 ) ;
#20665=LINE ( 'NONE', #26330, #38464 ) ;
#20666=VECTOR ( 'NONE', #36711, 1000.000000000000000 ) ;
#20668=CYLINDRICAL_SURFACE ( 'NONE', #65610, 0.2000000000000005107 ) ;
#20676=VECTOR ( 'NONE', #19377, 1000.000000000000000 ) ;
#20677=CARTESIAN_POINT ( 'NONE',  ( -8.250000000000001776, -7.249999999999998224, -9.000000000000001776 ) ) ;
#20678=DIRECTION ( 'NONE',  ( 1.000000000000000000, 0.000000000000000000, 0.000000000000000000 ) ) ;
#20679=ORIENTED_EDGE ( 'NONE', *, *, #7611, .T. ) ;
#20697=ORIENTED_EDGE ( 'NONE', *, *, #32575, .T. ) ;
#20699=EDGE_CURVE ( 'NONE', #6525, #31960, #21187, .T. ) ;
#20720=DIRECTION ( 'NONE',  ( 0.000000000000000000, 0.000000000000000000, -1.000000000000000000 ) ) ;
#20727=CARTESIAN_POINT ( 'NONE',  ( -7.250000000000000888, 7.250000000000001776, -14.50000000000000000 ) ) ;
#20728=EDGE_CURVE ( 'NONE', #14563, #63937, #54405, .T. ) ;
#20736=VECTOR ( 'NONE', #1981, 1000.000000000000000 ) ;
#20737=EDGE_LOOP ( 'NONE', ( #25679, #55760, #21894, #60783 ) ) ;
#20738=DIRECTION ( 'NONE',  ( 0.000000000000000000, 1.000000000000000000, 0.000000000000000000 ) ) ;
#20744=CIRCLE ( 'NONE', #36595, 0.2000000000000005107 ) ;
#20761=LINE ( 'NONE', #64597, #50959 ) ;
#20776=CARTESIAN_POINT ( 'NONE',  ( -8.250000000000001776, 0.000000000000000000, -18.00000000000000000 ) ) ;
#20784=DIRECTION ( 'NONE',  ( 0.000000000000000000, 0.000000000000000000, 1.000000000000000000 ) ) ;
#20787=CARTESIAN_POINT ( 'NONE',  ( -8.250000000000001776, 7.250000000000000888, -26.00000000000001066 ) ) ;
#20792=ORIENTED_EDGE ( 'NONE', *, *, #65315, .F. ) ;
#20814=DIRECTION ( 'NONE',  ( 0.000000000000000000, -0.000000000000000000, 1.000000000000000000 ) ) ;
#20819=CARTESIAN_POINT ( 'NONE',  ( 4.456444791733522252E-16, 7.450000000000002842, -10.50000000000000000 ) ) ;
#20821=ORIENTED_EDGE ( 'NONE', *, *, #30265, .F. ) ;
#20828=VERTEX_POINT ( 'NONE', #35152 ) ;
#20837=CARTESIAN_POINT ( 'NONE',  ( 7.450000000000006395, 7.250000000000000888, -21.50000000000000000 ) ) ;
#20844=ORIENTED_EDGE ( 'NONE', *, *, #26315, .F. ) ;
#20847=AXIS2_PLACEMENT_3D ( 'NONE', #56236, #35340, #39276 ) ;
#20848=AXIS2_PLACEMENT_3D ( 'NONE', #2542, #45319, #66888 ) ;
#20851=LINE ( 'NONE', #62571, #3899 ) ;
#20866=ORIENTED_EDGE ( 'NONE', *, *, #41456, .F. ) ;
#20872=CARTESIAN_POINT ( 'NONE',  ( -7.250000000000000888, 7.250000000000001776, -10.50000000000000000 ) ) ;
#20877=ORIENTED_EDGE ( 'NONE', *, *, #43721, .T. ) ;
#20890=AXIS2_PLACEMENT_3D ( 'NONE', #64035, #26190, #21923 ) ;
#20893=EDGE_CURVE ( 'NONE', #28576, #48129, #40397, .T. ) ;
#20898=CARTESIAN_POINT ( 'NONE',  ( 7.250000000000004441, 7.450000000000001954, -19.00000000000000000 ) ) ;
#20901=DIRECTION ( 'NONE',  ( 0.000000000000000000, 0.000000000000000000, 1.000000000000000000 ) ) ;
#20910=EDGE_LOOP ( 'NONE', ( #17622, #33708, #68235, #10370, #66608, #36637, #33260, #50258 ) ) ;
#20929=DIRECTION ( 'NONE',  ( -1.000000000000000000, 0.000000000000000000, 0.000000000000000000 ) ) ;
#20946=VECTOR ( 'NONE', #36701, 1000.000000000000000 ) ;
#20960=ORIENTED_EDGE ( 'NONE', *, *, #48604, .F. ) ;
#20964=DIRECTION ( 'NONE',  ( 1.000000000000000000, -0.000000000000000000, 0.000000000000000000 ) ) ;
#20966=PLANE ( 'NONE',  #26601 ) ;
#20969=LINE ( 'NONE', #48901, #57636 ) ;
#20985=EDGE_CURVE ( 'NONE', #31578, #58971, #30916, .T. ) ;
#20987=VECTOR ( 'NONE', #62042, 1000.000000000000000 ) ;
#20992=AXIS2_PLACEMENT_3D ( 'NONE', #69013, #13249, #3967 ) ;
#20996=DIRECTION ( 'NONE',  ( -1.000000000000000000, 2.602085213965213008E-15, 0.000000000000000000 ) ) ;
#20999=DIRECTION ( 'NONE',  ( 0.000000000000000000, -0.000000000000000000, 1.000000000000000000 ) ) ;
#21010=CIRCLE ( 'NONE', #67295, 0.2000000000000005107 ) ;
#21012=DIRECTION ( 'NONE',  ( 0.000000000000000000, -0.000000000000000000, 1.000000000000000000 ) ) ;
#21013=ORIENTED_EDGE ( 'NONE', *, *, #23700, .F. ) ;
#21015=PLANE ( 'NONE',  #37300 ) ;
#21032=EDGE_CURVE ( 'NONE', #34914, #40390, #32320, .T. ) ;
#21035=ORIENTED_EDGE ( 'NONE', *, *, #21919, .F. ) ;
#21050=CARTESIAN_POINT ( 'NONE',  ( -7.450000000000001954, 7.250000000000000000, -8.500000000000000000 ) ) ;
#21055=ORIENTED_EDGE ( 'NONE', *, *, #19731, .F. ) ;
#21058=AXIS2_PLACEMENT_3D ( 'NONE', #18696, #24000, #61844 ) ;
#21061=FACE_OUTER_BOUND ( 'NONE', #37126, .T. ) ;
#21062=EDGE_LOOP ( 'NONE', ( #29572, #68088, #9260, #32967, #33735, #22102, #6511, #2549 ) ) ;
#21067=CARTESIAN_POINT ( 'NONE',  ( 7.450000000000003730, -7.249999999999997335, -9.500000000000001776 ) ) ;
#21072=ORIENTED_EDGE ( 'NONE', *, *, #55654, .F. ) ;
#21073=CARTESIAN_POINT ( 'NONE',  ( 7.250000000000005329, 7.250000000000000888, -9.500000000000001776 ) ) ;
#21075=CARTESIAN_POINT ( 'NONE',  ( 7.250000000000005329, -7.249999999999998224, -12.00000000000000000 ) ) ;
#21077=DIRECTION ( 'NONE',  ( -1.000000000000000000, 0.000000000000000000, 0.000000000000000000 ) ) ;
#21081=CIRCLE ( 'NONE', #60593, 1.000000000000000000 ) ;
#21083=AXIS2_PLACEMENT_3D ( 'NONE', #55854, #45579, #66463 ) ;
#21089=CARTESIAN_POINT ( 'NONE',  ( 7.450000000000003730, -7.249999999999997335, -15.50000000000000000 ) ) ;
#21091=CARTESIAN_POINT ( 'NONE',  ( -7.450000000000001954, 7.250000000000000000, -25.00000000000000000 ) ) ;
#21098=CARTESIAN_POINT ( 'NONE',  ( 0.000000000000000000, 0.000000000000000000, -25.00000000000000000 ) ) ;
#21100=CARTESIAN_POINT ( 'NONE',  ( 8.250000000000005329, 7.250000000000000888, -26.00000000000001066 ) ) ;
#21102=DIRECTION ( 'NONE',  ( 1.000000000000000000, -5.981805089575194965E-17, 0.000000000000000000 ) ) ;
#21104=CARTESIAN_POINT ( 'NONE',  ( 7.250000000000005329, -7.449999999999998401, -20.50000000000000000 ) ) ;
#21105=DIRECTION ( 'NONE',  ( -1.794541526872559352E-16, -1.000000000000000000, 0.000000000000000000 ) ) ;
#21106=ADVANCED_FACE ( 'NONE', ( #43262 ), #64846, .T. ) ;
#21109=AXIS2_PLACEMENT_3D ( 'NONE', #67051, #29566, #2356 ) ;
#21128=EDGE_LOOP ( 'NONE', ( #49397, #61586, #5822, #35802 ) ) ;
#21132=DIRECTION ( 'NONE',  ( -0.000000000000000000, -0.000000000000000000, 1.000000000000000000 ) ) ;
#21135=ORIENTED_EDGE ( 'NONE', *, *, #11722, .F. ) ;
#21146=CIRCLE ( 'NONE', #50497, 0.2000000000000005107 ) ;
#21148=DIRECTION ( 'NONE',  ( 0.000000000000000000, -0.000000000000000000, 1.000000000000000000 ) ) ;
#21151=VECTOR ( 'NONE', #23086, 1000.000000000000000 ) ;
#21153=CARTESIAN_POINT ( 'NONE',  ( 8.250000000000005329, 8.250000000000001776, -26.00000000000001066 ) ) ;
#21159=VECTOR ( 'NONE', #9922, 1000.000000000000000 ) ;
#21164=LINE ( 'NONE', #53689, #68555 ) ;
#21166=ORIENTED_EDGE ( 'NONE', *, *, #38878, .T. ) ;
#21170=CYLINDRICAL_SURFACE ( 'NONE', #43699, 1.000000000000000000 ) ;
#21176=ADVANCED_FACE ( 'NONE', ( #12802 ), #18823, .T. ) ;
#21178=CARTESIAN_POINT ( 'NONE',  ( 9.690000000000001279, 9.690000000000001279, -5.000000000000000000 ) ) ;
#21181=ORIENTED_EDGE ( 'NONE', *, *, #51013, .T. ) ;
#21187=LINE ( 'NONE', #60036, #20016 ) ;
#21191=DIRECTION ( 'NONE',  ( -1.794541526872559352E-16, -1.000000000000000000, 0.000000000000000000 ) ) ;
#21193=DIRECTION ( 'NONE',  ( 1.000000000000000000, -0.000000000000000000, 0.000000000000000000 ) ) ;
#21202=CIRCLE ( 'NONE', #60694, 1.000000000000002665 ) ;
#21218=VECTOR ( 'NONE', #8324, 1000.000000000000000 ) ;
#21232=VERTEX_POINT ( 'NONE', #2210 ) ;
#21235=DIRECTION ( 'NONE',  ( 1.000000000000000000, 0.000000000000000000, 0.000000000000000000 ) ) ;
#21246=EDGE_LOOP ( 'NONE', ( #24671, #44508, #396, #54342 ) ) ;
#21252=CIRCLE ( 'NONE', #14480, 0.2000000000000005107 ) ;
#21253=EDGE_CURVE ( 'NONE', #7192, #7881, #19171, .T. ) ;
#21258=DIRECTION ( 'NONE',  ( -1.000000000000000000, 0.000000000000000000, 0.000000000000000000 ) ) ;
#21262=CIRCLE ( 'NONE', #69812, 1.500000000000000444 ) ;
#21273=ORIENTED_EDGE ( 'NONE', *, *, #25342, .F. ) ;
#21285=CYLINDRICAL_SURFACE ( 'NONE', #16749, 1.000000000000000000 ) ;
#21289=EDGE_LOOP ( 'NONE', ( #66254, #33301, #13198, #69600 ) ) ;
#21290=CARTESIAN_POINT ( 'NONE',  ( 7.450000000000006395, 7.250000000000000888, -19.00000000000000000 ) ) ;
#21298=EDGE_LOOP ( 'NONE', ( #22293, #41816, #24798, #25380 ) ) ;
#21299=AXIS2_PLACEMENT_3D ( 'NONE', #23098, #64948, #7173 ) ;
#21319=ORIENTED_EDGE ( 'NONE', *, *, #16142, .F. ) ;
#21320=VERTEX_POINT ( 'NONE', #47104 ) ;
#21322=PLANE ( 'NONE',  #15877 ) ;
#21323=ORIENTED_EDGE ( 'NONE', *, *, #44784, .F. ) ;
#21330=VERTEX_POINT ( 'NONE', #42491 ) ;
#21336=CARTESIAN_POINT ( 'NONE',  ( -7.450000000000001954, 7.250000000000000000, -17.50000000000000000 ) ) ;
#21342=FACE_OUTER_BOUND ( 'NONE', #30608, .T. ) ;
#21345=ADVANCED_FACE ( 'NONE', ( #69728 ), #21285, .T. ) ;
#21350=EDGE_LOOP ( 'NONE', ( #54533, #43940, #48891, #25928 ) ) ;
#21353=ADVANCED_FACE ( 'NONE', ( #65117 ), #1100, .T. ) ;
#21368=PLANE ( 'NONE',  #62432 ) ;
#21370=CARTESIAN_POINT ( 'NONE',  ( -8.250000000000001776, 7.250000000000000888, -26.00000000000001066 ) ) ;
#21377=CARTESIAN_POINT ( 'NONE',  ( 8.250000000000005329, 0.000000000000000000, -24.00000000000000000 ) ) ;
#21379=CARTESIAN_POINT ( 'NONE',  ( 7.250000000000005329, -7.249999999999998224, -11.50000000000000000 ) ) ;
#21384=DIRECTION ( 'NONE',  ( -1.000000000000000000, 0.000000000000000000, 0.000000000000000000 ) ) ;
#21388=EDGE_CURVE ( 'NONE', #36247, #4689, #54506, .T. ) ;
#21389=AXIS2_PLACEMENT_3D ( 'NONE', #61630, #17465, #44670 ) ;
#21396=ORIENTED_EDGE ( 'NONE', *, *, #51496, .T. ) ;
#21408=DIRECTION ( 'NONE',  ( -0.000000000000000000, -0.000000000000000000, 1.000000000000000000 ) ) ;
#21421=EDGE_CURVE ( 'NONE', #57899, #16799, #48499, .T. ) ;
#21425=DIRECTION ( 'NONE',  ( 1.000000000000000000, 0.000000000000000000, 0.000000000000000000 ) ) ;
#21429=APPLICATION_CONTEXT ( 'automotive_design' ) ;
#21430=CARTESIAN_POINT ( 'NONE',  ( -8.689999999999999503, 9.750000000000001776, -7.000000000000000000 ) ) ;
#21437=DIRECTION ( 'NONE',  ( -0.000000000000000000, -0.000000000000000000, 1.000000000000000000 ) ) ;
#21442=AXIS2_PLACEMENT_3D ( 'NONE', #56124, #56808, #24649 ) ;
#21443=DIRECTION ( 'NONE',  ( -1.000000000000000000, 0.000000000000000000, 0.000000000000000000 ) ) ;
#21445=ORIENTED_EDGE ( 'NONE', *, *, #53804, .T. ) ;
#21448=DIRECTION ( 'NONE',  ( -0.000000000000000000, -0.000000000000000000, 1.000000000000000000 ) ) ;
#21453=VERTEX_POINT ( 'NONE', #61508 ) ;
#21454=AXIS2_PLACEMENT_3D ( 'NONE', #18121, #39689, #12807 ) ;
#21457=LINE ( 'NONE', #53996, #10833 ) ;
#21462=LINE ( 'NONE', #4169, #2506 ) ;
#21466=ORIENTED_EDGE ( 'NONE', *, *, #47070, .T. ) ;
#21467=ORIENTED_EDGE ( 'NONE', *, *, #21701, .T. ) ;
#21469=ORIENTED_EDGE ( 'NONE', *, *, #34471, .F. ) ;
#21471=PLANE ( 'NONE',  #38255 ) ;
#21473=AXIS2_PLACEMENT_3D ( 'NONE', #52908, #48627, #64206 ) ;
#21475=VERTEX_POINT ( 'NONE', #40304 ) ;
#21479=EDGE_CURVE ( 'NONE', #34893, #14054, #28999, .T. ) ;
#21481=ORIENTED_EDGE ( 'NONE', *, *, #61369, .F. ) ;
#21483=VERTEX_POINT ( 'NONE', #62218 ) ;
#21501=CIRCLE ( 'NONE', #66927, 0.2000000000000005107 ) ;
#21506=CARTESIAN_POINT ( 'NONE',  ( -8.250000000000000000, 7.250000000000001776, -16.00000000000000000 ) ) ;
#21510=AXIS2_PLACEMENT_3D ( 'NONE', #32576, #53793, #43507 ) ;
#21516=ADVANCED_FACE ( 'NONE', ( #51256 ), #34645, .T. ) ;
#21522=ORIENTED_EDGE ( 'NONE', *, *, #7463, .T. ) ;
#21527=LINE ( 'NONE', #10225, #66861 ) ;
#21531=DIRECTION ( 'NONE',  ( 0.000000000000000000, 0.000000000000000000, 1.000000000000000000 ) ) ;
#21539=LINE ( 'NONE', #48763, #11695 ) ;
#21543=DIRECTION ( 'NONE',  ( 0.000000000000000000, 0.000000000000000000, 1.000000000000000000 ) ) ;
#21548=VECTOR ( 'NONE', #16844, 1000.000000000000000 ) ;
#21552=DIRECTION ( 'NONE',  ( -1.000000000000000000, 0.000000000000000000, -0.000000000000000000 ) ) ;
#21559=ORIENTED_EDGE ( 'NONE', *, *, #13507, .T. ) ;
#21562=DIRECTION ( 'NONE',  ( 0.000000000000000000, 1.000000000000000000, 0.000000000000000000 ) ) ;
#21563=VERTEX_POINT ( 'NONE', #31115 ) ;
#21567=FACE_OUTER_BOUND ( 'NONE', #28861, .T. ) ;
#21574=ORIENTED_EDGE ( 'NONE', *, *, #23263, .F. ) ;
#21577=CARTESIAN_POINT ( 'NONE',  ( 0.000000000000000000, -8.249999999999998224, -18.00000000000000000 ) ) ;
#21583=LINE ( 'NONE', #11641, #769 ) ;
#21585=ADVANCED_FACE ( 'NONE', ( #46654 ), #62557, .F. ) ;
#21589=ORIENTED_EDGE ( 'NONE', *, *, #68420, .F. ) ;
#21592=DIRECTION ( 'NONE',  ( -1.000000000000000000, 0.000000000000000000, 0.000000000000000000 ) ) ;
#21593=AXIS2_PLACEMENT_3D ( 'NONE', #30202, #47172, #25610 ) ;
#21599=CARTESIAN_POINT ( 'NONE',  ( 7.250000000000004441, 7.450000000000001954, -25.50000000000000355 ) ) ;
#21607=DIRECTION ( 'NONE',  ( 1.000000000000000000, 0.000000000000000000, 0.000000000000000000 ) ) ;
#21610=AXIS2_PLACEMENT_3D ( 'NONE', #64604, #53655, #69211 ) ;
#21640=EDGE_LOOP ( 'NONE', ( #3449, #67798, #12700, #57303 ) ) ;
#21660=VERTEX_POINT ( 'NONE', #320 ) ;
#21661=ORIENTED_EDGE ( 'NONE', *, *, #14557, .F. ) ;
#21668=CARTESIAN_POINT ( 'NONE',  ( 7.250000000000005329, -7.449999999999998401, -18.50000000000000000 ) ) ;
#21671=VERTEX_POINT ( 'NONE', #15887 ) ;
#21678=ORIENTED_EDGE ( 'NONE', *, *, #64488, .F. ) ;
#21685=VERTEX_POINT ( 'NONE', #54074 ) ;
#21688=CARTESIAN_POINT ( 'NONE',  ( -8.250000000000001776, 0.000000000000000000, -23.00000000000000000 ) ) ;
#21692=DIRECTION ( 'NONE',  ( 0.000000000000000000, 0.000000000000000000, -1.000000000000000000 ) ) ;
#21701=EDGE_CURVE ( 'NONE', #53480, #22431, #28690, .T. ) ;
#21710=VECTOR ( 'NONE', #63281, 1000.000000000000000 ) ;
#21714=ORIENTED_EDGE ( 'NONE', *, *, #29379, .F. ) ;
#21715=AXIS2_PLACEMENT_3D ( 'NONE', #20480, #31462, #63984 ) ;
#21716=DIRECTION ( 'NONE',  ( 1.000000000000000000, -0.000000000000000000, 0.000000000000000000 ) ) ;
#21718=VERTEX_POINT ( 'NONE', #10929 ) ;
#21722=ORIENTED_EDGE ( 'NONE', *, *, #8799, .T. ) ;
#21736=VERTEX_POINT ( 'NONE', #49099 ) ;
#21737=EDGE_CURVE ( 'NONE', #6284, #35692, #50141, .T. ) ;
#21738=ORIENTED_EDGE ( 'NONE', *, *, #31529, .F. ) ;
#21740=EDGE_CURVE ( 'NONE', #48173, #11798, #28556, .T. ) ;
#21741=FACE_OUTER_BOUND ( 'NONE', #2092, .T. ) ;
#21744=ORIENTED_EDGE ( 'NONE', *, *, #17258, .F. ) ;
#21749=ORIENTED_EDGE ( 'NONE', *, *, #34956, .F. ) ;
#21755=UNCERTAINTY_MEASURE_WITH_UNIT (LENGTH_MEASURE( 1.000000000000000082E-05 ), #23818, 'distance_accuracy_value', 'NONE');
#21763=AXIS2_PLACEMENT_3D ( 'NONE', #22494, #44038, #44723 ) ;
#21764=AXIS2_PLACEMENT_3D ( 'NONE', #18826, #61954, #18118 ) ;
#21768=EDGE_LOOP ( 'NONE', ( #43042, #25031, #19305, #13066 ) ) ;
#21773=DIRECTION ( 'NONE',  ( 0.000000000000000000, 0.000000000000000000, -1.000000000000000000 ) ) ;
#21776=PLANE ( 'NONE',  #832 ) ;
#21780=VECTOR ( 'NONE', #54948, 1000.000000000000000 ) ;
#21795=CARTESIAN_POINT ( 'NONE',  ( -7.250000000000000888, 7.450000000000003730, -25.50000000000000355 ) ) ;
#21796=DIRECTION ( 'NONE',  ( 1.000000000000000000, 0.000000000000000000, 0.000000000000000000 ) ) ;
#21802=AXIS2_PLACEMENT_3D ( 'NONE', #44935, #66499, #65477 ) ;
#21809=LINE ( 'NONE', #34130, #19412 ) ;
#21813=CIRCLE ( 'NONE', #22965, 0.2000000000000005107 ) ;
#21821=EDGE_CURVE ( 'NONE', #18330, #28426, #23090, .T. ) ;
#21824=CARTESIAN_POINT ( 'NONE',  ( 7.450000000000006395, 7.250000000000000888, -15.00000000000000000 ) ) ;
#21834=CARTESIAN_POINT ( 'NONE',  ( 7.250000000000005329, -7.249999999999998224, -25.50000000000000355 ) ) ;
#21841=PLANE ( 'NONE',  #56061 ) ;
#21842=ORIENTED_EDGE ( 'NONE', *, *, #2409, .T. ) ;
#21863=EDGE_LOOP ( 'NONE', ( #15051, #2096, #16717, #23764 ) ) ;
#21865=DIRECTION ( 'NONE',  ( -1.000000000000000000, 0.000000000000000000, 0.000000000000000000 ) ) ;
#21872=EDGE_CURVE ( 'NONE', #24588, #11628, #28739, .T. ) ;
#21879=CARTESIAN_POINT ( 'NONE',  ( -7.450000000000001954, 7.250000000000000000, -13.00000000000000178 ) ) ;
#21894=ORIENTED_EDGE ( 'NONE', *, *, #63531, .F. ) ;
#21896=CARTESIAN_POINT ( 'NONE',  ( 7.250000000000005329, -7.249999999999998224, -10.00000000000000000 ) ) ;
#21900=CARTESIAN_POINT ( 'NONE',  ( -9.750000000000001776, 9.690000000000001279, -5.000000000000000000 ) ) ;
#21909=LINE ( 'NONE', #11290, #9567 ) ;
#21911=ORIENTED_EDGE ( 'NONE', *, *, #55276, .F. ) ;
#21919=EDGE_CURVE ( 'NONE', #68564, #32818, #8745, .T. ) ;
#21922=EDGE_CURVE ( 'NONE', #17131, #67314, #38892, .T. ) ;
#21923=DIRECTION ( 'NONE',  ( -1.000000000000000000, 0.000000000000000000, -0.000000000000000000 ) ) ;
#21924=EDGE_CURVE ( 'NONE', #15298, #33692, #68275, .T. ) ;
#21929=ORIENTED_EDGE ( 'NONE', *, *, #16466, .F. ) ;
#21931=CARTESIAN_POINT ( 'NONE',  ( 7.250000000000004441, 7.450000000000001954, -21.00000000000000000 ) ) ;
#21934=DIRECTION ( 'NONE',  ( -0.000000000000000000, -0.000000000000000000, 1.000000000000000000 ) ) ;
#21948=ORIENTED_EDGE ( 'NONE', *, *, #28420, .F. ) ;
#21950=CARTESIAN_POINT ( 'NONE',  ( 7.250000000000005329, 8.250000000000001776, -26.00000000000001066 ) ) ;
#21958=AXIS2_PLACEMENT_3D ( 'NONE', #1442, #59810, #11366 ) ;
#21966=CIRCLE ( 'NONE', #62572, 0.1999999999999987899 ) ;
#21968=EDGE_CURVE ( 'NONE', #25188, #3392, #15240, .T. ) ;
#21984=VERTEX_POINT ( 'NONE', #40911 ) ;
#21985=VERTEX_POINT ( 'NONE', #35242 ) ;
#21990=FACE_OUTER_BOUND ( 'NONE', #36440, .T. ) ;
#21993=CARTESIAN_POINT ( 'NONE',  ( 7.250000000000005329, -8.249999999999998224, -15.50000000000000000 ) ) ;
#21997=DIRECTION ( 'NONE',  ( 1.000000000000000000, 0.000000000000000000, 0.000000000000000000 ) ) ;
#22005=EDGE_CURVE ( 'NONE', #31165, #11267, #8390, .T. ) ;
#22007=EDGE_CURVE ( 'NONE', #33692, #43764, #35598, .T. ) ;
#22013=ORIENTED_EDGE ( 'NONE', *, *, #34321, .T. ) ;
#22014=FACE_OUTER_BOUND ( 'NONE', #2168, .T. ) ;
#22015=CIRCLE ( 'NONE', #69408, 1.000000000000000000 ) ;
#22017=LINE ( 'NONE', #48198, #9451 ) ;
#22025=ORIENTED_EDGE ( 'NONE', *, *, #38797, .T. ) ;
#22026=AXIS2_PLACEMENT_3D ( 'NONE', #55690, #29159, #1261 ) ;
#22028=CIRCLE ( 'NONE', #11851, 1.000000000000000000 ) ;
#22032=VERTEX_POINT ( 'NONE', #10835 ) ;
#22036=PLANE ( 'NONE',  #65128 ) ;
#22046=EDGE_CURVE ( 'NONE', #11939, #66346, #49024, .T. ) ;
#22051=EDGE_LOOP ( 'NONE', ( #5684, #20126, #48253, #18103 ) ) ;
#22063=FACE_OUTER_BOUND ( 'NONE', #29251, .T. ) ;
#22064=DIRECTION ( 'NONE',  ( 0.000000000000000000, 0.000000000000000000, 1.000000000000000000 ) ) ;
#22068=DIRECTION ( 'NONE',  ( -1.000000000000000000, 0.000000000000000000, 0.000000000000000000 ) ) ;
#22074=DIRECTION ( 'NONE',  ( 0.000000000000000000, 1.000000000000000000, 0.000000000000000000 ) ) ;
#22079=AXIS2_PLACEMENT_3D ( 'NONE', #68756, #13947, #35153 ) ;
#22098=ORIENTED_EDGE ( 'NONE', *, *, #58524, .F. ) ;
#22101=ORIENTED_EDGE ( 'NONE', *, *, #36219, .T. ) ;
#22102=ORIENTED_EDGE ( 'NONE', *, *, #34772, .T. ) ;
#22104=CARTESIAN_POINT ( 'NONE',  ( 7.450000000000003730, -7.249999999999997335, -15.00000000000000000 ) ) ;
#22107=DIRECTION ( 'NONE',  ( 0.000000000000000000, 0.000000000000000000, -1.000000000000000000 ) ) ;
#22113=ORIENTED_EDGE ( 'NONE', *, *, #61452, .T. ) ;
#22117=AXIS2_PLACEMENT_3D ( 'NONE', #44091, #34158, #6269 ) ;
#22118=ORIENTED_EDGE ( 'NONE', *, *, #45013, .T. ) ;
#22119=DIRECTION ( 'NONE',  ( -1.000000000000000000, 0.000000000000000000, -0.000000000000000000 ) ) ;
#22123=CARTESIAN_POINT ( 'NONE',  ( 7.250000000000005329, -8.249999999999998224, -8.500000000000000000 ) ) ;
#22127=EDGE_CURVE ( 'NONE', #35485, #61156, #51355, .T. ) ;
#22141=CARTESIAN_POINT ( 'NONE',  ( -7.250000000000000888, 7.250000000000001776, -17.50000000000000000 ) ) ;
#22148=FACE_OUTER_BOUND ( 'NONE', #4765, .T. ) ;
#22149=CIRCLE ( 'NONE', #15391, 1.000000000000000000 ) ;
#22153=CYLINDRICAL_SURFACE ( 'NONE', #26357, 0.2000000000000005107 ) ;
#22161=DIRECTION ( 'NONE',  ( -1.794541526872559352E-16, -1.000000000000000000, 0.000000000000000000 ) ) ;
#22162=ORIENTED_EDGE ( 'NONE', *, *, #64785, .F. ) ;
#22167=ORIENTED_EDGE ( 'NONE', *, *, #40222, .T. ) ;
#22172=DIRECTION ( 'NONE',  ( 1.000000000000000000, 0.000000000000000000, 0.000000000000000000 ) ) ;
#22173=EDGE_LOOP ( 'NONE', ( #23536, #34837, #42400, #49013, #32554, #58611, #31131, #15153 ) ) ;
#22184=ORIENTED_EDGE ( 'NONE', *, *, #59182, .F. ) ;
#22190=PLANE ( 'NONE',  #58980 ) ;
#22192=CARTESIAN_POINT ( 'NONE',  ( -7.250000000000001776, -7.249999999999998224, -9.500000000000001776 ) ) ;
#22196=ORIENTED_EDGE ( 'NONE', *, *, #56272, .T. ) ;
#22197=ORIENTED_EDGE ( 'NONE', *, *, #8127, .F. ) ;
#22200=VECTOR ( 'NONE', #16286, 1000.000000000000000 ) ;
#22203=CIRCLE ( 'NONE', #767, 1.000000000000000000 ) ;
#22204=AXIS2_PLACEMENT_3D ( 'NONE', #44127, #1686, #66037 ) ;
#22206=VECTOR ( 'NONE', #48111, 1000.000000000000000 ) ;
#22211=ORIENTED_EDGE ( 'NONE', *, *, #40588, .T. ) ;
#22213=CIRCLE ( 'NONE', #58368, 0.2000000000000005107 ) ;
#22215=DIRECTION ( 'NONE',  ( 0.000000000000000000, 0.000000000000000000, -1.000000000000000000 ) ) ;
#22218=CARTESIAN_POINT ( 'NONE',  ( -7.250000000000000888, 7.250000000000001776, -19.00000000000000000 ) ) ;
#22231=FACE_OUTER_BOUND ( 'NONE', #20537, .T. ) ;
#22234=EDGE_LOOP ( 'NONE', ( #47409, #66785, #16644, #64833 ) ) ;
#22236=LINE ( 'NONE', #49785, #60941 ) ;
#22238=DIRECTION ( 'NONE',  ( 0.000000000000000000, 0.000000000000000000, 1.000000000000000000 ) ) ;
#22240=DIRECTION ( 'NONE',  ( 0.000000000000000000, 0.000000000000000000, -1.000000000000000000 ) ) ;
#22243=FACE_OUTER_BOUND ( 'NONE', #32293, .T. ) ;
#22247=VECTOR ( 'NONE', #65101, 1000.000000000000000 ) ;
#22262=CARTESIAN_POINT ( 'NONE',  ( 8.250000000000005329, 0.000000000000000000, -19.50000000000000000 ) ) ;
#22271=VECTOR ( 'NONE', #24643, 1000.000000000000000 ) ;
#22274=CARTESIAN_POINT ( 'NONE',  ( -7.250000000000001776, -7.249999999999998224, -11.00000000000000000 ) ) ;
#22282=FACE_BOUND ( 'NONE', #53238, .T. ) ;
#22284=LINE ( 'NONE', #2081, #34801 ) ;
#22290=DIRECTION ( 'NONE',  ( -0.000000000000000000, -0.000000000000000000, -1.000000000000000000 ) ) ;
#22293=ORIENTED_EDGE ( 'NONE', *, *, #44266, .T. ) ;
#22299=CARTESIAN_POINT ( 'NONE',  ( 4.456444791733522252E-16, 7.450000000000002842, -7.000000000000000000 ) ) ;
#22300=VERTEX_POINT ( 'NONE', #471 ) ;
#22301=LINE ( 'NONE', #27942, #47194 ) ;
#22309=ORIENTED_EDGE ( 'NONE', *, *, #24193, .T. ) ;
#22311=EDGE_CURVE ( 'NONE', #47920, #19060, #16556, .T. ) ;
#22313=ORIENTED_EDGE ( 'NONE', *, *, #22849, .F. ) ;
#22318=DIRECTION ( 'NONE',  ( -1.000000000000000000, 0.000000000000000000, 0.000000000000000000 ) ) ;
#22323=VECTOR ( 'NONE', #24332, 1000.000000000000000 ) ;
#22334=DIRECTION ( 'NONE',  ( 0.000000000000000000, 0.000000000000000000, -1.000000000000000000 ) ) ;
#22338=VERTEX_POINT ( 'NONE', #833 ) ;
#22339=LINE ( 'NONE', #27292, #67628 ) ;
#22350=ORIENTED_EDGE ( 'NONE', *, *, #53056, .F. ) ;
#22353=FACE_OUTER_BOUND ( 'NONE', #28970, .T. ) ;
#22356=CARTESIAN_POINT ( 'NONE',  ( -7.250000000000000888, 7.250000000000001776, -19.50000000000000000 ) ) ;
#22361=EDGE_LOOP ( 'NONE', ( #5770, #33603, #1967, #7621 ) ) ;
#22363=CARTESIAN_POINT ( 'NONE',  ( 7.450000000000003730, -7.249999999999997335, -7.500000000000000000 ) ) ;
#22371=EDGE_CURVE ( 'NONE', #67986, #27724, #6469, .T. ) ;
#22383=EDGE_CURVE ( 'NONE', #47820, #57771, #54221, .T. ) ;
#22386=ORIENTED_EDGE ( 'NONE', *, *, #39087, .F. ) ;
#22400=VECTOR ( 'NONE', #33947, 1000.000000000000000 ) ;
#22403=CARTESIAN_POINT ( 'NONE',  ( 7.450000000000003730, -7.249999999999997335, -12.50000000000000000 ) ) ;
#22405=ORIENTED_EDGE ( 'NONE', *, *, #45368, .T. ) ;
#22410=VECTOR ( 'NONE', #68237, 1000.000000000000000 ) ;
#22416=PLANE ( 'NONE',  #30173 ) ;
#22418=EDGE_LOOP ( 'NONE', ( #52525, #23116, #36211, #24850, #7847, #23044, #47643, #13925 ) ) ;
#22422=FACE_OUTER_BOUND ( 'NONE', #32003, .T. ) ;
#22423=DIRECTION ( 'NONE',  ( 1.000000000000000000, 0.000000000000000000, -0.000000000000000000 ) ) ;
#22424=ORIENTED_EDGE ( 'NONE', *, *, #64835, .F. ) ;
#22431=VERTEX_POINT ( 'NONE', #10723 ) ;
#22433=DIRECTION ( 'NONE',  ( -1.000000000000000000, 0.000000000000000000, 0.000000000000000000 ) ) ;
#22444=ORIENTED_EDGE ( 'NONE', *, *, #50032, .T. ) ;
#22445=EDGE_LOOP ( 'NONE', ( #30700, #24340, #68558, #32602 ) ) ;
#22450=ORIENTED_EDGE ( 'NONE', *, *, #54969, .F. ) ;
#22465=EDGE_CURVE ( 'NONE', #44295, #13178, #61655, .T. ) ;
#22490=DIRECTION ( 'NONE',  ( 1.000000000000000000, 0.000000000000000000, 0.000000000000000000 ) ) ;
#22491=EDGE_CURVE ( 'NONE', #7579, #28918, #7827, .T. ) ;
#22493=DIRECTION ( 'NONE',  ( -0.000000000000000000, -0.000000000000000000, 1.000000000000000000 ) ) ;
#22494=CARTESIAN_POINT ( 'NONE',  ( 7.750000000000001776, 7.750000000000000000, -5.000000000000000000 ) ) ;
#22495=DIRECTION ( 'NONE',  ( 0.000000000000000000, 1.000000000000000000, -0.000000000000000000 ) ) ;
#22498=CARTESIAN_POINT ( 'NONE',  ( -7.750000000000001776, -7.348062532927999158, 5.000000000000000000 ) ) ;
#22503=DIRECTION ( 'NONE',  ( 0.000000000000000000, 0.000000000000000000, -1.000000000000000000 ) ) ;
#22506=EDGE_LOOP ( 'NONE', ( #14033, #47552, #52543, #22679 ) ) ;
#22512=ORIENTED_EDGE ( 'NONE', *, *, #17265, .T. ) ;
#22515=EDGE_LOOP ( 'NONE', ( #65305, #7699, #67205, #23741 ) ) ;
#22517=DIRECTION ( 'NONE',  ( -0.000000000000000000, -0.000000000000000000, -1.000000000000000000 ) ) ;
#22518=VERTEX_POINT ( 'NONE', #39325 ) ;
#22524=ORIENTED_EDGE ( 'NONE', *, *, #25167, .T. ) ;
#22553=PLANE ( 'NONE',  #29834 ) ;
#22564=DIRECTION ( 'NONE',  ( 0.000000000000000000, 0.000000000000000000, -1.000000000000000000 ) ) ;
#22566=LINE ( 'NONE', #45150, #11884 ) ;
#22567=ADVANCED_FACE ( 'NONE', ( #12363 ), #9086, .T. ) ;
#22571=VECTOR ( 'NONE', #30814, 1000.000000000000000 ) ;
#22572=DIRECTION ( 'NONE',  ( 0.000000000000000000, 0.000000000000000000, 1.000000000000000000 ) ) ;
#22578=PLANE ( 'NONE',  #22204 ) ;
#22580=FACE_OUTER_BOUND ( 'NONE', #68220, .T. ) ;
#22588=DIRECTION ( 'NONE',  ( -1.000000000000000000, 0.000000000000000000, 0.000000000000000000 ) ) ;
#22594=VERTEX_POINT ( 'NONE', #66131 ) ;
#22599=LINE ( 'NONE', #61096, #38074 ) ;
#22618=AXIS2_PLACEMENT_3D ( 'NONE', #37547, #48503, #53821 ) ;
#22625=LINE ( 'NONE', #17303, #40198 ) ;
#22626=ORIENTED_EDGE ( 'NONE', *, *, #64540, .F. ) ;
#22629=CARTESIAN_POINT ( 'NONE',  ( 7.250000000000005329, 7.250000000000000888, -8.500000000000000000 ) ) ;
#22633=DIRECTION ( 'NONE',  ( 0.000000000000000000, 1.000000000000000000, 0.000000000000000000 ) ) ;
#22643=DIRECTION ( 'NONE',  ( 0.000000000000000000, 0.000000000000000000, 1.000000000000000000 ) ) ;
#22646=VECTOR ( 'NONE', #28613, 1000.000000000000000 ) ;
#22652=DIRECTION ( 'NONE',  ( 0.000000000000000000, 0.000000000000000000, -1.000000000000000000 ) ) ;
#22653=EDGE_CURVE ( 'NONE', #35273, #48543, #52708, .T. ) ;
#22654=CARTESIAN_POINT ( 'NONE',  ( 7.450000000000003730, -7.249999999999997335, -19.50000000000000000 ) ) ;
#22656=EDGE_CURVE ( 'NONE', #55322, #34914, #22203, .T. ) ;
#22659=DIRECTION ( 'NONE',  ( -1.000000000000000000, 0.000000000000000000, 0.000000000000000000 ) ) ;
#22660=EDGE_CURVE ( 'NONE', #34914, #2392, #28996, .T. ) ;
#22662=AXIS2_PLACEMENT_3D ( 'NONE', #69195, #64250, #42318 ) ;
#22664=FACE_OUTER_BOUND ( 'NONE', #58395, .T. ) ;
#22671=DIRECTION ( 'NONE',  ( 0.000000000000000000, 0.000000000000000000, 1.000000000000000000 ) ) ;
#22674=CARTESIAN_POINT ( 'NONE',  ( 7.250000000000005329, -7.449999999999998401, -10.50000000000000000 ) ) ;
#22675=CARTESIAN_POINT ( 'NONE',  ( 7.250000000000005329, -7.449999999999998401, -14.50000000000000000 ) ) ;
#22679=ORIENTED_EDGE ( 'NONE', *, *, #35885, .T. ) ;
#22689=LINE ( 'NONE', #27649, #51057 ) ;
#22697=ADVANCED_FACE ( 'NONE', ( #14401 ), #35957, .F. ) ;
#22711=PLANE ( 'NONE',  #38467 ) ;
#22732=CARTESIAN_POINT ( 'NONE',  ( 7.250000000000005329, -7.249999999999998224, -8.500000000000000000 ) ) ;
#22749=ORIENTED_EDGE ( 'NONE', *, *, #48254, .F. ) ;
#22758=PLANE ( 'NONE',  #18155 ) ;
#22763=FACE_OUTER_BOUND ( 'NONE', #67659, .T. ) ;
#22767=DIRECTION ( 'NONE',  ( -0.000000000000000000, -0.000000000000000000, 1.000000000000000000 ) ) ;
#22772=PLANE ( 'NONE',  #67056 ) ;
#22773=DIRECTION ( 'NONE',  ( 0.000000000000000000, 1.000000000000000000, 0.000000000000000000 ) ) ;
#22774=ADVANCED_FACE ( 'NONE', ( #16490 ), #59626, .F. ) ;
#22775=CARTESIAN_POINT ( 'NONE',  ( 0.000000000000000000, 0.000000000000000000, 0.000000000000000000 ) ) ;
#22776=AXIS2_PLACEMENT_3D ( 'NONE', #9682, #68373, #58485 ) ;
#22778=ORIENTED_EDGE ( 'NONE', *, *, #49525, .F. ) ;
#22780=EDGE_CURVE ( 'NONE', #66616, #41194, #69536, .T. ) ;
#22782=CARTESIAN_POINT ( 'NONE',  ( 0.000000000000000000, -7.449999999999998401, -8.500000000000000000 ) ) ;
#22787=ORIENTED_EDGE ( 'NONE', *, *, #5361, .F. ) ;
#22789=EDGE_CURVE ( 'NONE', #28744, #65501, #42308, .T. ) ;
#22793=EDGE_CURVE ( 'NONE', #61464, #2063, #42661, .T. ) ;
#22802=VECTOR ( 'NONE', #45436, 1000.000000000000000 ) ;
#22810=EDGE_CURVE ( 'NONE', #1208, #8765, #5189, .T. ) ;
#22812=DIRECTION ( 'NONE',  ( 0.000000000000000000, 0.000000000000000000, -1.000000000000000000 ) ) ;
#22815=DIRECTION ( 'NONE',  ( 0.000000000000000000, 0.000000000000000000, -1.000000000000000000 ) ) ;
#22820=FACE_OUTER_BOUND ( 'NONE', #45566, .T. ) ;
#22824=DIRECTION ( 'NONE',  ( 1.000000000000000000, 0.000000000000000000, 0.000000000000000000 ) ) ;
#22834=ADVANCED_FACE ( 'NONE', ( #16136 ), #53982, .F. ) ;
#22836=VECTOR ( 'NONE', #1000, 1000.000000000000000 ) ;
#22837=EDGE_LOOP ( 'NONE', ( #36031, #46616, #5230, #7977 ) ) ;
#22840=ADVANCED_FACE ( 'NONE', ( #63542, #15098 ), #31380, .F. ) ;
#22846=ORIENTED_EDGE ( 'NONE', *, *, #32259, .T. ) ;
#22848=EDGE_CURVE ( 'NONE', #50228, #43197, #49323, .T. ) ;
#22849=EDGE_CURVE ( 'NONE', #69381, #22338, #59509, .T. ) ;
#22854=LINE ( 'NONE', #12228, #51211 ) ;
#22856=FACE_OUTER_BOUND ( 'NONE', #31496, .T. ) ;
#22859=ADVANCED_FACE ( 'NONE', ( #49701 ), #12205, .F. ) ;
#22866=VERTEX_POINT ( 'NONE', #60660 ) ;
#22870=CARTESIAN_POINT ( 'NONE',  ( 7.250000000000004441, 7.450000000000001954, -23.00000000000000000 ) ) ;
#22882=LINE ( 'NONE', #44099, #59526 ) ;
#22890=CIRCLE ( 'NONE', #45441, 0.9999999999999991118 ) ;
#22896=DIRECTION ( 'NONE',  ( 0.000000000000000000, 0.000000000000000000, -1.000000000000000000 ) ) ;
#22904=LINE ( 'NONE', #55100, #33016 ) ;
#22909=ORIENTED_EDGE ( 'NONE', *, *, #28192, .F. ) ;
#22913=ORIENTED_EDGE ( 'NONE', *, *, #6861, .T. ) ;
#22915=FACE_BOUND ( 'NONE', #59748, .T. ) ;
#22917=CARTESIAN_POINT ( 'NONE',  ( -7.250000000000001776, -7.249999999999998224, -23.50000000000000000 ) ) ;
#22921=DIRECTION ( 'NONE',  ( -1.000000000000000000, 0.000000000000000000, 0.000000000000000000 ) ) ;
#22922=AXIS2_PLACEMENT_3D ( 'NONE', #42800, #64383, #65754 ) ;
#22940=VECTOR ( 'NONE', #6348, 1000.000000000000000 ) ;
#22943=FACE_OUTER_BOUND ( 'NONE', #4166, .T. ) ;
#22947=ORIENTED_EDGE ( 'NONE', *, *, #63724, .T. ) ;
#22950=EDGE_CURVE ( 'NONE', #57065, #18463, #61689, .T. ) ;
#22960=CARTESIAN_POINT ( 'NONE',  ( -8.250000000000000000, 7.250000000000001776, -13.00000000000000178 ) ) ;
#22965=AXIS2_PLACEMENT_3D ( 'NONE', #1335, #22896, #66020 ) ;
#22977=DIRECTION ( 'NONE',  ( -1.000000000000000000, 0.000000000000000000, 0.000000000000000000 ) ) ;
#22982=CARTESIAN_POINT ( 'NONE',  ( -7.250000000000000888, 8.250000000000001776, -21.50000000000000000 ) ) ;
#22986=ORIENTED_EDGE ( 'NONE', *, *, #58161, .F. ) ;
#22987=CARTESIAN_POINT ( 'NONE',  ( -7.250000000000000000, -7.449999999999998401, -19.50000000000000000 ) ) ;
#22988=DIRECTION ( 'NONE',  ( -0.000000000000000000, -0.000000000000000000, 1.000000000000000000 ) ) ;
#22994=ADVANCED_FACE ( 'NONE', ( #67699 ), #63103, .F. ) ;
#23016=CARTESIAN_POINT ( 'NONE',  ( 7.250000000000004441, 7.450000000000001954, -20.50000000000000000 ) ) ;
#23026=ORIENTED_EDGE ( 'NONE', *, *, #51636, .T. ) ;
#23027=DIRECTION ( 'NONE',  ( -0.000000000000000000, -1.000000000000000000, -0.000000000000000000 ) ) ;
#23038=EDGE_CURVE ( 'NONE', #9556, #43562, #19981, .T. ) ;
#23040=DIRECTION ( 'NONE',  ( -1.000000000000000000, 0.000000000000000000, 0.000000000000000000 ) ) ;
#23042=ADVANCED_FACE ( 'NONE', ( #3705 ), #51795, .T. ) ;
#23044=ORIENTED_EDGE ( 'NONE', *, *, #12876, .F. ) ;
#23050=DIRECTION ( 'NONE',  ( -1.000000000000000000, 0.000000000000000000, 0.000000000000000000 ) ) ;
#23054=CARTESIAN_POINT ( 'NONE',  ( 7.250000000000005329, 7.250000000000000888, -10.50000000000000000 ) ) ;
#23057=AXIS2_PLACEMENT_3D ( 'NONE', #34016, #55257, #6801 ) ;
#23070=AXIS2_PLACEMENT_3D ( 'NONE', #3945, #8527, #13841 ) ;
#23077=DIRECTION ( 'NONE',  ( -0.000000000000000000, -0.000000000000000000, -1.000000000000000000 ) ) ;
#23084=VECTOR ( 'NONE', #33014, 1000.000000000000000 ) ;
#23086=DIRECTION ( 'NONE',  ( 0.000000000000000000, 1.000000000000000000, 0.000000000000000000 ) ) ;
#23087=DIRECTION ( 'NONE',  ( 1.000000000000000000, 0.000000000000000000, 0.000000000000000000 ) ) ;
#23090=CIRCLE ( 'NONE', #33305, 0.7499999999999997780 ) ;
#23098=CARTESIAN_POINT ( 'NONE',  ( -7.250000000000001776, -7.249999999999998224, -9.500000000000001776 ) ) ;
#23100=DIRECTION ( 'NONE',  ( -0.000000000000000000, -0.000000000000000000, 1.000000000000000000 ) ) ;
#23101=CARTESIAN_POINT ( 'NONE',  ( 0.000000000000000000, -7.449999999999998401, -15.00000000000000000 ) ) ;
#23102=ORIENTED_EDGE ( 'NONE', *, *, #64860, .F. ) ;
#23112=DIRECTION ( 'NONE',  ( -1.000000000000000000, 0.000000000000000000, 0.000000000000000000 ) ) ;
#23115=DIRECTION ( 'NONE',  ( -0.000000000000000000, -0.000000000000000000, -1.000000000000000000 ) ) ;
#23116=ORIENTED_EDGE ( 'NONE', *, *, #6972, .F. ) ;
#23118=ORIENTED_EDGE ( 'NONE', *, *, #11126, .T. ) ;
#23124=ADVANCED_FACE ( 'NONE', ( #30926, #68763 ), #52498, .T. ) ;
#23130=DIRECTION ( 'NONE',  ( -1.000000000000000000, 0.000000000000000000, 0.000000000000000000 ) ) ;
#23132=PLANE ( 'NONE',  #36962 ) ;
#23138=PLANE ( 'NONE',  #13047 ) ;
#23146=CARTESIAN_POINT ( 'NONE',  ( 6.749999999999996447, -7.348062532928000934, 5.000000000000000000 ) ) ;
#23150=AXIS2_PLACEMENT_3D ( 'NONE', #45541, #62155, #28938 ) ;
#23161=COLOUR_RGB ( '', 0.40784314, 0.44705882, 0.49803922) ;
#23172=LINE ( 'NONE', #17873, #69398 ) ;
#23179=EDGE_CURVE ( 'NONE', #66712, #26265, #42581, .T. ) ;
#23182=VERTEX_POINT ( 'NONE', #25983 ) ;
#23183=EDGE_CURVE ( 'NONE', #49229, #41582, #52766, .T. ) ;
#23184=CARTESIAN_POINT ( 'NONE',  ( -7.750000000000001776, 7.750000000000001776, 5.000000000000000000 ) ) ;
#23186=ORIENTED_EDGE ( 'NONE', *, *, #43721, .F. ) ;
#23197=CARTESIAN_POINT ( 'NONE',  ( 7.250000000000005329, 7.250000000000000888, -11.00000000000000000 ) ) ;
#23198=VECTOR ( 'NONE', #44005, 1000.000000000000000 ) ;
#23217=VECTOR ( 'NONE', #55174, 1000.000000000000000 ) ;
#23219=ADVANCED_FACE ( 'NONE', ( #48588 ), #10066, .T. ) ;
#23220=CARTESIAN_POINT ( 'NONE',  ( -7.250000000000000000, -7.449999999999998401, -25.00000000000000000 ) ) ;
#23221=CARTESIAN_POINT ( 'NONE',  ( -8.250000000000001776, 7.250000000000000888, -26.00000000000001066 ) ) ;
#23226=EDGE_CURVE ( 'NONE', #39124, #34907, #26674, .T. ) ;
#23230=ORIENTED_EDGE ( 'NONE', *, *, #40947, .T. ) ;
#23237=CIRCLE ( 'NONE', #62768, 1.500000000000000444 ) ;
#23238=DIRECTION ( 'NONE',  ( -1.000000000000000000, 0.000000000000000000, 0.000000000000000000 ) ) ;
#23241=CARTESIAN_POINT ( 'NONE',  ( 7.250000000000005329, -7.449999999999998401, -25.50000000000000355 ) ) ;
#23246=VECTOR ( 'NONE', #1144, 1000.000000000000000 ) ;
#23253=LINE ( 'NONE', #65366, #26230 ) ;
#23256=DIRECTION ( 'NONE',  ( 0.000000000000000000, 0.000000000000000000, 1.000000000000000000 ) ) ;
#23262=DIRECTION ( 'NONE',  ( 1.000000000000000000, 0.000000000000000000, 0.000000000000000000 ) ) ;
#23263=EDGE_CURVE ( 'NONE', #35740, #23540, #55618, .T. ) ;
#23264=CARTESIAN_POINT ( 'NONE',  ( 7.450000000000004619, -1.336933437520057563E-15, -24.00000000000000000 ) ) ;
#23266=EDGE_CURVE ( 'NONE', #29173, #54436, #28389, .T. ) ;
#23276=EDGE_LOOP ( 'NONE', ( #63397, #26318, #18335, #6459 ) ) ;
#23277=VERTEX_POINT ( 'NONE', #16762 ) ;
#23291=AXIS2_PLACEMENT_3D ( 'NONE', #64869, #54262, #37650 ) ;
#23297=EDGE_LOOP ( 'NONE', ( #60413, #9232, #46862, #54305 ) ) ;
#23300=VECTOR ( 'NONE', #64085, 1000.000000000000000 ) ;
#23308=DIRECTION ( 'NONE',  ( 0.000000000000000000, -1.000000000000000000, 0.000000000000000000 ) ) ;
#23309=ADVANCED_FACE ( 'NONE', ( #37987 ), #22416, .F. ) ;
#23312=LINE ( 'NONE', #50179, #61313 ) ;
#23322=VERTEX_POINT ( 'NONE', #65208 ) ;
#23324=VERTEX_POINT ( 'NONE', #11777 ) ;
#23338=LINE ( 'NONE', #1764, #62669 ) ;
#23339=ORIENTED_EDGE ( 'NONE', *, *, #55276, .T. ) ;
#23343=ADVANCED_FACE ( 'NONE', ( #22063 ), #43631, .F. ) ;
#23347=LINE ( 'NONE', #27614, #48649 ) ;
#23348=ORIENTED_EDGE ( 'NONE', *, *, #63563, .T. ) ;
#23350=DIRECTION ( 'NONE',  ( 0.000000000000000000, 0.000000000000000000, -1.000000000000000000 ) ) ;
#23356=AXIS2_PLACEMENT_3D ( 'NONE', #34457, #14321, #57444 ) ;
#23357=PLANE ( 'NONE',  #65861 ) ;
#23364=AXIS2_PLACEMENT_3D ( 'NONE', #27946, #38227, #59778 ) ;
#23372=VERTEX_POINT ( 'NONE', #39693 ) ;
#23377=CYLINDRICAL_SURFACE ( 'NONE', #52286, 1.000000000000001776 ) ;
#23379=DIRECTION ( 'NONE',  ( -1.000000000000000000, 0.000000000000000000, 0.000000000000000000 ) ) ;
#23380=DIRECTION ( 'NONE',  ( 0.000000000000000000, -1.000000000000000000, -0.000000000000000000 ) ) ;
#23384=ORIENTED_EDGE ( 'NONE', *, *, #20985, .T. ) ;
#23394=CARTESIAN_POINT ( 'NONE',  ( 7.450000000000003730, -7.249999999999997335, -19.50000000000000000 ) ) ;
#23397=EDGE_CURVE ( 'NONE', #58971, #66435, #27908, .T. ) ;
#23402=VECTOR ( 'NONE', #53962, 1000.000000000000000 ) ;
#23405=EDGE_CURVE ( 'NONE', #47564, #7150, #67625, .T. ) ;
#23411=CARTESIAN_POINT ( 'NONE',  ( 7.250000000000005329, -7.249999999999998224, -23.50000000000000000 ) ) ;
#23419=DIRECTION ( 'NONE',  ( 0.000000000000000000, 0.000000000000000000, 1.000000000000000000 ) ) ;
#23422=CARTESIAN_POINT ( 'NONE',  ( 7.450000000000003730, -7.249999999999997335, -16.00000000000000000 ) ) ;
#23424=CARTESIAN_POINT ( 'NONE',  ( 7.250000000000004441, 7.450000000000001954, -18.50000000000000000 ) ) ;
#23436=PLANE ( 'NONE',  #26619 ) ;
#23438=PLANE ( 'NONE',  #21764 ) ;
#23439=EDGE_LOOP ( 'NONE', ( #10268, #7112, #50658, #18343 ) ) ;
#23440=CARTESIAN_POINT ( 'NONE',  ( -9.189999999999999503, 9.750000000000000000, -5.000000000000000000 ) ) ;
#23456=VECTOR ( 'NONE', #27676, 1000.000000000000000 ) ;
#23460=DIRECTION ( 'NONE',  ( -1.000000000000000000, 0.000000000000000000, 0.000000000000000000 ) ) ;
#23466=ORIENTED_EDGE ( 'NONE', *, *, #15952, .F. ) ;
#23467=VERTEX_POINT ( 'NONE', #3269 ) ;
#23480=EDGE_CURVE ( 'NONE', #127, #33326, #19525, .T. ) ;
#23484=DIRECTION ( 'NONE',  ( 0.000000000000000000, 0.000000000000000000, -1.000000000000000000 ) ) ;
#23485=EDGE_CURVE ( 'NONE', #9508, #26490, #16665, .T. ) ;
#23492=LINE ( 'NONE', #13577, #38165 ) ;
#23498=CYLINDRICAL_SURFACE ( 'NONE', #63908, 1.000000000000000000 ) ;
#23522=DIRECTION ( 'NONE',  ( -1.000000000000000000, 0.000000000000000000, 0.000000000000000000 ) ) ;
#23527=DIRECTION ( 'NONE',  ( 1.000000000000000000, 0.000000000000000000, 0.000000000000000000 ) ) ;
#23536=ORIENTED_EDGE ( 'NONE', *, *, #53073, .T. ) ;
#23538=ORIENTED_EDGE ( 'NONE', *, *, #35555, .F. ) ;
#23540=VERTEX_POINT ( 'NONE', #36866 ) ;
#23545=PLANE ( 'NONE',  #51924 ) ;
#23561=CARTESIAN_POINT ( 'NONE',  ( -8.250000000000001776, -8.249999999999998224, -26.00000000000001066 ) ) ;
#23584=CARTESIAN_POINT ( 'NONE',  ( 7.450000000000004619, -1.336933437520057563E-15, -25.50000000000000355 ) ) ;
#23593=CARTESIAN_POINT ( 'NONE',  ( -7.250000000000000000, -7.449999999999998401, -23.50000000000000000 ) ) ;
#23598=CIRCLE ( 'NONE', #20233, 0.2000000000000005107 ) ;
#23635=CARTESIAN_POINT ( 'NONE',  ( -7.250000000000000888, -8.249999999999998224, -9.000000000000001776 ) ) ;
#23638=VERTEX_POINT ( 'NONE', #21290 ) ;
#23644=VECTOR ( 'NONE', #59439, 1000.000000000000000 ) ;
#23645=DIRECTION ( 'NONE',  ( -1.000000000000000000, 0.000000000000000000, 0.000000000000000000 ) ) ;
#23650=CARTESIAN_POINT ( 'NONE',  ( 8.250000000000005329, 7.250000000000000888, -14.00000000000000000 ) ) ;
#23668=CARTESIAN_POINT ( 'NONE',  ( -8.250000000000001776, -7.249999999999998224, -26.00000000000001066 ) ) ;
#23678=ORIENTED_EDGE ( 'NONE', *, *, #19906, .T. ) ;
#23680=DIRECTION ( 'NONE',  ( 0.000000000000000000, 0.000000000000000000, -1.000000000000000000 ) ) ;
#23691=CARTESIAN_POINT ( 'NONE',  ( 8.250000000000005329, -8.249999999999998224, -26.00000000000001066 ) ) ;
#23695=ORIENTED_EDGE ( 'NONE', *, *, #9660, .T. ) ;
#23696=EDGE_CURVE ( 'NONE', #48304, #23277, #44563, .T. ) ;
#23698=AXIS2_PLACEMENT_3D ( 'NONE', #31454, #26140, #53019 ) ;
#23700=EDGE_CURVE ( 'NONE', #66129, #7579, #35874, .T. ) ;
#23704=DIRECTION ( 'NONE',  ( 0.000000000000000000, 0.000000000000000000, -1.000000000000000000 ) ) ;
#23708=CIRCLE ( 'NONE', #63245, 0.1999999999999996503 ) ;
#23734=EDGE_CURVE ( 'NONE', #29129, #26202, #55196, .T. ) ;
#23741=ORIENTED_EDGE ( 'NONE', *, *, #16783, .F. ) ;
#23743=EDGE_CURVE ( 'NONE', #18330, #20587, #6743, .T. ) ;
#23745=AXIS2_PLACEMENT_3D ( 'NONE', #32558, #48461, #21592 ) ;
#23756=DIRECTION ( 'NONE',  ( 1.000000000000000000, -0.000000000000000000, 0.000000000000000000 ) ) ;
#23759=DIRECTION ( 'NONE',  ( -1.000000000000000000, 1.794541526872559352E-16, 0.000000000000000000 ) ) ;
#23760=AXIS2_PLACEMENT_3D ( 'NONE', #23878, #24927, #67706 ) ;
#23762=PLANE ( 'NONE',  #65431 ) ;
#23763=CIRCLE ( 'NONE', #33900, 0.2000000000000005107 ) ;
#23764=ORIENTED_EDGE ( 'NONE', *, *, #8445, .T. ) ;
#23776=ORIENTED_EDGE ( 'NONE', *, *, #13487, .T. ) ;
#23788=CYLINDRICAL_SURFACE ( 'NONE', #44363, 1.000000000000000000 ) ;
#23799=ORIENTED_EDGE ( 'NONE', *, *, #4814, .F. ) ;
#23804=CARTESIAN_POINT ( 'NONE',  ( -8.250000000000001776, -7.249999999999998224, -23.00000000000000000 ) ) ;
#23810=CIRCLE ( 'NONE', #30581, 0.7499999999999997780 ) ;
#23818=( LENGTH_UNIT ( ) NAMED_UNIT ( * ) SI_UNIT ( .MILLI., .METRE. ) );
#23825=EDGE_LOOP ( 'NONE', ( #32071, #16882, #5939, #62904 ) ) ;
#23832=DIRECTION ( 'NONE',  ( -1.000000000000000000, 1.794541526872559352E-16, 0.000000000000000000 ) ) ;
#23835=DIRECTION ( 'NONE',  ( -0.000000000000000000, -0.000000000000000000, -1.000000000000000000 ) ) ;
#23840=DIRECTION ( 'NONE',  ( -1.000000000000000000, 0.000000000000000000, 0.000000000000000000 ) ) ;
#23863=CARTESIAN_POINT ( 'NONE',  ( 6.500000000000000888, -6.500000000000002665, -1.000000000000000000 ) ) ;
#23878=CARTESIAN_POINT ( 'NONE',  ( -7.250000000000000888, 7.250000000000001776, -12.50000000000000000 ) ) ;
#23881=DIRECTION ( 'NONE',  ( 0.000000000000000000, 0.000000000000000000, 1.000000000000000000 ) ) ;
#23883=EDGE_CURVE ( 'NONE', #14054, #61969, #31456, .T. ) ;
#23885=VECTOR ( 'NONE', #42274, 1000.000000000000000 ) ;
#23894=VECTOR ( 'NONE', #45574, 1000.000000000000000 ) ;
#23897=CARTESIAN_POINT ( 'NONE',  ( 0.000000000000000000, 0.000000000000000000, -14.50000000000000000 ) ) ;
#23912=LINE ( 'NONE', #51129, #59367 ) ;
#23920=EDGE_CURVE ( 'NONE', #53694, #56954, #21252, .T. ) ;
#23922=DIRECTION ( 'NONE',  ( 0.000000000000000000, 0.000000000000000000, -1.000000000000000000 ) ) ;
#23924=CYLINDRICAL_SURFACE ( 'NONE', #10939, 1.000000000000000000 ) ;
#23929=VERTEX_POINT ( 'NONE', #25820 ) ;
#23943=VECTOR ( 'NONE', #1460, 1000.000000000000000 ) ;
#23947=CARTESIAN_POINT ( 'NONE',  ( 0.000000000000000000, -8.249999999999998224, -24.00000000000000000 ) ) ;
#23949=PLANE ( 'NONE',  #7411 ) ;
#23953=DIRECTION ( 'NONE',  ( -1.000000000000000000, 0.000000000000000000, 0.000000000000000000 ) ) ;
#23954=EDGE_CURVE ( 'NONE', #43073, #13160, #42066, .T. ) ;
#23963=DIRECTION ( 'NONE',  ( -1.000000000000000000, 0.000000000000000000, 0.000000000000000000 ) ) ;
#23964=VECTOR ( 'NONE', #42745, 1000.000000000000000 ) ;
#23966=CARTESIAN_POINT ( 'NONE',  ( -7.450000000000001954, 7.250000000000000000, -24.00000000000000000 ) ) ;
#23968=VERTEX_POINT ( 'NONE', #64005 ) ;
#23973=EDGE_CURVE ( 'NONE', #19060, #34012, #31479, .T. ) ;
#23975=DIRECTION ( 'NONE',  ( -1.794541526872559352E-16, -1.000000000000000000, 0.000000000000000000 ) ) ;
#23980=FACE_OUTER_BOUND ( 'NONE', #30421, .T. ) ;
#23982=CARTESIAN_POINT ( 'NONE',  ( 7.250000000000005329, 8.250000000000001776, -11.00000000000000000 ) ) ;
#23995=CARTESIAN_POINT ( 'NONE',  ( 7.250000000000005329, -7.449999999999998401, -14.00000000000000000 ) ) ;
#23996=FACE_BOUND ( 'NONE', #52956, .T. ) ;
#23997=ORIENTED_EDGE ( 'NONE', *, *, #39676, .T. ) ;
#23999=DIRECTION ( 'NONE',  ( -1.000000000000000000, 0.000000000000000000, 0.000000000000000000 ) ) ;
#24000=DIRECTION ( 'NONE',  ( 0.000000000000000000, 0.000000000000000000, 1.000000000000000000 ) ) ;
#24006=FACE_OUTER_BOUND ( 'NONE', #38668, .T. ) ;
#24016=EDGE_CURVE ( 'NONE', #35816, #39001, #68946, .T. ) ;
#24022=LINE ( 'NONE', #45233, #23217 ) ;
#24023=LINE ( 'NONE', #14115, #52546 ) ;
#24024=ORIENTED_EDGE ( 'NONE', *, *, #21872, .T. ) ;
#24030=LINE ( 'NONE', #36044, #27211 ) ;
#24033=DIRECTION ( 'NONE',  ( -1.000000000000000000, 0.000000000000000000, 0.000000000000000000 ) ) ;
#24035=VECTOR ( 'NONE', #24206, 1000.000000000000000 ) ;
#24054=ORIENTED_EDGE ( 'NONE', *, *, #4386, .F. ) ;
#24058=LINE ( 'NONE', #13800, #4448 ) ;
#24060=VECTOR ( 'NONE', #27994, 1000.000000000000000 ) ;
#24061=CARTESIAN_POINT ( 'NONE',  ( -7.250000000000000888, 7.250000000000001776, -18.50000000000000000 ) ) ;
#24066=DIRECTION ( 'NONE',  ( 0.000000000000000000, 1.000000000000000000, 0.000000000000000000 ) ) ;
#24069=ORIENTED_EDGE ( 'NONE', *, *, #847, .T. ) ;
#24070=DIRECTION ( 'NONE',  ( 1.000000000000000000, 0.000000000000000000, 0.000000000000000000 ) ) ;
#24075=AXIS2_PLACEMENT_3D ( 'NONE', #34178, #55769, #44798 ) ;
#24085=EDGE_CURVE ( 'NONE', #46497, #59150, #54085, .T. ) ;
#24100=CARTESIAN_POINT ( 'NONE',  ( -7.250000000000000888, 7.250000000000001776, -9.000000000000001776 ) ) ;
#24115=CIRCLE ( 'NONE', #39749, 0.9999999999999991118 ) ;
#24134=CARTESIAN_POINT ( 'NONE',  ( -7.250000000000000888, 7.250000000000001776, -21.00000000000000000 ) ) ;
#24148=VERTEX_POINT ( 'NONE', #11609 ) ;
#24151=CARTESIAN_POINT ( 'NONE',  ( 7.250000000000005329, 8.250000000000001776, -26.00000000000001066 ) ) ;
#24177=EDGE_CURVE ( 'NONE', #59322, #11827, #11951, .T. ) ;
#24178=ORIENTED_EDGE ( 'NONE', *, *, #49204, .F. ) ;
#24186=DIRECTION ( 'NONE',  ( 0.000000000000000000, 0.000000000000000000, 1.000000000000000000 ) ) ;
#24187=CARTESIAN_POINT ( 'NONE',  ( -8.250000000000001776, 7.250000000000000888, -9.500000000000001776 ) ) ;
#24190=ORIENTED_EDGE ( 'NONE', *, *, #68107, .T. ) ;
#24192=VERTEX_POINT ( 'NONE', #50828 ) ;
#24193=EDGE_CURVE ( 'NONE', #46075, #69141, #26907, .T. ) ;
#24201=DIRECTION ( 'NONE',  ( -0.000000000000000000, 0.000000000000000000, 1.000000000000000000 ) ) ;
#24203=EDGE_CURVE ( 'NONE', #21453, #56437, #3109, .T. ) ;
#24206=DIRECTION ( 'NONE',  ( -0.000000000000000000, -0.000000000000000000, 1.000000000000000000 ) ) ;
#24209=EDGE_CURVE ( 'NONE', #5145, #12839, #44949, .T. ) ;
#24213=ADVANCED_FACE ( 'NONE', ( #2398 ), #39863, .T. ) ;
#24223=AXIS2_PLACEMENT_3D ( 'NONE', #17023, #49885, #32935 ) ;
#24224=ORIENTED_EDGE ( 'NONE', *, *, #33690, .F. ) ;
#24239=ORIENTED_EDGE ( 'NONE', *, *, #15841, .T. ) ;
#24249=ORIENTED_EDGE ( 'NONE', *, *, #19924, .T. ) ;
#24252=CARTESIAN_POINT ( 'NONE',  ( -7.450000000000001954, 0.000000000000000000, -17.50000000000000000 ) ) ;
#24266=ORIENTED_EDGE ( 'NONE', *, *, #69411, .T. ) ;
#24268=ORIENTED_EDGE ( 'NONE', *, *, #66981, .T. ) ;
#24273=CARTESIAN_POINT ( 'NONE',  ( 8.250000000000005329, 7.250000000000000888, -19.50000000000000000 ) ) ;
#24277=CARTESIAN_POINT ( 'NONE',  ( 7.250000000000005329, -7.249999999999998224, -7.500000000000000000 ) ) ;
#24279=DIRECTION ( 'NONE',  ( 1.000000000000000000, 0.000000000000000000, 0.000000000000000000 ) ) ;
#24293=CARTESIAN_POINT ( 'NONE',  ( -7.250000000000001776, -7.249999999999998224, -7.500000000000000000 ) ) ;
#24296=DIRECTION ( 'NONE',  ( 0.000000000000000000, 1.000000000000000000, 0.000000000000000000 ) ) ;
#24332=DIRECTION ( 'NONE',  ( 0.000000000000000000, 1.000000000000000000, 0.000000000000000000 ) ) ;
#24334=DIRECTION ( 'NONE',  ( 1.000000000000000000, 0.000000000000000000, 0.000000000000000000 ) ) ;
#24337=CARTESIAN_POINT ( 'NONE',  ( 9.690000000000001279, -9.690000000000001279, -5.000000000000000000 ) ) ;
#24340=ORIENTED_EDGE ( 'NONE', *, *, #3922, .T. ) ;
#24349=EDGE_LOOP ( 'NONE', ( #39333, #65661, #48169, #65250 ) ) ;
#24358=DIRECTION ( 'NONE',  ( -1.000000000000000000, 0.000000000000000000, 0.000000000000000000 ) ) ;
#24364=DIRECTION ( 'NONE',  ( -1.000000000000000000, 0.000000000000000000, 0.000000000000000000 ) ) ;
#24385=VECTOR ( 'NONE', #34364, 1000.000000000000000 ) ;
#24395=DIRECTION ( 'NONE',  ( 1.000000000000000000, 0.000000000000000000, 0.000000000000000000 ) ) ;
#24397=CARTESIAN_POINT ( 'NONE',  ( 7.250000000000005329, 7.250000000000000888, -23.50000000000000000 ) ) ;
#24400=DIRECTION ( 'NONE',  ( 1.000000000000000000, 0.000000000000000000, 0.000000000000000000 ) ) ;
#24406=EDGE_CURVE ( 'NONE', #35196, #7192, #58557, .T. ) ;
#24413=ORIENTED_EDGE ( 'NONE', *, *, #28802, .F. ) ;
#24414=DIRECTION ( 'NONE',  ( 0.000000000000000000, 0.000000000000000000, 1.000000000000000000 ) ) ;
#24421=DIRECTION ( 'NONE',  ( 0.000000000000000000, 0.000000000000000000, 1.000000000000000000 ) ) ;
#24428=CIRCLE ( 'NONE', #63966, 0.1999999999999987899 ) ;
#24432=CARTESIAN_POINT ( 'NONE',  ( -7.450000000000001954, 0.000000000000000000, -25.50000000000000355 ) ) ;
#24438=VECTOR ( 'NONE', #41258, 1000.000000000000000 ) ;
#24442=FACE_BOUND ( 'NONE', #41404, .T. ) ;
#24461=AXIS2_PLACEMENT_3D ( 'NONE', #46759, #8931, #19194 ) ;
#24471=EDGE_CURVE ( 'NONE', #33622, #20378, #53307, .T. ) ;
#24480=CARTESIAN_POINT ( 'NONE',  ( 7.250000000000005329, -8.249999999999998224, -14.50000000000000000 ) ) ;
#24491=ORIENTED_EDGE ( 'NONE', *, *, #7420, .F. ) ;
#24495=DIRECTION ( 'NONE',  ( -0.000000000000000000, -0.000000000000000000, -1.000000000000000000 ) ) ;
#24498=DIRECTION ( 'NONE',  ( 0.000000000000000000, -1.000000000000000000, -0.000000000000000000 ) ) ;
#24505=DIRECTION ( 'NONE',  ( 0.000000000000000000, 0.000000000000000000, -1.000000000000000000 ) ) ;
#24511=ADVANCED_FACE ( 'NONE', ( #43368 ), #10847, .T. ) ;
#24518=ORIENTED_EDGE ( 'NONE', *, *, #50520, .T. ) ;
#24519=EDGE_CURVE ( 'NONE', #10256, #44295, #59289, .T. ) ;
#24527=VERTEX_POINT ( 'NONE', #39020 ) ;
#24533=VERTEX_POINT ( 'NONE', #39705 ) ;
#24546=FACE_OUTER_BOUND ( 'NONE', #9118, .T. ) ;
#24568=CIRCLE ( 'NONE', #7590, 1.000000000000000000 ) ;
#24570=FACE_OUTER_BOUND ( 'NONE', #47753, .T. ) ;
#24573=ORIENTED_EDGE ( 'NONE', *, *, #20699, .F. ) ;
#24574=CARTESIAN_POINT ( 'NONE',  ( -7.450000000000001954, 0.000000000000000000, -9.500000000000001776 ) ) ;
#24575=CARTESIAN_POINT ( 'NONE',  ( -7.250000000000000888, 7.450000000000003730, -24.50000000000000000 ) ) ;
#24581=ORIENTED_EDGE ( 'NONE', *, *, #37549, .T. ) ;
#24582=CARTESIAN_POINT ( 'NONE',  ( -7.250000000000001776, -7.249999999999998224, -15.00000000000000000 ) ) ;
#24586=CARTESIAN_POINT ( 'NONE',  ( 7.250000000000005329, -8.249999999999998224, -25.00000000000000000 ) ) ;
#24588=VERTEX_POINT ( 'NONE', #246 ) ;
#24605=LINE ( 'NONE', #56077, #7142 ) ;
#24612=LINE ( 'NONE', #67735, #50461 ) ;
#24617=ORIENTED_EDGE ( 'NONE', *, *, #66657, .T. ) ;
#24619=EDGE_CURVE ( 'NONE', #34317, #22594, #60791, .T. ) ;
#24622=DIRECTION ( 'NONE',  ( 0.000000000000000000, 1.000000000000000000, 0.000000000000000000 ) ) ;
#24627=CARTESIAN_POINT ( 'NONE',  ( 0.000000000000000000, -7.449999999999998401, -10.50000000000000000 ) ) ;
#24634=DIRECTION ( 'NONE',  ( 0.000000000000000000, 0.000000000000000000, -1.000000000000000000 ) ) ;
#24643=DIRECTION ( 'NONE',  ( 1.000000000000000000, -0.000000000000000000, 0.000000000000000000 ) ) ;
#24645=DIRECTION ( 'NONE',  ( 1.000000000000000000, 0.000000000000000000, 0.000000000000000000 ) ) ;
#24649=DIRECTION ( 'NONE',  ( -1.000000000000000000, 0.000000000000000000, 0.000000000000000000 ) ) ;
#24654=DIRECTION ( 'NONE',  ( 1.000000000000000000, 0.000000000000000000, 0.000000000000000000 ) ) ;
#24671=ORIENTED_EDGE ( 'NONE', *, *, #27336, .T. ) ;
#24672=EDGE_CURVE ( 'NONE', #34593, #31382, #2581, .T. ) ;
#24674=CIRCLE ( 'NONE', #59704, 0.2000000000000005107 ) ;
#24676=ORIENTED_EDGE ( 'NONE', *, *, #22046, .F. ) ;
#24679=EDGE_CURVE ( 'NONE', #48765, #68595, #39343, .T. ) ;
#24692=ORIENTED_EDGE ( 'NONE', *, *, #17512, .T. ) ;
#24695=ORIENTED_EDGE ( 'NONE', *, *, #64605, .T. ) ;
#24696=EDGE_CURVE ( 'NONE', #24963, #33875, #62671, .T. ) ;
#24702=LINE ( 'NONE', #14086, #44118 ) ;
#24705=CARTESIAN_POINT ( 'NONE',  ( -10.50000000000000178, 9.690000000000001279, -4.250000000000000000 ) ) ;
#24706=ORIENTED_EDGE ( 'NONE', *, *, #18507, .T. ) ;
#24714=ADVANCED_FACE ( 'NONE', ( #40041 ), #61974, .F. ) ;
#24719=VERTEX_POINT ( 'NONE', #52074 ) ;
#24733=VECTOR ( 'NONE', #18630, 1000.000000000000000 ) ;
#24737=DIRECTION ( 'NONE',  ( 0.000000000000000000, 0.000000000000000000, -1.000000000000000000 ) ) ;
#24740=ORIENTED_EDGE ( 'NONE', *, *, #50614, .F. ) ;
#24744=ORIENTED_EDGE ( 'NONE', *, *, #36231, .T. ) ;
#24758=VECTOR ( 'NONE', #22773, 1000.000000000000000 ) ;
#24761=ORIENTED_EDGE ( 'NONE', *, *, #51593, .T. ) ;
#24762=ADVANCED_FACE ( 'NONE', ( #68700 ), #26255, .F. ) ;
#24769=EDGE_LOOP ( 'NONE', ( #25819, #4797, #43668, #27058 ) ) ;
#24770=DIRECTION ( 'NONE',  ( 1.000000000000000000, 0.000000000000000000, 0.000000000000000000 ) ) ;
#24778=LINE ( 'NONE', #68258, #16325 ) ;
#24781=DIRECTION ( 'NONE',  ( 0.000000000000000000, 0.000000000000000000, -1.000000000000000000 ) ) ;
#24784=VERTEX_POINT ( 'NONE', #5033 ) ;
#24788=FACE_OUTER_BOUND ( 'NONE', #34151, .T. ) ;
#24794=VERTEX_POINT ( 'NONE', #3991 ) ;
#24797=DIRECTION ( 'NONE',  ( 1.000000000000000000, 0.000000000000000000, 0.000000000000000000 ) ) ;
#24798=ORIENTED_EDGE ( 'NONE', *, *, #34476, .T. ) ;
#24805=ORIENTED_EDGE ( 'NONE', *, *, #47778, .T. ) ;
#24809=DIRECTION ( 'NONE',  ( -1.000000000000000000, 0.000000000000000000, 0.000000000000000000 ) ) ;
#24817=VECTOR ( 'NONE', #11868, 1000.000000000000000 ) ;
#24826=VERTEX_POINT ( 'NONE', #10681 ) ;
#24839=CARTESIAN_POINT ( 'NONE',  ( -8.250000000000001776, 0.000000000000000000, -21.50000000000000000 ) ) ;
#24840=CIRCLE ( 'NONE', #42913, 0.1999999999999996503 ) ;
#24843=DIRECTION ( 'NONE',  ( -1.000000000000000000, 0.000000000000000000, 0.000000000000000000 ) ) ;
#24844=DIRECTION ( 'NONE',  ( -1.794541526872559352E-16, -1.000000000000000000, 0.000000000000000000 ) ) ;
#24850=ORIENTED_EDGE ( 'NONE', *, *, #65663, .F. ) ;
#24859=ORIENTED_EDGE ( 'NONE', *, *, #66500, .F. ) ;
#24862=ORIENTED_EDGE ( 'NONE', *, *, #51681, .F. ) ;
#24868=VECTOR ( 'NONE', #36309, 1000.000000000000000 ) ;
#24870=ORIENTED_EDGE ( 'NONE', *, *, #61649, .T. ) ;
#24877=EDGE_LOOP ( 'NONE', ( #17718, #26543, #3737, #33962 ) ) ;
#24882=DIRECTION ( 'NONE',  ( 0.000000000000000000, 0.000000000000000000, 1.000000000000000000 ) ) ;
#24883=ORIENTED_EDGE ( 'NONE', *, *, #45821, .T. ) ;
#24893=AXIS2_PLACEMENT_3D ( 'NONE', #27830, #43743, #60690 ) ;
#24897=LINE ( 'NONE', #57420, #45153 ) ;
#24898=ORIENTED_EDGE ( 'NONE', *, *, #63069, .F. ) ;
#24899=CARTESIAN_POINT ( 'NONE',  ( 7.450000000000004619, -1.336933437520057563E-15, -9.000000000000001776 ) ) ;
#24903=ORIENTED_EDGE ( 'NONE', *, *, #10326, .F. ) ;
#24913=AXIS2_PLACEMENT_3D ( 'NONE', #41755, #63333, #37175 ) ;
#24927=DIRECTION ( 'NONE',  ( 0.000000000000000000, 0.000000000000000000, -1.000000000000000000 ) ) ;
#24939=DIRECTION ( 'NONE',  ( 0.000000000000000000, 0.000000000000000000, -1.000000000000000000 ) ) ;
#24940=EDGE_CURVE ( 'NONE', #40904, #5241, #43896, .T. ) ;
#24955=DIRECTION ( 'NONE',  ( -1.000000000000000000, 0.000000000000000000, 0.000000000000000000 ) ) ;
#24957=VERTEX_POINT ( 'NONE', #66156 ) ;
#24960=DIRECTION ( 'NONE',  ( -0.000000000000000000, -0.000000000000000000, 1.000000000000000000 ) ) ;
#24961=AXIS2_PLACEMENT_3D ( 'NONE', #67846, #40618, #24358 ) ;
#24963=VERTEX_POINT ( 'NONE', #38604 ) ;
#24980=CYLINDRICAL_SURFACE ( 'NONE', #36848, 1.000000000000000000 ) ;
#24982=DIRECTION ( 'NONE',  ( 0.000000000000000000, 0.000000000000000000, -1.000000000000000000 ) ) ;
#24987=CIRCLE ( 'NONE', #4711, 1.000000000000000000 ) ;
#24994=LINE ( 'NONE', #66720, #58755 ) ;
#25004=DIRECTION ( 'NONE',  ( 1.000000000000000000, 0.000000000000000000, 0.000000000000000000 ) ) ;
#25005=DIRECTION ( 'NONE',  ( 0.000000000000000000, 0.000000000000000000, 1.000000000000000000 ) ) ;
#25006=ADVANCED_FACE ( 'NONE', ( #21990 ), #59820, .F. ) ;
#25031=ORIENTED_EDGE ( 'NONE', *, *, #34150, .F. ) ;
#25034=EDGE_CURVE ( 'NONE', #62579, #66346, #24058, .T. ) ;
#25040=DIRECTION ( 'NONE',  ( 1.334402673828312846E-16, 1.000000000000000000, 0.000000000000000000 ) ) ;
#25057=ORIENTED_EDGE ( 'NONE', *, *, #23266, .F. ) ;
#25080=AXIS2_PLACEMENT_3D ( 'NONE', #16932, #40485, #29174 ) ;
#25081=DIRECTION ( 'NONE',  ( 0.000000000000000000, 1.000000000000000000, 0.000000000000000000 ) ) ;
#25090=DIRECTION ( 'NONE',  ( 0.000000000000000000, 0.000000000000000000, 1.000000000000000000 ) ) ;
#25093=VERTEX_POINT ( 'NONE', #29706 ) ;
#25096=ORIENTED_EDGE ( 'NONE', *, *, #1229, .T. ) ;
#25112=ORIENTED_EDGE ( 'NONE', *, *, #11126, .F. ) ;
#25114=FACE_OUTER_BOUND ( 'NONE', #25173, .T. ) ;
#25133=VECTOR ( 'NONE', #67297, 1000.000000000000000 ) ;
#25138=VERTEX_POINT ( 'NONE', #40677 ) ;
#25140=AXIS2_PLACEMENT_3D ( 'NONE', #31788, #26474, #68565 ) ;
#25141=AXIS2_PLACEMENT_3D ( 'NONE', #45162, #12284, #23262 ) ;
#25147=VECTOR ( 'NONE', #29315, 1000.000000000000000 ) ;
#25155=EDGE_LOOP ( 'NONE', ( #4177, #34703, #11384, #28553 ) ) ;
#25158=CARTESIAN_POINT ( 'NONE',  ( 7.250000000000005329, -7.249999999999998224, -23.50000000000000000 ) ) ;
#25159=LINE ( 'NONE', #52753, #12616 ) ;
#25160=ADVANCED_FACE ( 'NONE', ( #50593 ), #30067, .T. ) ;
#25165=DIRECTION ( 'NONE',  ( 0.000000000000000000, 1.000000000000000000, 0.000000000000000000 ) ) ;
#25166=EDGE_CURVE ( 'NONE', #27562, #15739, #41016, .T. ) ;
#25167=EDGE_CURVE ( 'NONE', #16770, #44864, #14510, .T. ) ;
#25168=DIRECTION ( 'NONE',  ( 1.000000000000000000, 0.000000000000000000, 0.000000000000000000 ) ) ;
#25173=EDGE_LOOP ( 'NONE', ( #63641, #27145, #3300, #6493 ) ) ;
#25187=ORIENTED_EDGE ( 'NONE', *, *, #38369, .T. ) ;
#25188=VERTEX_POINT ( 'NONE', #47384 ) ;
#25193=CIRCLE ( 'NONE', #69256, 0.1999999999999996503 ) ;
#25206=LINE ( 'NONE', #30504, #15435 ) ;
#25227=VERTEX_POINT ( 'NONE', #20511 ) ;
#25231=ORIENTED_EDGE ( 'NONE', *, *, #33293, .T. ) ;
#25235=VERTEX_POINT ( 'NONE', #26880 ) ;
#25236=CARTESIAN_POINT ( 'NONE',  ( 0.000000000000000000, -7.449999999999998401, -17.00000000000000000 ) ) ;
#25242=DIRECTION ( 'NONE',  ( -1.000000000000000000, 0.000000000000000000, 0.000000000000000000 ) ) ;
#25251=AXIS2_PLACEMENT_3D ( 'NONE', #63958, #54385, #4904 ) ;
#25254=EDGE_CURVE ( 'NONE', #65843, #16435, #69299, .T. ) ;
#25255=VERTEX_POINT ( 'NONE', #15581 ) ;
#25263=ORIENTED_EDGE ( 'NONE', *, *, #48066, .F. ) ;
#25276=CARTESIAN_POINT ( 'NONE',  ( 0.000000000000000000, -8.249999999999998224, -8.500000000000000000 ) ) ;
#25281=VERTEX_POINT ( 'NONE', #25471 ) ;
#25284=CARTESIAN_POINT ( 'NONE',  ( -7.450000000000001954, 7.250000000000000000, -23.50000000000000000 ) ) ;
#25300=ORIENTED_EDGE ( 'NONE', *, *, #24406, .F. ) ;
#25306=ORIENTED_EDGE ( 'NONE', *, *, #33851, .F. ) ;
#25315=CARTESIAN_POINT ( 'NONE',  ( 8.250000000000005329, -7.249999999999998224, -26.00000000000001066 ) ) ;
#25322=EDGE_LOOP ( 'NONE', ( #50136, #43228, #58925, #49028 ) ) ;
#25326=ORIENTED_EDGE ( 'NONE', *, *, #38369, .F. ) ;
#25337=VECTOR ( 'NONE', #31906, 1000.000000000000000 ) ;
#25339=VECTOR ( 'NONE', #36933, 1000.000000000000000 ) ;
#25342=EDGE_CURVE ( 'NONE', #33795, #25480, #55255, .T. ) ;
#25345=EDGE_CURVE ( 'NONE', #67717, #18722, #54164, .T. ) ;
#25353=CIRCLE ( 'NONE', #17472, 0.2000000000000005107 ) ;
#25360=CARTESIAN_POINT ( 'NONE',  ( -7.450000000000001954, 0.000000000000000000, -24.00000000000000000 ) ) ;
#25362=DIRECTION ( 'NONE',  ( -0.000000000000000000, -0.000000000000000000, -1.000000000000000000 ) ) ;
#25369=VERTEX_POINT ( 'NONE', #21900 ) ;
#25372=DIRECTION ( 'NONE',  ( 0.000000000000000000, 0.000000000000000000, 1.000000000000000000 ) ) ;
#25375=DIRECTION ( 'NONE',  ( -0.000000000000000000, -0.000000000000000000, -1.000000000000000000 ) ) ;
#25380=ORIENTED_EDGE ( 'NONE', *, *, #51363, .T. ) ;
#25388=DIRECTION ( 'NONE',  ( 1.000000000000000000, -0.000000000000000000, 0.000000000000000000 ) ) ;
#25391=EDGE_CURVE ( 'NONE', #21660, #36053, #66060, .T. ) ;
#25398=CARTESIAN_POINT ( 'NONE',  ( 7.250000000000005329, -7.449999999999998401, -23.50000000000000000 ) ) ;
#25408=DIRECTION ( 'NONE',  ( 1.000000000000000000, 0.000000000000000000, 0.000000000000000000 ) ) ;
#25426=FACE_OUTER_BOUND ( 'NONE', #59922, .T. ) ;
#25430=CARTESIAN_POINT ( 'NONE',  ( 8.250000000000005329, 0.000000000000000000, -24.50000000000000000 ) ) ;
#25433=ADVANCED_FACE ( 'NONE', ( #33202 ), #27552, .T. ) ;
#25441=CIRCLE ( 'NONE', #63859, 0.1999999999999996503 ) ;
#25444=LINE ( 'NONE', #68583, #29814 ) ;
#25445=CYLINDRICAL_SURFACE ( 'NONE', #10295, 1.000000000000000000 ) ;
#25447=LINE ( 'NONE', #37117, #59372 ) ;
#25449=VECTOR ( 'NONE', #42399, 1000.000000000000000 ) ;
#25452=CARTESIAN_POINT ( 'NONE',  ( 7.250000000000005329, 8.250000000000001776, -10.00000000000000000 ) ) ;
#25453=AXIS2_PLACEMENT_3D ( 'NONE', #58507, #69098, #10058 ) ;
#25454=ORIENTED_EDGE ( 'NONE', *, *, #21701, .F. ) ;
#25457=EDGE_LOOP ( 'NONE', ( #25561, #33476, #37469, #54727 ) ) ;
#25462=ADVANCED_FACE ( 'NONE', ( #5992 ), #1044, .F. ) ;
#25464=FACE_OUTER_BOUND ( 'NONE', #64591, .T. ) ;
#25471=CARTESIAN_POINT ( 'NONE',  ( -7.250000000000000888, 8.250000000000001776, -24.00000000000000000 ) ) ;
#25472=CARTESIAN_POINT ( 'NONE',  ( -7.450000000000001954, -7.249999999999998224, -19.50000000000000000 ) ) ;
#25477=LINE ( 'NONE', #53406, #37922 ) ;
#25480=VERTEX_POINT ( 'NONE', #40932 ) ;
#25482=DIRECTION ( 'NONE',  ( -0.000000000000000000, -0.000000000000000000, 1.000000000000000000 ) ) ;
#25490=VECTOR ( 'NONE', #36037, 1000.000000000000000 ) ;
#25497=AXIS2_PLACEMENT_3D ( 'NONE', #66003, #55082, #32799 ) ;
#25498=VECTOR ( 'NONE', #54691, 1000.000000000000000 ) ;
#25499=AXIS2_PLACEMENT_3D ( 'NONE', #45623, #51290, #3210 ) ;
#25500=DIRECTION ( 'NONE',  ( 1.000000000000000000, -0.000000000000000000, -0.000000000000000000 ) ) ;
#25501=DIRECTION ( 'NONE',  ( -0.000000000000000000, -0.000000000000000000, 1.000000000000000000 ) ) ;
#25512=FACE_OUTER_BOUND ( 'NONE', #57872, .T. ) ;
#25515=VERTEX_POINT ( 'NONE', #45532 ) ;
#25519=CARTESIAN_POINT ( 'NONE',  ( -7.450000000000001954, 7.250000000000000000, -24.50000000000000000 ) ) ;
#25533=CARTESIAN_POINT ( 'NONE',  ( -8.250000000000001776, -8.249999999999998224, -26.00000000000001066 ) ) ;
#25536=CARTESIAN_POINT ( 'NONE',  ( -8.250000000000001776, -8.249999999999998224, -26.00000000000001066 ) ) ;
#25538=ORIENTED_EDGE ( 'NONE', *, *, #10184, .T. ) ;
#25542=AXIS2_PLACEMENT_3D ( 'NONE', #60983, #43704, #22490 ) ;
#25543=VECTOR ( 'NONE', #26900, 1000.000000000000000 ) ;
#25544=CARTESIAN_POINT ( 'NONE',  ( -7.250000000000000000, -7.449999999999998401, -7.500000000000000000 ) ) ;
#25548=VERTEX_POINT ( 'NONE', #29265 ) ;
#25559=ORIENTED_EDGE ( 'NONE', *, *, #30209, .F. ) ;
#25561=ORIENTED_EDGE ( 'NONE', *, *, #27930, .F. ) ;
#25562=ORIENTED_EDGE ( 'NONE', *, *, #31259, .T. ) ;
#25564=VECTOR ( 'NONE', #14753, 1000.000000000000000 ) ;
#25576=ORIENTED_EDGE ( 'NONE', *, *, #49204, .T. ) ;
#25586=ORIENTED_EDGE ( 'NONE', *, *, #41153, .F. ) ;
#25594=AXIS2_PLACEMENT_3D ( 'NONE', #5686, #21934, #38217 ) ;
#25600=AXIS2_PLACEMENT_3D ( 'NONE', #66130, #8463, #19434 ) ;
#25609=AXIS2_PLACEMENT_3D ( 'NONE', #56423, #55734, #33809 ) ;
#25610=DIRECTION ( 'NONE',  ( -1.794541526872559352E-16, -1.000000000000000000, 0.000000000000000000 ) ) ;
#25627=PLANE ( 'NONE',  #22079 ) ;
#25628=CARTESIAN_POINT ( 'NONE',  ( 7.250000000000005329, -7.249999999999998224, -26.00000000000001066 ) ) ;
#25629=ORIENTED_EDGE ( 'NONE', *, *, #22653, .F. ) ;
#25633=VECTOR ( 'NONE', #26572, 1000.000000000000000 ) ;
#25642=AXIS2_PLACEMENT_3D ( 'NONE', #13400, #34954, #56534 ) ;
#25648=AXIS2_PLACEMENT_3D ( 'NONE', #57521, #44552, #52218 ) ;
#25654=CYLINDRICAL_SURFACE ( 'NONE', #46569, 1.000000000000000000 ) ;
#25658=DIRECTION ( 'NONE',  ( 1.000000000000000000, 0.000000000000000000, 0.000000000000000000 ) ) ;
#25661=ORIENTED_EDGE ( 'NONE', *, *, #61318, .T. ) ;
#25679=ORIENTED_EDGE ( 'NONE', *, *, #67049, .T. ) ;
#25681=VERTEX_POINT ( 'NONE', #36336 ) ;
#25686=LINE ( 'NONE', #47244, #66774 ) ;
#25687=DIRECTION ( 'NONE',  ( 0.000000000000000000, 1.000000000000000000, 0.000000000000000000 ) ) ;
#25695=AXIS2_PLACEMENT_3D ( 'NONE', #52550, #58561, #41929 ) ;
#25696=LINE ( 'NONE', #47255, #45797 ) ;
#25709=LINE ( 'NONE', #4138, #36497 ) ;
#25712=LINE ( 'NONE', #41955, #30526 ) ;
#25724=CYLINDRICAL_SURFACE ( 'NONE', #17584, 1.000000000000000000 ) ;
#25732=VECTOR ( 'NONE', #23077, 1000.000000000000000 ) ;
#25736=EDGE_LOOP ( 'NONE', ( #15229, #52107, #8850, #49317 ) ) ;
#25738=ORIENTED_EDGE ( 'NONE', *, *, #25345, .F. ) ;
#25751=EDGE_CURVE ( 'NONE', #14563, #52575, #20177, .T. ) ;
#25754=CIRCLE ( 'NONE', #40419, 0.9999999999999991118 ) ;
#25756=FACE_OUTER_BOUND ( 'NONE', #9937, .T. ) ;
#25787=CARTESIAN_POINT ( 'NONE',  ( 7.250000000000005329, -8.749999999999998224, -30.00000000000001066 ) ) ;
#25794=CARTESIAN_POINT ( 'NONE',  ( -7.250000000000000888, 7.250000000000001776, -15.00000000000000000 ) ) ;
#25800=DIRECTION ( 'NONE',  ( -1.000000000000000000, 1.794541526872559352E-16, 0.000000000000000000 ) ) ;
#25803=CARTESIAN_POINT ( 'NONE',  ( 7.250000000000005329, -8.249999999999998224, -18.50000000000000000 ) ) ;
#25806=CYLINDRICAL_SURFACE ( 'NONE', #61083, 0.1999999999999996503 ) ;
#25809=DIRECTION ( 'NONE',  ( 0.000000000000000000, -1.000000000000000000, -0.000000000000000000 ) ) ;
#25813=VECTOR ( 'NONE', #56987, 1000.000000000000000 ) ;
#25819=ORIENTED_EDGE ( 'NONE', *, *, #64705, .T. ) ;
#25820=CARTESIAN_POINT ( 'NONE',  ( -7.450000000000001954, -7.249999999999998224, -13.50000000000000178 ) ) ;
#25825=VERTEX_POINT ( 'NONE', #48351 ) ;
#25826=DIRECTION ( 'NONE',  ( 1.000000000000000000, 0.000000000000000000, 0.000000000000000000 ) ) ;
#25839=CARTESIAN_POINT ( 'NONE',  ( 8.250000000000005329, -7.249999999999998224, -23.00000000000000000 ) ) ;
#25840=ADVANCED_FACE ( 'NONE', ( #64958, #22856 ), #21471, .F. ) ;
#25845=EDGE_CURVE ( 'NONE', #36419, #48765, #55055, .T. ) ;
#25847=SHAPE_REPRESENTATION ( '6266N13_Heavy Duty Locking-Slotted Fitting1_6266N13', ( #45918 ), #48210 ) ;
#25848=CARTESIAN_POINT ( 'NONE',  ( -7.250000000000000888, -8.249999999999998224, -24.50000000000000000 ) ) ;
#25851=AXIS2_PLACEMENT_3D ( 'NONE', #67342, #9697, #40810 ) ;
#25853=DIRECTION ( 'NONE',  ( -0.000000000000000000, -0.000000000000000000, -1.000000000000000000 ) ) ;
#25860=VECTOR ( 'NONE', #32740, 1000.000000000000000 ) ;
#25864=DIRECTION ( 'NONE',  ( 0.000000000000000000, 1.000000000000000000, -0.000000000000000000 ) ) ;
#25865=ORIENTED_EDGE ( 'NONE', *, *, #29632, .F. ) ;
#25868=DIRECTION ( 'NONE',  ( 0.000000000000000000, 0.000000000000000000, 1.000000000000000000 ) ) ;
#25869=CARTESIAN_POINT ( 'NONE',  ( -7.450000000000001954, 7.250000000000000000, -12.00000000000000000 ) ) ;
#25873=DIRECTION ( 'NONE',  ( 0.000000000000000000, 0.000000000000000000, 1.000000000000000000 ) ) ;
#25875=ORIENTED_EDGE ( 'NONE', *, *, #35897, .T. ) ;
#25876=CARTESIAN_POINT ( 'NONE',  ( 9.690000000000001279, -9.750000000000001776, -5.000000000000000000 ) ) ;
#25877=ADVANCED_FACE ( 'NONE', ( #1293 ), #44404, .T. ) ;
#25879=ORIENTED_EDGE ( 'NONE', *, *, #10347, .F. ) ;
#25889=VECTOR ( 'NONE', #17823, 1000.000000000000000 ) ;
#25890=CARTESIAN_POINT ( 'NONE',  ( 7.250000000000004441, 7.450000000000001954, -11.50000000000000000 ) ) ;
#25896=CARTESIAN_POINT ( 'NONE',  ( 7.250000000000005329, -7.249999999999998224, -9.000000000000001776 ) ) ;
#25906=ADVANCED_FACE ( 'NONE', ( #67393 ), #23545, .F. ) ;
#25908=CIRCLE ( 'NONE', #3331, 0.1999999999999987899 ) ;
#25909=DIRECTION ( 'NONE',  ( -1.000000000000000000, 0.000000000000000000, 0.000000000000000000 ) ) ;
#25920=EDGE_CURVE ( 'NONE', #45036, #9839, #39792, .T. ) ;
#25921=CARTESIAN_POINT ( 'NONE',  ( 7.250000000000005329, -8.249999999999998224, -23.00000000000000000 ) ) ;
#25924=AXIS2_PLACEMENT_3D ( 'NONE', #8534, #34349, #50282 ) ;
#25928=ORIENTED_EDGE ( 'NONE', *, *, #61545, .T. ) ;
#25933=EDGE_CURVE ( 'NONE', #49333, #35740, #41665, .T. ) ;
#25937=EDGE_LOOP ( 'NONE', ( #49988, #12683, #63959, #42260 ) ) ;
#25939=ORIENTED_EDGE ( 'NONE', *, *, #14644, .T. ) ;
#25944=EDGE_LOOP ( 'NONE', ( #50675, #3600, #4283, #18262 ) ) ;
#25947=VERTEX_POINT ( 'NONE', #7272 ) ;
#25951=ADVANCED_BREP_SHAPE_REPRESENTATION ( '', ( #44754, #45918 ), #48210 ) ;
#25963=ORIENTED_EDGE ( 'NONE', *, *, #285, .F. ) ;
#25972=FACE_OUTER_BOUND ( 'NONE', #30769, .T. ) ;
#25975=ADVANCED_FACE ( 'NONE', ( #10094 ), #26013, .T. ) ;
#25977=DIRECTION ( 'NONE',  ( 1.000000000000000000, 0.000000000000000000, 0.000000000000000000 ) ) ;
#25983=CARTESIAN_POINT ( 'NONE',  ( 8.750000000000005329, -7.249999999999997335, -26.00000000000001066 ) ) ;
#26001=FACE_OUTER_BOUND ( 'NONE', #16612, .T. ) ;
#26004=CARTESIAN_POINT ( 'NONE',  ( -7.450000000000001954, 0.000000000000000000, -23.50000000000000000 ) ) ;
#26012=AXIS2_PLACEMENT_3D ( 'NONE', #1781, #18381, #12038 ) ;
#26013=CYLINDRICAL_SURFACE ( 'NONE', #6632, 0.1999999999999996503 ) ;
#26014=DIRECTION ( 'NONE',  ( 0.000000000000000000, 0.000000000000000000, 1.000000000000000000 ) ) ;
#26023=VERTEX_POINT ( 'NONE', #47567 ) ;
#26029=DIRECTION ( 'NONE',  ( 0.000000000000000000, 0.000000000000000000, 1.000000000000000000 ) ) ;
#26033=EDGE_LOOP ( 'NONE', ( #1230, #66080, #48998, #27210 ) ) ;
#26035=DIRECTION ( 'NONE',  ( 0.000000000000000000, 0.000000000000000000, -1.000000000000000000 ) ) ;
#26037=ORIENTED_EDGE ( 'NONE', *, *, #25933, .T. ) ;
#26039=VECTOR ( 'NONE', #29524, 1000.000000000000000 ) ;
#26040=DIRECTION ( 'NONE',  ( 0.000000000000000000, 0.000000000000000000, 1.000000000000000000 ) ) ;
#26041=CYLINDRICAL_SURFACE ( 'NONE', #18909, 1.000000000000000000 ) ;
#26043=ORIENTED_EDGE ( 'NONE', *, *, #31157, .T. ) ;
#26047=EDGE_CURVE ( 'NONE', #54166, #68564, #12264, .T. ) ;
#26053=EDGE_CURVE ( 'NONE', #19699, #6379, #51815, .T. ) ;
#26073=CARTESIAN_POINT ( 'NONE',  ( 6.750000000000000000, 7.750000000000000000, 0.000000000000000000 ) ) ;
#26077=AXIS2_PLACEMENT_3D ( 'NONE', #28518, #55407, #27838 ) ;
#26082=ORIENTED_EDGE ( 'NONE', *, *, #7209, .T. ) ;
#26084=VERTEX_POINT ( 'NONE', #14692 ) ;
#26086=FACE_OUTER_BOUND ( 'NONE', #3623, .T. ) ;
#26091=ADVANCED_FACE ( 'NONE', ( #36978 ), #3384, .T. ) ;
#26100=CARTESIAN_POINT ( 'NONE',  ( -7.250000000000000888, -8.249999999999998224, -15.00000000000000000 ) ) ;
#26102=ORIENTED_EDGE ( 'NONE', *, *, #17658, .T. ) ;
#26108=ORIENTED_EDGE ( 'NONE', *, *, #28184, .T. ) ;
#26110=DIRECTION ( 'NONE',  ( -1.000000000000000000, 0.000000000000000000, 0.000000000000000000 ) ) ;
#26113=CARTESIAN_POINT ( 'NONE',  ( -7.250000000000001776, -7.249999999999998224, -17.00000000000000000 ) ) ;
#26123=VERTEX_POINT ( 'NONE', #54975 ) ;
#26127=VECTOR ( 'NONE', #30972, 1000.000000000000000 ) ;
#26131=ORIENTED_EDGE ( 'NONE', *, *, #21740, .F. ) ;
#26135=LINE ( 'NONE', #4226, #52050 ) ;
#26139=EDGE_CURVE ( 'NONE', #27517, #11827, #16438, .T. ) ;
#26140=DIRECTION ( 'NONE',  ( -5.981805089575196197E-17, -1.000000000000000000, 0.000000000000000000 ) ) ;
#26146=EDGE_CURVE ( 'NONE', #60163, #30760, #4399, .T. ) ;
#26147=CARTESIAN_POINT ( 'NONE',  ( -8.250000000000001776, -7.249999999999998224, -22.00000000000000000 ) ) ;
#26152=CARTESIAN_POINT ( 'NONE',  ( 7.250000000000005329, -8.249999999999998224, -11.50000000000000000 ) ) ;
#26153=ORIENTED_EDGE ( 'NONE', *, *, #21421, .T. ) ;
#26160=DIRECTION ( 'NONE',  ( -1.000000000000000000, 0.000000000000000000, 0.000000000000000000 ) ) ;
#26161=ADVANCED_FACE ( 'NONE', ( #6531 ), #49321, .T. ) ;
#26172=ORIENTED_EDGE ( 'NONE', *, *, #25166, .F. ) ;
#26173=DIRECTION ( 'NONE',  ( -1.000000000000000000, 0.000000000000000000, 0.000000000000000000 ) ) ;
#26184=DIRECTION ( 'NONE',  ( 0.000000000000000000, -0.000000000000000000, 1.000000000000000000 ) ) ;
#26186=PLANE ( 'NONE',  #5941 ) ;
#26190=DIRECTION ( 'NONE',  ( 0.000000000000000000, 0.000000000000000000, -1.000000000000000000 ) ) ;
#26192=LINE ( 'NONE', #9936, #48535 ) ;
#26199=CARTESIAN_POINT ( 'NONE',  ( 7.450000000000003730, -7.249999999999997335, -7.000000000000000000 ) ) ;
#26202=VERTEX_POINT ( 'NONE', #42954 ) ;
#26203=CARTESIAN_POINT ( 'NONE',  ( -7.250000000000000888, 7.250000000000001776, -26.00000000000001066 ) ) ;
#26205=DIRECTION ( 'NONE',  ( 0.000000000000000000, 0.000000000000000000, 1.000000000000000000 ) ) ;
#26220=ORIENTED_EDGE ( 'NONE', *, *, #31953, .F. ) ;
#26223=EDGE_CURVE ( 'NONE', #18304, #29522, #16800, .T. ) ;
#26230=VECTOR ( 'NONE', #22572, 1000.000000000000000 ) ;
#26238=EDGE_CURVE ( 'NONE', #37936, #60008, #11177, .T. ) ;
#26239=CARTESIAN_POINT ( 'NONE',  ( -8.250000000000001776, 0.000000000000000000, -11.00000000000000000 ) ) ;
#26255=PLANE ( 'NONE',  #49553 ) ;
#26257=CARTESIAN_POINT ( 'NONE',  ( 7.250000000000005329, -7.249999999999998224, -24.00000000000000000 ) ) ;
#26265=VERTEX_POINT ( 'NONE', #59915 ) ;
#26274=CARTESIAN_POINT ( 'NONE',  ( -7.250000000000000000, -7.449999999999998401, -21.50000000000000000 ) ) ;
#26275=ORIENTED_EDGE ( 'NONE', *, *, #41904, .F. ) ;
#26278=ORIENTED_EDGE ( 'NONE', *, *, #13798, .F. ) ;
#26288=EDGE_CURVE ( 'NONE', #27857, #7713, #34060, .T. ) ;
#26290=ORIENTED_EDGE ( 'NONE', *, *, #34216, .F. ) ;
#26310=ORIENTED_EDGE ( 'NONE', *, *, #19563, .F. ) ;
#26315=EDGE_CURVE ( 'NONE', #381, #40067, #45082, .T. ) ;
#26318=ORIENTED_EDGE ( 'NONE', *, *, #1433, .F. ) ;
#26319=DIRECTION ( 'NONE',  ( 0.000000000000000000, 1.000000000000000000, 0.000000000000000000 ) ) ;
#26322=CARTESIAN_POINT ( 'NONE',  ( -7.250000000000000888, -8.249999999999998224, -26.00000000000001066 ) ) ;
#26327=VECTOR ( 'NONE', #22064, 1000.000000000000000 ) ;
#26330=CARTESIAN_POINT ( 'NONE',  ( -7.450000000000001954, -7.249999999999998224, -12.50000000000000000 ) ) ;
#26333=LINE ( 'NONE', #47891, #50910 ) ;
#26344=EDGE_CURVE ( 'NONE', #29352, #19794, #67662, .T. ) ;
#26345=EDGE_LOOP ( 'NONE', ( #24266, #52365, #2566, #39552 ) ) ;
#26347=EDGE_CURVE ( 'NONE', #65501, #18999, #29122, .T. ) ;
#26350=VECTOR ( 'NONE', #35445, 1000.000000000000000 ) ;
#26357=AXIS2_PLACEMENT_3D ( 'NONE', #49384, #947, #55704 ) ;
#26362=ORIENTED_EDGE ( 'NONE', *, *, #46099, .T. ) ;
#26364=CIRCLE ( 'NONE', #4914, 1.000000000000000000 ) ;
#26365=EDGE_CURVE ( 'NONE', #32920, #42042, #50679, .T. ) ;
#26368=DIRECTION ( 'NONE',  ( 1.000000000000000000, -0.000000000000000000, 0.000000000000000000 ) ) ;
#26371=VERTEX_POINT ( 'NONE', #2251 ) ;
#26374=EDGE_CURVE ( 'NONE', #21984, #7881, #42833, .T. ) ;
#26397=ADVANCED_FACE ( 'NONE', ( #43875, #22664 ), #59796, .T. ) ;
#26405=VECTOR ( 'NONE', #11445, 1000.000000000000000 ) ;
#26407=AXIS2_PLACEMENT_3D ( 'NONE', #61312, #28118, #49680 ) ;
#26419=FACE_OUTER_BOUND ( 'NONE', #45471, .T. ) ;
#26425=CARTESIAN_POINT ( 'NONE',  ( 8.250000000000005329, -7.249999999999998224, -26.00000000000001066 ) ) ;
#26426=VERTEX_POINT ( 'NONE', #49190 ) ;
#26429=VERTEX_POINT ( 'NONE', #16316 ) ;
#26435=ORIENTED_EDGE ( 'NONE', *, *, #56282, .F. ) ;
#26437=ADVANCED_FACE ( 'NONE', ( #54159 ), #55185, .T. ) ;
#26440=LINE ( 'NONE', #41649, #32210 ) ;
#26447=ORIENTED_EDGE ( 'NONE', *, *, #65869, .T. ) ;
#26458=VECTOR ( 'NONE', #36432, 1000.000000000000000 ) ;
#26459=AXIS2_PLACEMENT_3D ( 'NONE', #20234, #19886, #25909 ) ;
#26463=DIRECTION ( 'NONE',  ( 0.000000000000000000, 0.000000000000000000, 1.000000000000000000 ) ) ;
#26465=AXIS2_PLACEMENT_3D ( 'NONE', #61180, #12738, #61896 ) ;
#26473=VECTOR ( 'NONE', #24066, 1000.000000000000000 ) ;
#26474=DIRECTION ( 'NONE',  ( 0.000000000000000000, 0.000000000000000000, 1.000000000000000000 ) ) ;
#26475=CARTESIAN_POINT ( 'NONE',  ( 7.450000000000006395, 7.250000000000000888, -12.50000000000000000 ) ) ;
#26477=DIRECTION ( 'NONE',  ( 0.000000000000000000, 0.000000000000000000, 1.000000000000000000 ) ) ;
#26487=EDGE_CURVE ( 'NONE', #62127, #17538, #49874, .T. ) ;
#26488=CARTESIAN_POINT ( 'NONE',  ( 7.250000000000005329, -8.249999999999998224, -26.00000000000001066 ) ) ;
#26489=CARTESIAN_POINT ( 'NONE',  ( 0.000000000000000000, -8.249999999999998224, -19.00000000000000000 ) ) ;
#26490=VERTEX_POINT ( 'NONE', #15973 ) ;
#26495=DIRECTION ( 'NONE',  ( 1.000000000000000000, -5.981805089575194965E-17, 0.000000000000000000 ) ) ;
#26501=CIRCLE ( 'NONE', #42284, 1.000000000000000000 ) ;
#26507=DIRECTION ( 'NONE',  ( 0.000000000000000000, 0.000000000000000000, -1.000000000000000000 ) ) ;
#26517=ORIENTED_EDGE ( 'NONE', *, *, #66136, .T. ) ;
#26543=ORIENTED_EDGE ( 'NONE', *, *, #53763, .T. ) ;
#26556=ORIENTED_EDGE ( 'NONE', *, *, #54668, .F. ) ;
#26557=CARTESIAN_POINT ( 'NONE',  ( 6.749999999999996447, -7.348062532928000934, -5.000000000000000000 ) ) ;
#26569=ORIENTED_EDGE ( 'NONE', *, *, #8296, .T. ) ;
#26570=DIRECTION ( 'NONE',  ( 0.000000000000000000, -0.000000000000000000, 1.000000000000000000 ) ) ;
#26572=DIRECTION ( 'NONE',  ( 0.000000000000000000, 1.000000000000000000, 0.000000000000000000 ) ) ;
#26575=EDGE_CURVE ( 'NONE', #38612, #46075, #33816, .T. ) ;
#26578=CARTESIAN_POINT ( 'NONE',  ( -7.250000000000000888, 7.450000000000003730, -12.00000000000000000 ) ) ;
#26598=ORIENTED_EDGE ( 'NONE', *, *, #12088, .F. ) ;
#26601=AXIS2_PLACEMENT_3D ( 'NONE', #68366, #30531, #47833 ) ;
#26608=DIRECTION ( 'NONE',  ( 1.000000000000000000, -0.000000000000000000, 0.000000000000000000 ) ) ;
#26610=ORIENTED_EDGE ( 'NONE', *, *, #30821, .F. ) ;
#26617=EDGE_CURVE ( 'NONE', #31212, #47075, #60699, .T. ) ;
#26619=AXIS2_PLACEMENT_3D ( 'NONE', #50300, #17428, #28053 ) ;
#26624=EDGE_CURVE ( 'NONE', #51641, #53480, #29908, .T. ) ;
#26627=CARTESIAN_POINT ( 'NONE',  ( -6.500000000000002665, 6.500000000000002665, -1.000000000000000000 ) ) ;
#26636=LINE ( 'NONE', #69781, #40146 ) ;
#26643=ORIENTED_EDGE ( 'NONE', *, *, #49864, .F. ) ;
#26647=PLANE ( 'NONE',  #31796 ) ;
#26649=DIRECTION ( 'NONE',  ( 0.000000000000000000, -0.000000000000000000, 1.000000000000000000 ) ) ;
#26651=VERTEX_POINT ( 'NONE', #39468 ) ;
#26656=CIRCLE ( 'NONE', #11930, 0.1999999999999987899 ) ;
#26658=LINE ( 'NONE', #57775, #28934 ) ;
#26661=AXIS2_PLACEMENT_3D ( 'NONE', #27767, #33064, #54647 ) ;
#26674=LINE ( 'NONE', #53903, #44839 ) ;
#26693=ORIENTED_EDGE ( 'NONE', *, *, #31074, .F. ) ;
#26703=AXIS2_PLACEMENT_3D ( 'NONE', #32924, #47789, #26938 ) ;
#26705=EDGE_CURVE ( 'NONE', #11793, #5559, #33355, .T. ) ;
#26715=VECTOR ( 'NONE', #10283, 1000.000000000000000 ) ;
#26719=DIRECTION ( 'NONE',  ( -1.000000000000000000, 0.000000000000000000, 0.000000000000000000 ) ) ;
#26724=VECTOR ( 'NONE', #3787, 1000.000000000000000 ) ;
#26748=CARTESIAN_POINT ( 'NONE',  ( 7.450000000000006395, 7.250000000000000888, -14.00000000000000000 ) ) ;
#26749=AXIS2_PLACEMENT_3D ( 'NONE', #5534, #48669, #41963 ) ;
#26756=CARTESIAN_POINT ( 'NONE',  ( 7.250000000000005329, 8.250000000000001776, -26.00000000000001066 ) ) ;
#26759=EDGE_LOOP ( 'NONE', ( #47413, #61477, #64803, #31785 ) ) ;
#26766=DIRECTION ( 'NONE',  ( -1.000000000000000000, 0.000000000000000000, -0.000000000000000000 ) ) ;
#26772=DIRECTION ( 'NONE',  ( 0.000000000000000000, 1.000000000000000000, 0.000000000000000000 ) ) ;
#26778=CARTESIAN_POINT ( 'NONE',  ( 7.250000000000005329, -8.249999999999998224, -26.00000000000001066 ) ) ;
#26786=DIRECTION ( 'NONE',  ( 0.000000000000000000, 0.000000000000000000, 1.000000000000000000 ) ) ;
#26800=ORIENTED_EDGE ( 'NONE', *, *, #12422, .F. ) ;
#26802=VECTOR ( 'NONE', #3498, 1000.000000000000000 ) ;
#26805=CARTESIAN_POINT ( 'NONE',  ( 7.250000000000005329, -7.449999999999998401, -20.00000000000000000 ) ) ;
#26832=DIRECTION ( 'NONE',  ( -0.000000000000000000, -0.000000000000000000, -1.000000000000000000 ) ) ;
#26835=DIRECTION ( 'NONE',  ( -1.794541526872559352E-16, -1.000000000000000000, 0.000000000000000000 ) ) ;
#26839=CARTESIAN_POINT ( 'NONE',  ( -8.250000000000001776, 7.250000000000000888, -26.00000000000001066 ) ) ;
#26845=CARTESIAN_POINT ( 'NONE',  ( -8.250000000000001776, 0.000000000000000000, -20.50000000000000000 ) ) ;
#26846=EDGE_CURVE ( 'NONE', #16332, #27411, #17139, .T. ) ;
#26853=CARTESIAN_POINT ( 'NONE',  ( 4.456444791733522252E-16, 7.450000000000002842, -8.500000000000000000 ) ) ;
#26861=FACE_OUTER_BOUND ( 'NONE', #37602, .T. ) ;
#26867=VERTEX_POINT ( 'NONE', #15757 ) ;
#26868=DIRECTION ( 'NONE',  ( -0.000000000000000000, 0.000000000000000000, 1.000000000000000000 ) ) ;
#26872=CARTESIAN_POINT ( 'NONE',  ( 7.250000000000005329, 7.250000000000000888, -9.000000000000001776 ) ) ;
#26880=CARTESIAN_POINT ( 'NONE',  ( 7.250000000000005329, 8.250000000000001776, -26.00000000000001066 ) ) ;
#26883=ORIENTED_EDGE ( 'NONE', *, *, #53665, .F. ) ;
#26887=VERTEX_POINT ( 'NONE', #11139 ) ;
#26888=EDGE_LOOP ( 'NONE', ( #14885, #39833, #45460, #1991 ) ) ;
#26893=EDGE_CURVE ( 'NONE', #40508, #20305, #36749, .T. ) ;
#26900=DIRECTION ( 'NONE',  ( 0.000000000000000000, 0.000000000000000000, 1.000000000000000000 ) ) ;
#26902=VERTEX_POINT ( 'NONE', #27060 ) ;
#26907=CIRCLE ( 'NONE', #51728, 0.1999999999999987899 ) ;
#26911=ORIENTED_EDGE ( 'NONE', *, *, #27930, .T. ) ;
#26912=DIRECTION ( 'NONE',  ( -1.000000000000000000, 0.000000000000000000, 0.000000000000000000 ) ) ;
#26913=VERTEX_POINT ( 'NONE', #43317 ) ;
#26920=CARTESIAN_POINT ( 'NONE',  ( -8.250000000000001776, -7.249999999999998224, -18.50000000000000000 ) ) ;
#26926=ADVANCED_FACE ( 'NONE', ( #21061 ), #538, .T. ) ;
#26930=DIRECTION ( 'NONE',  ( 0.000000000000000000, 0.000000000000000000, -1.000000000000000000 ) ) ;
#26938=DIRECTION ( 'NONE',  ( -1.000000000000000000, 0.000000000000000000, 0.000000000000000000 ) ) ;
#26942=EDGE_CURVE ( 'NONE', #26902, #48304, #51416, .T. ) ;
#26944=CARTESIAN_POINT ( 'NONE',  ( 7.250000000000004441, 7.450000000000001954, -15.00000000000000000 ) ) ;
#26946=EDGE_LOOP ( 'NONE', ( #51190, #5441, #29538, #48777 ) ) ;
#26949=DIRECTION ( 'NONE',  ( -1.000000000000000000, 0.000000000000000000, 0.000000000000000000 ) ) ;
#26950=DIRECTION ( 'NONE',  ( -1.000000000000000000, 0.000000000000000000, 0.000000000000000000 ) ) ;
#26957=DIRECTION ( 'NONE',  ( -1.794541526872559352E-16, -1.000000000000000000, 0.000000000000000000 ) ) ;
#26961=CARTESIAN_POINT ( 'NONE',  ( 4.456444791733522252E-16, 7.450000000000002842, -22.50000000000000000 ) ) ;
#26970=DIRECTION ( 'NONE',  ( -0.000000000000000000, -0.000000000000000000, 1.000000000000000000 ) ) ;
#26975=DIRECTION ( 'NONE',  ( 0.000000000000000000, 0.000000000000000000, 1.000000000000000000 ) ) ;
#26980=EDGE_CURVE ( 'NONE', #47295, #2646, #40444, .T. ) ;
#26986=VERTEX_POINT ( 'NONE', #2266 ) ;
#27002=AXIS2_PLACEMENT_3D ( 'NONE', #46411, #61617, #57373 ) ;
#27007=DIRECTION ( 'NONE',  ( 0.000000000000000000, 0.000000000000000000, 1.000000000000000000 ) ) ;
#27008=VECTOR ( 'NONE', #17414, 1000.000000000000000 ) ;
#27019=FACE_OUTER_BOUND ( 'NONE', #21128, .T. ) ;
#27025=EDGE_LOOP ( 'NONE', ( #6240, #24676, #50917, #30293 ) ) ;
#27044=ORIENTED_EDGE ( 'NONE', *, *, #49810, .F. ) ;
#27058=ORIENTED_EDGE ( 'NONE', *, *, #52864, .T. ) ;
#27060=CARTESIAN_POINT ( 'NONE',  ( -7.250000000000000000, -7.449999999999998401, -20.00000000000000000 ) ) ;
#27075=DIRECTION ( 'NONE',  ( -1.000000000000000000, 0.000000000000000000, 0.000000000000000000 ) ) ;
#27081=LINE ( 'NONE', #21430, #64721 ) ;
#27094=DIRECTION ( 'NONE',  ( -1.000000000000000000, 0.000000000000000000, 0.000000000000000000 ) ) ;
#27102=DIRECTION ( 'NONE',  ( -1.000000000000000000, 0.000000000000000000, 0.000000000000000000 ) ) ;
#27114=DIRECTION ( 'NONE',  ( -0.000000000000000000, -0.000000000000000000, -1.000000000000000000 ) ) ;
#27125=CARTESIAN_POINT ( 'NONE',  ( 0.000000000000000000, -8.249999999999998224, -15.50000000000000000 ) ) ;
#27128=DIRECTION ( 'NONE',  ( 1.000000000000000000, -5.981805089575194965E-17, 0.000000000000000000 ) ) ;
#27130=VECTOR ( 'NONE', #32710, 1000.000000000000000 ) ;
#27131=EDGE_CURVE ( 'NONE', #37776, #62704, #67665, .T. ) ;
#27143=AXIS2_PLACEMENT_3D ( 'NONE', #61920, #13478, #3231 ) ;
#27145=ORIENTED_EDGE ( 'NONE', *, *, #55993, .F. ) ;
#27147=AXIS2_PLACEMENT_3D ( 'NONE', #7608, #3357, #19610 ) ;
#27153=EDGE_LOOP ( 'NONE', ( #57884, #3531, #4309, #45280 ) ) ;
#27155=FACE_OUTER_BOUND ( 'NONE', #40205, .T. ) ;
#27159=ORIENTED_EDGE ( 'NONE', *, *, #16142, .T. ) ;
#27160=CIRCLE ( 'NONE', #66028, 0.2000000000000005107 ) ;
#27161=CARTESIAN_POINT ( 'NONE',  ( -7.250000000000000888, 7.250000000000001776, -22.50000000000000000 ) ) ;
#27165=ORIENTED_EDGE ( 'NONE', *, *, #55654, .T. ) ;
#27169=VECTOR ( 'NONE', #67522, 1000.000000000000000 ) ;
#27170=AXIS2_PLACEMENT_3D ( 'NONE', #18163, #55651, #45727 ) ;
#27175=EDGE_CURVE ( 'NONE', #28094, #20614, #36906, .T. ) ;
#27185=CARTESIAN_POINT ( 'NONE',  ( -8.250000000000001776, -7.249999999999998224, -26.00000000000001066 ) ) ;
#27197=PLANE ( 'NONE',  #61538 ) ;
#27199=EDGE_CURVE ( 'NONE', #35627, #50861, #43549, .T. ) ;
#27210=ORIENTED_EDGE ( 'NONE', *, *, #31290, .T. ) ;
#27211=VECTOR ( 'NONE', #57616, 1000.000000000000000 ) ;
#27214=VECTOR ( 'NONE', #7252, 1000.000000000000000 ) ;
#27231=CARTESIAN_POINT ( 'NONE',  ( 8.689999999999999503, -8.750000000000000000, -7.000000000000000000 ) ) ;
#27242=ADVANCED_FACE ( 'NONE', ( #37601 ), #65170, .F. ) ;
#27254=DIRECTION ( 'NONE',  ( -0.000000000000000000, 0.000000000000000000, -1.000000000000000000 ) ) ;
#27268=EDGE_CURVE ( 'NONE', #32145, #23467, #26636, .T. ) ;
#27270=DIRECTION ( 'NONE',  ( -1.000000000000000000, 0.000000000000000000, 0.000000000000000000 ) ) ;
#27292=CARTESIAN_POINT ( 'NONE',  ( -7.450000000000001954, 7.250000000000000000, -15.50000000000000000 ) ) ;
#27298=LINE ( 'NONE', #48862, #40819 ) ;
#27300=ORIENTED_EDGE ( 'NONE', *, *, #2078, .F. ) ;
#27310=DIRECTION ( 'NONE',  ( -1.000000000000000000, 0.000000000000000000, 0.000000000000000000 ) ) ;
#27313=EDGE_LOOP ( 'NONE', ( #19640, #1183, #63839, #5054 ) ) ;
#27326=CIRCLE ( 'NONE', #54429, 1.500000000000001332 ) ;
#27327=CARTESIAN_POINT ( 'NONE',  ( -7.450000000000001954, 7.250000000000000000, -24.50000000000000000 ) ) ;
#27333=ORIENTED_EDGE ( 'NONE', *, *, #69494, .T. ) ;
#27336=EDGE_CURVE ( 'NONE', #21475, #55726, #44687, .T. ) ;
#27348=CIRCLE ( 'NONE', #66830, 0.9999999999999991118 ) ;
#27361=EDGE_LOOP ( 'NONE', ( #30599, #65164, #15915, #20877 ) ) ;
#27364=ADVANCED_FACE ( 'NONE', ( #49249 ), #7475, .T. ) ;
#27369=ADVANCED_FACE ( 'NONE', ( #18080 ), #55923, .F. ) ;
#27375=DIRECTION ( 'NONE',  ( 0.000000000000000000, 0.000000000000000000, 1.000000000000000000 ) ) ;
#27378=DIRECTION ( 'NONE',  ( -0.000000000000000000, -0.000000000000000000, -1.000000000000000000 ) ) ;
#27385=CARTESIAN_POINT ( 'NONE',  ( 0.000000000000000000, -7.449999999999998401, -20.00000000000000000 ) ) ;
#27395=CARTESIAN_POINT ( 'NONE',  ( -8.689999999999999503, 8.750000000000000000, -5.000000000000000000 ) ) ;
#27411=VERTEX_POINT ( 'NONE', #65842 ) ;
#27416=VERTEX_POINT ( 'NONE', #38968 ) ;
#27418=VECTOR ( 'NONE', #51665, 1000.000000000000000 ) ;
#27420=VECTOR ( 'NONE', #2455, 1000.000000000000000 ) ;
#27426=DIRECTION ( 'NONE',  ( -0.000000000000000000, 0.000000000000000000, 1.000000000000000000 ) ) ;
#27446=DIRECTION ( 'NONE',  ( -0.000000000000000000, -0.000000000000000000, 1.000000000000000000 ) ) ;
#27450=CARTESIAN_POINT ( 'NONE',  ( 7.250000000000005329, -8.249999999999998224, -26.00000000000001066 ) ) ;
#27457=ORIENTED_EDGE ( 'NONE', *, *, #44717, .F. ) ;
#27482=PLANE ( 'NONE',  #52547 ) ;
#27487=CARTESIAN_POINT ( 'NONE',  ( 8.250000000000005329, 7.250000000000000888, -12.00000000000000000 ) ) ;
#27509=CARTESIAN_POINT ( 'NONE',  ( 7.250000000000005329, 7.250000000000000888, -16.50000000000000000 ) ) ;
#27517=VERTEX_POINT ( 'NONE', #30097 ) ;
#27520=DIRECTION ( 'NONE',  ( -0.000000000000000000, -0.000000000000000000, -1.000000000000000000 ) ) ;
#27526=DIRECTION ( 'NONE',  ( -0.000000000000000000, -0.000000000000000000, -1.000000000000000000 ) ) ;
#27529=CARTESIAN_POINT ( 'NONE',  ( -7.250000000000000000, -7.449999999999998401, -24.50000000000000000 ) ) ;
#27550=ORIENTED_EDGE ( 'NONE', *, *, #10878, .T. ) ;
#27551=ORIENTED_EDGE ( 'NONE', *, *, #9925, .F. ) ;
#27552=PLANE ( 'NONE',  #12321 ) ;
#27557=EDGE_CURVE ( 'NONE', #5241, #42070, #46356, .T. ) ;
#27562=VERTEX_POINT ( 'NONE', #46355 ) ;
#27563=AXIS2_PLACEMENT_3D ( 'NONE', #19185, #13528, #40403 ) ;
#27568=ORIENTED_EDGE ( 'NONE', *, *, #24696, .T. ) ;
#27569=ADVANCED_FACE ( 'NONE', ( #56620 ), #62979, .T. ) ;
#27572=CYLINDRICAL_SURFACE ( 'NONE', #44955, 0.1999999999999996503 ) ;
#27574=ORIENTED_EDGE ( 'NONE', *, *, #39676, .F. ) ;
#27576=AXIS2_PLACEMENT_3D ( 'NONE', #53489, #19902, #63393 ) ;
#27583=PLANE ( 'NONE',  #35040 ) ;
#27588=CIRCLE ( 'NONE', #12872, 0.1999999999999987899 ) ;
#27598=CARTESIAN_POINT ( 'NONE',  ( 7.250000000000005329, -8.749999999999998224, -26.00000000000001066 ) ) ;
#27599=PLANE ( 'NONE',  #59775 ) ;
#27608=CARTESIAN_POINT ( 'NONE',  ( -7.250000000000000888, 8.250000000000001776, -8.000000000000000000 ) ) ;
#27614=CARTESIAN_POINT ( 'NONE',  ( -8.250000000000001776, 0.000000000000000000, -22.50000000000000000 ) ) ;
#27625=ADVANCED_FACE ( 'NONE', ( #3936 ), #41751, .T. ) ;
#27632=EDGE_CURVE ( 'NONE', #67039, #6107, #11314, .T. ) ;
#27637=EDGE_LOOP ( 'NONE', ( #5206, #14158, #36960, #60797, #66195, #67147 ) ) ;
#27639=CARTESIAN_POINT ( 'NONE',  ( -7.450000000000001954, 0.000000000000000000, -9.500000000000001776 ) ) ;
#27644=EDGE_CURVE ( 'NONE', #20195, #22032, #69328, .T. ) ;
#27649=CARTESIAN_POINT ( 'NONE',  ( -7.250000000000000000, -7.449999999999998401, -21.50000000000000000 ) ) ;
#27653=ORIENTED_EDGE ( 'NONE', *, *, #33208, .T. ) ;
#27656=DIRECTION ( 'NONE',  ( 0.000000000000000000, 0.000000000000000000, 1.000000000000000000 ) ) ;
#27662=ORIENTED_EDGE ( 'NONE', *, *, #40706, .F. ) ;
#27664=AXIS2_PLACEMENT_3D ( 'NONE', #26872, #43812, #22588 ) ;
#27671=ADVANCED_FACE ( 'NONE', ( #38214 ), #27583, .F. ) ;
#27676=DIRECTION ( 'NONE',  ( 0.000000000000000000, -1.000000000000000000, 0.000000000000000000 ) ) ;
#27685=DIRECTION ( 'NONE',  ( 1.000000000000000000, 0.000000000000000000, 0.000000000000000000 ) ) ;
#27688=LINE ( 'NONE', #60549, #27008 ) ;
#27696=FACE_OUTER_BOUND ( 'NONE', #21640, .T. ) ;
#27710=CARTESIAN_POINT ( 'NONE',  ( 0.000000000000000000, -7.449999999999998401, -12.50000000000000000 ) ) ;
#27715=LINE ( 'NONE', #21370, #60433 ) ;
#27718=CIRCLE ( 'NONE', #41227, 1.000000000000000000 ) ;
#27720=EDGE_CURVE ( 'NONE', #24719, #27819, #51971, .T. ) ;
#27724=VERTEX_POINT ( 'NONE', #37855 ) ;
#27744=ORIENTED_EDGE ( 'NONE', *, *, #65703, .T. ) ;
#27748=ORIENTED_EDGE ( 'NONE', *, *, #6103, .F. ) ;
#27749=AXIS2_PLACEMENT_3D ( 'NONE', #61338, #12896, #51800 ) ;
#27751=EDGE_CURVE ( 'NONE', #18134, #7863, #1399, .T. ) ;
#27753=ORIENTED_EDGE ( 'NONE', *, *, #41780, .F. ) ;
#27756=VECTOR ( 'NONE', #42187, 1000.000000000000000 ) ;
#27762=VERTEX_POINT ( 'NONE', #38879 ) ;
#27767=CARTESIAN_POINT ( 'NONE',  ( -7.250000000000000888, 7.250000000000001776, -8.500000000000000000 ) ) ;
#27772=DIRECTION ( 'NONE',  ( 0.000000000000000000, 0.000000000000000000, 1.000000000000000000 ) ) ;
#27782=DIRECTION ( 'NONE',  ( 0.000000000000000000, 0.000000000000000000, -1.000000000000000000 ) ) ;
#27785=ORIENTED_EDGE ( 'NONE', *, *, #65686, .F. ) ;
#27799=CARTESIAN_POINT ( 'NONE',  ( -7.450000000000001954, -7.249999999999998224, -14.50000000000000000 ) ) ;
#27802=EDGE_CURVE ( 'NONE', #35620, #20264, #68936, .T. ) ;
#27818=CARTESIAN_POINT ( 'NONE',  ( 7.250000000000005329, -7.249999999999998224, -9.500000000000001776 ) ) ;
#27819=VERTEX_POINT ( 'NONE', #55153 ) ;
#27830=CARTESIAN_POINT ( 'NONE',  ( 7.749999999999998224, -7.348062532928000934, -5.000000000000000000 ) ) ;
#27837=CARTESIAN_POINT ( 'NONE',  ( 9.690000000000001279, 9.690000000000001279, -5.000000000000000000 ) ) ;
#27838=DIRECTION ( 'NONE',  ( -1.000000000000000000, 0.000000000000000000, 0.000000000000000000 ) ) ;
#27851=ORIENTED_EDGE ( 'NONE', *, *, #20499, .T. ) ;
#27857=VERTEX_POINT ( 'NONE', #55498 ) ;
#27858=VERTEX_POINT ( 'NONE', #44874 ) ;
#27863=CYLINDRICAL_SURFACE ( 'NONE', #55083, 1.000000000000000000 ) ;
#27870=PLANE ( 'NONE',  #69422 ) ;
#27879=CARTESIAN_POINT ( 'NONE',  ( -7.450000000000001954, -7.249999999999998224, -15.50000000000000000 ) ) ;
#27880=ORIENTED_EDGE ( 'NONE', *, *, #64378, .T. ) ;
#27892=ADVANCED_FACE ( 'NONE', ( #29652 ), #41668, .T. ) ;
#27908=CIRCLE ( 'NONE', #64073, 1.000000000000000000 ) ;
#27915=CIRCLE ( 'NONE', #51638, 0.1999999999999996503 ) ;
#27918=ORIENTED_EDGE ( 'NONE', *, *, #22007, .T. ) ;
#27924=FACE_OUTER_BOUND ( 'NONE', #16961, .T. ) ;
#27930=EDGE_CURVE ( 'NONE', #43298, #37385, #59935, .T. ) ;
#27935=CARTESIAN_POINT ( 'NONE',  ( -8.250000000000001776, 0.000000000000000000, -13.00000000000000178 ) ) ;
#27938=DIRECTION ( 'NONE',  ( 1.000000000000000000, 0.000000000000000000, 0.000000000000000000 ) ) ;
#27942=CARTESIAN_POINT ( 'NONE',  ( -8.250000000000001776, 0.000000000000000000, -24.50000000000000000 ) ) ;
#27946=CARTESIAN_POINT ( 'NONE',  ( 9.690000000000001279, 9.690000000000001279, 0.000000000000000000 ) ) ;
#27947=PLANE ( 'NONE',  #50863 ) ;
#27950=EDGE_CURVE ( 'NONE', #7833, #40446, #51589, .T. ) ;
#27951=CARTESIAN_POINT ( 'NONE',  ( -8.250000000000001776, 0.000000000000000000, -17.50000000000000000 ) ) ;
#27961=AXIS2_PLACEMENT_3D ( 'NONE', #64494, #16049, #37621 ) ;
#27962=ORIENTED_EDGE ( 'NONE', *, *, #60350, .T. ) ;
#27966=VERTEX_POINT ( 'NONE', #34951 ) ;
#27980=CARTESIAN_POINT ( 'NONE',  ( 8.250000000000005329, 7.250000000000000888, -26.00000000000001066 ) ) ;
#27987=ORIENTED_EDGE ( 'NONE', *, *, #53763, .F. ) ;
#27993=DIRECTION ( 'NONE',  ( 0.000000000000000000, 0.000000000000000000, 1.000000000000000000 ) ) ;
#27994=DIRECTION ( 'NONE',  ( -1.000000000000000000, 0.000000000000000000, 0.000000000000000000 ) ) ;
#27998=DIRECTION ( 'NONE',  ( -0.000000000000000000, -0.000000000000000000, -1.000000000000000000 ) ) ;
#28001=ORIENTED_EDGE ( 'NONE', *, *, #50884, .T. ) ;
#28003=VERTEX_POINT ( 'NONE', #14461 ) ;
#28009=DIRECTION ( 'NONE',  ( -0.000000000000000000, -0.000000000000000000, 1.000000000000000000 ) ) ;
#28017=ORIENTED_EDGE ( 'NONE', *, *, #35850, .F. ) ;
#28021=CARTESIAN_POINT ( 'NONE',  ( -8.250000000000001776, -8.249999999999998224, -26.00000000000001066 ) ) ;
#28023=ADVANCED_FACE ( 'NONE', ( #1241, #4215 ), #6550, .T. ) ;
#28027=CARTESIAN_POINT ( 'NONE',  ( -7.450000000000001954, -7.249999999999998224, -22.50000000000000000 ) ) ;
#28035=EDGE_CURVE ( 'NONE', #35740, #43050, #42718, .T. ) ;
#28053=DIRECTION ( 'NONE',  ( 0.000000000000000000, 0.000000000000000000, -1.000000000000000000 ) ) ;
#28056=ORIENTED_EDGE ( 'NONE', *, *, #53222, .T. ) ;
#28060=ORIENTED_EDGE ( 'NONE', *, *, #63443, .F. ) ;
#28093=ORIENTED_EDGE ( 'NONE', *, *, #6603, .F. ) ;
#28094=VERTEX_POINT ( 'NONE', #44013 ) ;
#28098=DIRECTION ( 'NONE',  ( 0.000000000000000000, 0.000000000000000000, 1.000000000000000000 ) ) ;
#28104=CARTESIAN_POINT ( 'NONE',  ( 7.450000000000003730, -7.249999999999997335, -14.00000000000000000 ) ) ;
#28111=CARTESIAN_POINT ( 'NONE',  ( 8.250000000000005329, 7.250000000000000888, -9.000000000000001776 ) ) ;
#28117=VECTOR ( 'NONE', #69073, 1000.000000000000000 ) ;
#28118=DIRECTION ( 'NONE',  ( 0.000000000000000000, 1.000000000000000000, -0.000000000000000000 ) ) ;
#28121=FACE_OUTER_BOUND ( 'NONE', #39914, .T. ) ;
#28126=DIRECTION ( 'NONE',  ( 0.000000000000000000, 0.000000000000000000, -1.000000000000000000 ) ) ;
#28138=DIRECTION ( 'NONE',  ( 0.000000000000000000, -0.000000000000000000, 1.000000000000000000 ) ) ;
#28140=AXIS2_PLACEMENT_3D ( 'NONE', #1219, #1905, #23112 ) ;
#28144=ORIENTED_EDGE ( 'NONE', *, *, #51500, .T. ) ;
#28152=ORIENTED_EDGE ( 'NONE', *, *, #9944, .F. ) ;
#28155=ORIENTED_EDGE ( 'NONE', *, *, #54678, .T. ) ;
#28160=AXIS2_PLACEMENT_3D ( 'NONE', #1264, #22493, #12202 ) ;
#28163=EDGE_LOOP ( 'NONE', ( #14995, #17898, #35838, #20254 ) ) ;
#28165=CARTESIAN_POINT ( 'NONE',  ( -7.750000000000001776, 7.750000000000001776, 0.000000000000000000 ) ) ;
#28171=FACE_OUTER_BOUND ( 'NONE', #632, .T. ) ;
#28173=DIRECTION ( 'NONE',  ( 0.000000000000000000, 0.000000000000000000, -1.000000000000000000 ) ) ;
#28180=ORIENTED_EDGE ( 'NONE', *, *, #23226, .F. ) ;
#28181=ADVANCED_FACE ( 'NONE', ( #39400 ), #7576, .T. ) ;
#28184=EDGE_CURVE ( 'NONE', #56406, #43147, #39741, .T. ) ;
#28186=LINE ( 'NONE', #44774, #57235 ) ;
#28192=EDGE_CURVE ( 'NONE', #36247, #50834, #4637, .T. ) ;
#28193=LINE ( 'NONE', #49759, #38056 ) ;
#28199=VECTOR ( 'NONE', #12702, 1000.000000000000000 ) ;
#28200=DIRECTION ( 'NONE',  ( 1.000000000000000000, -0.000000000000000000, 0.000000000000000000 ) ) ;
#28208=DIRECTION ( 'NONE',  ( 0.000000000000000000, 1.000000000000000000, 0.000000000000000000 ) ) ;
#28210=DIRECTION ( 'NONE',  ( 0.000000000000000000, 1.000000000000000000, 0.000000000000000000 ) ) ;
#28213=AXIS2_PLACEMENT_3D ( 'NONE', #64484, #21692, #37265 ) ;
#28215=ORIENTED_EDGE ( 'NONE', *, *, #691, .T. ) ;
#28224=CARTESIAN_POINT ( 'NONE',  ( -7.250000000000000888, 7.250000000000001776, -26.00000000000001066 ) ) ;
#28226=ORIENTED_EDGE ( 'NONE', *, *, #49690, .T. ) ;
#28227=CARTESIAN_POINT ( 'NONE',  ( -7.250000000000000888, -8.249999999999998224, -13.00000000000000178 ) ) ;
#28231=EDGE_CURVE ( 'NONE', #22594, #60163, #13583, .T. ) ;
#28245=AXIS2_PLACEMENT_3D ( 'NONE', #23584, #12964, #67072 ) ;
#28246=CARTESIAN_POINT ( 'NONE',  ( -8.750000000000001776, 0.000000000000000000, -30.00000000000001066 ) ) ;
#28247=CARTESIAN_POINT ( 'NONE',  ( 7.450000000000006395, 7.250000000000000888, -11.50000000000000000 ) ) ;
#28248=DIRECTION ( 'NONE',  ( -1.000000000000000000, 0.000000000000000000, 0.000000000000000000 ) ) ;
#28252=VERTEX_POINT ( 'NONE', #35851 ) ;
#28253=VECTOR ( 'NONE', #57972, 1000.000000000000000 ) ;
#28270=ADVANCED_FACE ( 'NONE', ( #68028 ), #4038, .F. ) ;
#28271=ORIENTED_EDGE ( 'NONE', *, *, #34680, .F. ) ;
#28272=ADVANCED_FACE ( 'NONE', ( #63430 ), #36196, .F. ) ;
#28285=DIRECTION ( 'NONE',  ( 0.000000000000000000, 0.000000000000000000, -1.000000000000000000 ) ) ;
#28288=AXIS2_PLACEMENT_3D ( 'NONE', #22629, #29299, #60099 ) ;
#28297=CARTESIAN_POINT ( 'NONE',  ( 7.250000000000005329, -7.249999999999998224, -22.00000000000000000 ) ) ;
#28299=VERTEX_POINT ( 'NONE', #14992 ) ;
#28305=VECTOR ( 'NONE', #54957, 1000.000000000000000 ) ;
#28307=ORIENTED_EDGE ( 'NONE', *, *, #18596, .F. ) ;
#28310=ORIENTED_EDGE ( 'NONE', *, *, #48734, .T. ) ;
#28312=CARTESIAN_POINT ( 'NONE',  ( 10.50000000000000000, -9.690000000000001279, -5.000000000000000000 ) ) ;
#28318=ORIENTED_EDGE ( 'NONE', *, *, #47440, .T. ) ;
#28325=DIRECTION ( 'NONE',  ( 1.000000000000000000, -0.000000000000000000, 0.000000000000000000 ) ) ;
#28329=FACE_OUTER_BOUND ( 'NONE', #27025, .T. ) ;
#28336=CIRCLE ( 'NONE', #64501, 0.2000000000000005107 ) ;
#28338=CIRCLE ( 'NONE', #54354, 0.2000000000000005107 ) ;
#28347=AXIS2_PLACEMENT_3D ( 'NONE', #1980, #33800, #6597 ) ;
#28353=VECTOR ( 'NONE', #14104, 1000.000000000000000 ) ;
#28358=ORIENTED_EDGE ( 'NONE', *, *, #57933, .T. ) ;
#28386=LINE ( 'NONE', #23440, #64369 ) ;
#28389=LINE ( 'NONE', #49620, #47145 ) ;
#28390=DIRECTION ( 'NONE',  ( 0.000000000000000000, 0.000000000000000000, 1.000000000000000000 ) ) ;
#28420=EDGE_CURVE ( 'NONE', #54414, #18330, #69029, .T. ) ;
#28422=LINE ( 'NONE', #22782, #45209 ) ;
#28423=ORIENTED_EDGE ( 'NONE', *, *, #27268, .F. ) ;
#28426=VERTEX_POINT ( 'NONE', #38641 ) ;
#28441=CARTESIAN_POINT ( 'NONE',  ( 7.250000000000005329, -8.249999999999998224, -14.00000000000000000 ) ) ;
#28443=ADVANCED_FACE ( 'NONE', ( #54916 ), #835, .F. ) ;
#28446=CARTESIAN_POINT ( 'NONE',  ( 9.689999999999999503, -10.50000000000000178, -5.000000000000000000 ) ) ;
#28459=PLANE ( 'NONE',  #18611 ) ;
#28469=LINE ( 'NONE', #44728, #3411 ) ;
#28471=CARTESIAN_POINT ( 'NONE',  ( -8.250000000000001776, -7.249999999999998224, -19.00000000000000000 ) ) ;
#28473=DIRECTION ( 'NONE',  ( -1.000000000000000000, 0.000000000000000000, 0.000000000000000000 ) ) ;
#28479=CARTESIAN_POINT ( 'NONE',  ( -7.450000000000001954, 7.250000000000000000, -7.500000000000000000 ) ) ;
#28483=AXIS2_PLACEMENT_3D ( 'NONE', #35021, #51294, #7798 ) ;
#28487=AXIS2_PLACEMENT_3D ( 'NONE', #52888, #69124, #20678 ) ;
#28492=CARTESIAN_POINT ( 'NONE',  ( 8.250000000000005329, -7.249999999999998224, -26.00000000000001066 ) ) ;
#28493=CARTESIAN_POINT ( 'NONE',  ( -8.689999999999999503, -9.750000000000001776, -7.000000000000000000 ) ) ;
#28501=PLANE ( 'NONE',  #25609 ) ;
#28504=LINE ( 'NONE', #11545, #31675 ) ;
#28516=ADVANCED_FACE ( 'NONE', ( #37262 ), #26647, .F. ) ;
#28518=CARTESIAN_POINT ( 'NONE',  ( -7.250000000000001776, -7.249999999999998224, -19.00000000000000000 ) ) ;
#28523=DIRECTION ( 'NONE',  ( -1.000000000000000000, 0.000000000000000000, 0.000000000000000000 ) ) ;
#28536=CARTESIAN_POINT ( 'NONE',  ( -8.250000000000001776, -7.249999999999998224, -11.00000000000000000 ) ) ;
#28553=ORIENTED_EDGE ( 'NONE', *, *, #11730, .T. ) ;
#28556=LINE ( 'NONE', #50130, #11732 ) ;
#28558=CIRCLE ( 'NONE', #48932, 1.000000000000000000 ) ;
#28559=LINE ( 'NONE', #55449, #42950 ) ;
#28570=VECTOR ( 'NONE', #54249, 1000.000000000000000 ) ;
#28576=VERTEX_POINT ( 'NONE', #18091 ) ;
#28581=VERTEX_POINT ( 'NONE', #61930 ) ;
#28584=DIRECTION ( 'NONE',  ( -1.000000000000000000, 0.000000000000000000, 0.000000000000000000 ) ) ;
#28589=DIRECTION ( 'NONE',  ( -1.000000000000000000, 0.000000000000000000, -0.000000000000000000 ) ) ;
#28599=AXIS2_PLACEMENT_3D ( 'NONE', #13803, #40334, #61897 ) ;
#28605=CARTESIAN_POINT ( 'NONE',  ( -8.250000000000001776, 0.000000000000000000, -17.00000000000000000 ) ) ;
#28613=DIRECTION ( 'NONE',  ( 1.000000000000000000, -5.981805089575194965E-17, 0.000000000000000000 ) ) ;
#28618=CARTESIAN_POINT ( 'NONE',  ( 7.250000000000005329, -7.249999999999998224, -26.00000000000001066 ) ) ;
#28625=PLANE ( 'NONE',  #7570 ) ;
#28644=DIRECTION ( 'NONE',  ( 0.000000000000000000, 0.000000000000000000, 1.000000000000000000 ) ) ;
#28651=VERTEX_POINT ( 'NONE', #2190 ) ;
#28661=VECTOR ( 'NONE', #37568, 1000.000000000000000 ) ;
#28662=VECTOR ( 'NONE', #56040, 1000.000000000000000 ) ;
#28663=CARTESIAN_POINT ( 'NONE',  ( 7.250000000000005329, 7.250000000000000888, -30.00000000000001066 ) ) ;
#28668=CARTESIAN_POINT ( 'NONE',  ( 7.450000000000006395, 7.250000000000000888, -12.00000000000000000 ) ) ;
#28669=ORIENTED_EDGE ( 'NONE', *, *, #69008, .T. ) ;
#28677=DIRECTION ( 'NONE',  ( -0.000000000000000000, -0.000000000000000000, 1.000000000000000000 ) ) ;
#28688=CARTESIAN_POINT ( 'NONE',  ( 7.250000000000005329, 7.250000000000000888, -30.00000000000001066 ) ) ;
#28690=CIRCLE ( 'NONE', #30978, 1.000000000000000000 ) ;
#28697=AXIS2_PLACEMENT_3D ( 'NONE', #5753, #48888, #43911 ) ;
#28704=EDGE_CURVE ( 'NONE', #59416, #48640, #68991, .T. ) ;
#28705=CYLINDRICAL_SURFACE ( 'NONE', #11806, 1.000000000000002665 ) ;
#28707=AXIS2_PLACEMENT_3D ( 'NONE', #41457, #58069, #42507 ) ;
#28708=AXIS2_PLACEMENT_3D ( 'NONE', #24582, #58151, #57795 ) ;
#28712=EDGE_CURVE ( 'NONE', #6107, #67217, #35397, .T. ) ;
#28714=AXIS2_PLACEMENT_3D ( 'NONE', #49125, #21562, #16252 ) ;
#28719=CYLINDRICAL_SURFACE ( 'NONE', #23057, 0.1999999999999987899 ) ;
#28728=SURFACE_STYLE_USAGE ( .BOTH. , #43621 ) ;
#28729=PLANE ( 'NONE',  #313 ) ;
#28739=CIRCLE ( 'NONE', #63796, 1.000000000000000000 ) ;
#28744=VERTEX_POINT ( 'NONE', #63699 ) ;
#28749=EDGE_CURVE ( 'NONE', #34855, #23968, #25159, .T. ) ;
#28774=ORIENTED_EDGE ( 'NONE', *, *, #52760, .F. ) ;
#28782=ORIENTED_EDGE ( 'NONE', *, *, #33651, .F. ) ;
#28788=VERTEX_POINT ( 'NONE', #25869 ) ;
#28794=ORIENTED_EDGE ( 'NONE', *, *, #27720, .F. ) ;
#28798=DIRECTION ( 'NONE',  ( 0.000000000000000000, 0.000000000000000000, 1.000000000000000000 ) ) ;
#28802=EDGE_CURVE ( 'NONE', #61047, #68976, #20550, .T. ) ;
#28803=DIRECTION ( 'NONE',  ( -1.000000000000000000, 0.000000000000000000, 0.000000000000000000 ) ) ;
#28805=DIRECTION ( 'NONE',  ( 1.000000000000000000, 0.000000000000000000, 0.000000000000000000 ) ) ;
#28811=CARTESIAN_POINT ( 'NONE',  ( 7.250000000000005329, -7.249999999999998224, -20.50000000000000000 ) ) ;
#28836=LINE ( 'NONE', #56764, #20736 ) ;
#28846=CARTESIAN_POINT ( 'NONE',  ( 0.000000000000000000, 8.250000000000001776, -20.50000000000000000 ) ) ;
#28850=VERTEX_POINT ( 'NONE', #43856 ) ;
#28861=EDGE_LOOP ( 'NONE', ( #41982, #66273, #14763, #2134 ) ) ;
#28866=LINE ( 'NONE', #23221, #48224 ) ;
#28872=EDGE_LOOP ( 'NONE', ( #7801, #56627 ) ) ;
#28873=VERTEX_POINT ( 'NONE', #59433 ) ;
#28874=EDGE_CURVE ( 'NONE', #60123, #43073, #5844, .T. ) ;
#28879=DIRECTION ( 'NONE',  ( 0.000000000000000000, 0.000000000000000000, -1.000000000000000000 ) ) ;
#28885=DIRECTION ( 'NONE',  ( -1.000000000000000000, 0.000000000000000000, -0.000000000000000000 ) ) ;
#28889=AXIS2_PLACEMENT_3D ( 'NONE', #4295, #25501, #47063 ) ;
#28898=EDGE_LOOP ( 'NONE', ( #33164, #34302, #5209, #41131 ) ) ;
#28899=CARTESIAN_POINT ( 'NONE',  ( 8.250000000000005329, 0.000000000000000000, -25.50000000000000355 ) ) ;
#28910=CARTESIAN_POINT ( 'NONE',  ( 7.450000000000006395, 7.250000000000000888, -15.50000000000000000 ) ) ;
#28912=EDGE_CURVE ( 'NONE', #6104, #64750, #37867, .T. ) ;
#28913=DIRECTION ( 'NONE',  ( 0.000000000000000000, -1.000000000000000000, 0.000000000000000000 ) ) ;
#28916=EDGE_CURVE ( 'NONE', #23540, #12421, #64397, .T. ) ;
#28918=VERTEX_POINT ( 'NONE', #37522 ) ;
#28926=EDGE_CURVE ( 'NONE', #9481, #48587, #56652, .T. ) ;
#28928=VERTEX_POINT ( 'NONE', #59776 ) ;
#28934=VECTOR ( 'NONE', #30910, 1000.000000000000000 ) ;
#28938=DIRECTION ( 'NONE',  ( 1.000000000000000000, 0.000000000000000000, 0.000000000000000000 ) ) ;
#28939=ORIENTED_EDGE ( 'NONE', *, *, #13665, .F. ) ;
#28958=CARTESIAN_POINT ( 'NONE',  ( -9.690000000000001279, -8.750000000000000000, -7.000000000000000000 ) ) ;
#28960=CARTESIAN_POINT ( 'NONE',  ( -7.250000000000000888, 7.450000000000003730, -16.00000000000000000 ) ) ;
#28968=FACE_OUTER_BOUND ( 'NONE', #67371, .T. ) ;
#28970=EDGE_LOOP ( 'NONE', ( #39466, #51931, #46925, #34759, #13653, #42249, #25231, #62920 ) ) ;
#28971=LINE ( 'NONE', #22299, #58353 ) ;
#28975=EDGE_CURVE ( 'NONE', #33710, #55788, #44527, .T. ) ;
#28976=CARTESIAN_POINT ( 'NONE',  ( 8.690000000000001279, -9.750000000000001776, -5.000000000000000000 ) ) ;
#28979=CARTESIAN_POINT ( 'NONE',  ( -8.250000000000001776, 0.000000000000000000, -18.50000000000000000 ) ) ;
#28980=ORIENTED_EDGE ( 'NONE', *, *, #36219, .F. ) ;
#28982=CYLINDRICAL_SURFACE ( 'NONE', #7843, 1.000000000000000000 ) ;
#28992=DIRECTION ( 'NONE',  ( -0.000000000000000000, 0.000000000000000000, 1.000000000000000000 ) ) ;
#28996=LINE ( 'NONE', #66478, #4144 ) ;
#28998=VECTOR ( 'NONE', #16898, 1000.000000000000000 ) ;
#28999=LINE ( 'NONE', #66817, #22400 ) ;
#29001=AXIS2_PLACEMENT_3D ( 'NONE', #40115, #29520, #3352 ) ;
#29009=VECTOR ( 'NONE', #19664, 1000.000000000000000 ) ;
#29013=LINE ( 'NONE', #46931, #56614 ) ;
#29015=EDGE_LOOP ( 'NONE', ( #2580, #32183, #37934, #31799 ) ) ;
#29021=ADVANCED_FACE ( 'NONE', ( #13409 ), #55510, .F. ) ;
#29023=CARTESIAN_POINT ( 'NONE',  ( -7.250000000000001776, -7.249999999999998224, -17.50000000000000000 ) ) ;
#29026=EDGE_CURVE ( 'NONE', #22338, #27411, #39238, .T. ) ;
#29027=DIRECTION ( 'NONE',  ( -1.000000000000000000, 0.000000000000000000, 0.000000000000000000 ) ) ;
#29029=LINE ( 'NONE', #32953, #32315 ) ;
#29037=ORIENTED_EDGE ( 'NONE', *, *, #1696, .T. ) ;
#29040=FACE_OUTER_BOUND ( 'NONE', #42165, .T. ) ;
#29042=ORIENTED_EDGE ( 'NONE', *, *, #68272, .T. ) ;
#29050=VECTOR ( 'NONE', #2218, 1000.000000000000000 ) ;
#29056=VERTEX_POINT ( 'NONE', #50191 ) ;
#29058=CARTESIAN_POINT ( 'NONE',  ( -7.250000000000000888, 8.250000000000001776, -21.00000000000000000 ) ) ;
#29063=EDGE_CURVE ( 'NONE', #67323, #59830, #10387, .T. ) ;
#29064=DIRECTION ( 'NONE',  ( 0.000000000000000000, 0.000000000000000000, 1.000000000000000000 ) ) ;
#29066=FACE_OUTER_BOUND ( 'NONE', #24769, .T. ) ;
#29071=VERTEX_POINT ( 'NONE', #39916 ) ;
#29078=ADVANCED_FACE ( 'NONE', ( #13050 ), #34620, .T. ) ;
#29092=CARTESIAN_POINT ( 'NONE',  ( -7.250000000000000888, -8.249999999999998224, -26.00000000000001066 ) ) ;
#29093=FACE_OUTER_BOUND ( 'NONE', #46053, .T. ) ;
#29108=FACE_OUTER_BOUND ( 'NONE', #23276, .T. ) ;
#29109=CARTESIAN_POINT ( 'NONE',  ( -7.250000000000000888, 8.250000000000001776, -18.00000000000000000 ) ) ;
#29122=LINE ( 'NONE', #61275, #39434 ) ;
#29125=VERTEX_POINT ( 'NONE', #14471 ) ;
#29128=EDGE_LOOP ( 'NONE', ( #68459, #38047, #31757, #14574 ) ) ;
#29129=VERTEX_POINT ( 'NONE', #29664 ) ;
#29134=EDGE_LOOP ( 'NONE', ( #67783, #47870, #57720, #20960, #21911, #34783, #63012, #5587 ) ) ;
#29142=CARTESIAN_POINT ( 'NONE',  ( 7.250000000000005329, 7.250000000000000888, -26.00000000000001066 ) ) ;
#29148=AXIS2_PLACEMENT_3D ( 'NONE', #7694, #8036, #23963 ) ;
#29159=DIRECTION ( 'NONE',  ( 0.000000000000000000, 0.000000000000000000, -1.000000000000000000 ) ) ;
#29168=VERTEX_POINT ( 'NONE', #3859 ) ;
#29169=DIRECTION ( 'NONE',  ( 0.000000000000000000, -1.000000000000000000, 0.000000000000000000 ) ) ;
#29171=FACE_OUTER_BOUND ( 'NONE', #51059, .T. ) ;
#29173=VERTEX_POINT ( 'NONE', #25787 ) ;
#29174=DIRECTION ( 'NONE',  ( 1.000000000000000000, 0.000000000000000000, 0.000000000000000000 ) ) ;
#29175=ORIENTED_EDGE ( 'NONE', *, *, #33293, .F. ) ;
#29183=DIRECTION ( 'NONE',  ( 0.000000000000000000, 0.000000000000000000, 1.000000000000000000 ) ) ;
#29184=ORIENTED_EDGE ( 'NONE', *, *, #13662, .F. ) ;
#29185=ORIENTED_EDGE ( 'NONE', *, *, #51832, .F. ) ;
#29219=EDGE_LOOP ( 'NONE', ( #54723, #1642, #2941, #6167 ) ) ;
#29229=CARTESIAN_POINT ( 'NONE',  ( -7.250000000000000888, 7.450000000000003730, -22.50000000000000000 ) ) ;
#29231=ADVANCED_FACE ( 'NONE', ( #67520 ), #19065, .T. ) ;
#29240=LINE ( 'NONE', #8374, #50789 ) ;
#29242=DIRECTION ( 'NONE',  ( 1.000000000000000000, 0.000000000000000000, 0.000000000000000000 ) ) ;
#29250=DIRECTION ( 'NONE',  ( 0.000000000000000000, 0.000000000000000000, 1.000000000000000000 ) ) ;
#29251=EDGE_LOOP ( 'NONE', ( #54641, #9287, #65855, #48033 ) ) ;
#29253=EDGE_CURVE ( 'NONE', #12885, #39877, #66838, .T. ) ;
#29260=ORIENTED_EDGE ( 'NONE', *, *, #62478, .T. ) ;
#29261=ORIENTED_EDGE ( 'NONE', *, *, #25167, .F. ) ;
#29262=CARTESIAN_POINT ( 'NONE',  ( 8.250000000000005329, -8.249999999999998224, -26.00000000000001066 ) ) ;
#29265=CARTESIAN_POINT ( 'NONE',  ( 7.450000000000006395, 7.250000000000000888, -11.50000000000000000 ) ) ;
#29266=CARTESIAN_POINT ( 'NONE',  ( 7.250000000000005329, -8.249999999999998224, -20.50000000000000000 ) ) ;
#29268=VECTOR ( 'NONE', #39467, 1000.000000000000000 ) ;
#29270=CARTESIAN_POINT ( 'NONE',  ( 8.250000000000005329, -8.249999999999998224, -26.00000000000001066 ) ) ;
#29276=ORIENTED_EDGE ( 'NONE', *, *, #36883, .F. ) ;
#29278=EDGE_CURVE ( 'NONE', #57470, #997, #69257, .T. ) ;
#29283=CARTESIAN_POINT ( 'NONE',  ( 7.250000000000005329, 7.250000000000000888, -26.00000000000001066 ) ) ;
#29288=EDGE_CURVE ( 'NONE', #59582, #61023, #43416, .T. ) ;
#29297=PLANE ( 'NONE',  #9897 ) ;
#29299=DIRECTION ( 'NONE',  ( 0.000000000000000000, 0.000000000000000000, -1.000000000000000000 ) ) ;
#29303=DIRECTION ( 'NONE',  ( 0.000000000000000000, 0.000000000000000000, 1.000000000000000000 ) ) ;
#29311=AXIS2_PLACEMENT_3D ( 'NONE', #9836, #25388, #63578 ) ;
#29314=DIRECTION ( 'NONE',  ( -1.000000000000000000, 1.794541526872559352E-16, 0.000000000000000000 ) ) ;
#29315=DIRECTION ( 'NONE',  ( 0.000000000000000000, -1.000000000000000000, 0.000000000000000000 ) ) ;
#29335=DIRECTION ( 'NONE',  ( -0.000000000000000000, -0.000000000000000000, 1.000000000000000000 ) ) ;
#29337=AXIS2_PLACEMENT_3D ( 'NONE', #43031, #64609, #16522 ) ;
#29346=VECTOR ( 'NONE', #6991, 1000.000000000000000 ) ;
#29352=VERTEX_POINT ( 'NONE', #32484 ) ;
#29355=VECTOR ( 'NONE', #59108, 1000.000000000000000 ) ;
#29359=DIRECTION ( 'NONE',  ( -0.000000000000000000, -0.000000000000000000, -1.000000000000000000 ) ) ;
#29379=EDGE_CURVE ( 'NONE', #51438, #31236, #17578, .T. ) ;
#29388=VECTOR ( 'NONE', #19491, 1000.000000000000000 ) ;
#29392=EDGE_CURVE ( 'NONE', #28928, #37936, #65683, .T. ) ;
#29400=LINE ( 'NONE', #20197, #11328 ) ;
#29422=ORIENTED_EDGE ( 'NONE', *, *, #65869, .F. ) ;
#29425=DIRECTION ( 'NONE',  ( 0.000000000000000000, 0.000000000000000000, 1.000000000000000000 ) ) ;
#29428=AXIS2_PLACEMENT_3D ( 'NONE', #40953, #67837, #62510 ) ;
#29429=DIRECTION ( 'NONE',  ( -1.000000000000000000, 0.000000000000000000, 0.000000000000000000 ) ) ;
#29430=ORIENTED_EDGE ( 'NONE', *, *, #8976, .F. ) ;
#29433=CARTESIAN_POINT ( 'NONE',  ( -7.250000000000000888, 7.450000000000003730, -7.500000000000000000 ) ) ;
#29456=EDGE_CURVE ( 'NONE', #47564, #63930, #7663, .T. ) ;
#29469=CARTESIAN_POINT ( 'NONE',  ( -7.450000000000001954, 0.000000000000000000, -14.00000000000000000 ) ) ;
#29479=VERTEX_POINT ( 'NONE', #2369 ) ;
#29482=ORIENTED_EDGE ( 'NONE', *, *, #48028, .T. ) ;
#29485=LINE ( 'NONE', #51054, #4724 ) ;
#29486=CIRCLE ( 'NONE', #31783, 0.2000000000000005107 ) ;
#29501=ORIENTED_EDGE ( 'NONE', *, *, #60910, .T. ) ;
#29507=CIRCLE ( 'NONE', #46467, 1.500000000000000444 ) ;
#29509=CIRCLE ( 'NONE', #21610, 0.1999999999999987899 ) ;
#29520=DIRECTION ( 'NONE',  ( -0.000000000000000000, -0.000000000000000000, 1.000000000000000000 ) ) ;
#29522=VERTEX_POINT ( 'NONE', #57854 ) ;
#29524=DIRECTION ( 'NONE',  ( -0.000000000000000000, -0.000000000000000000, -1.000000000000000000 ) ) ;
#29528=VERTEX_POINT ( 'NONE', #3420 ) ;
#29529=DIRECTION ( 'NONE',  ( -1.000000000000000000, 0.000000000000000000, 0.000000000000000000 ) ) ;
#29535=DIRECTION ( 'NONE',  ( 0.000000000000000000, 0.000000000000000000, -1.000000000000000000 ) ) ;
#29538=ORIENTED_EDGE ( 'NONE', *, *, #45368, .F. ) ;
#29543=VECTOR ( 'NONE', #38225, 1000.000000000000000 ) ;
#29549=ORIENTED_EDGE ( 'NONE', *, *, #61652, .T. ) ;
#29550=EDGE_LOOP ( 'NONE', ( #66268, #14275, #16020, #61646 ) ) ;
#29562=ORIENTED_EDGE ( 'NONE', *, *, #23954, .T. ) ;
#29566=DIRECTION ( 'NONE',  ( 0.000000000000000000, -1.000000000000000000, -0.000000000000000000 ) ) ;
#29569=CARTESIAN_POINT ( 'NONE',  ( -7.250000000000000888, 8.250000000000001776, -20.50000000000000000 ) ) ;
#29572=ORIENTED_EDGE ( 'NONE', *, *, #5347, .T. ) ;
#29575=FACE_OUTER_BOUND ( 'NONE', #48553, .T. ) ;
#29583=ORIENTED_EDGE ( 'NONE', *, *, #57339, .T. ) ;
#29591=AXIS2_PLACEMENT_3D ( 'NONE', #46502, #62406, #2671 ) ;
#29597=CARTESIAN_POINT ( 'NONE',  ( 4.456444791733522252E-16, 7.450000000000002842, -20.00000000000000000 ) ) ;
#29604=CARTESIAN_POINT ( 'NONE',  ( -7.450000000000001954, 0.000000000000000000, -11.50000000000000000 ) ) ;
#29608=ORIENTED_EDGE ( 'NONE', *, *, #66040, .F. ) ;
#29620=PRODUCT_DEFINITION_CONTEXT ( 'detailed design', #45367, 'design' ) ;
#29626=EDGE_LOOP ( 'NONE', ( #20442, #17740, #29482, #61537, #20205, #44885, #60233, #50309 ) ) ;
#29632=EDGE_CURVE ( 'NONE', #11295, #54217, #34874, .T. ) ;
#29644=CARTESIAN_POINT ( 'NONE',  ( 0.000000000000000000, -7.449999999999998401, -8.500000000000000000 ) ) ;
#29648=FACE_OUTER_BOUND ( 'NONE', #27313, .T. ) ;
#29652=FACE_OUTER_BOUND ( 'NONE', #6414, .T. ) ;
#29654=AXIS2_PLACEMENT_3D ( 'NONE', #21379, #48261, #33029 ) ;
#29655=DIRECTION ( 'NONE',  ( 1.000000000000000000, 0.000000000000000000, 0.000000000000000000 ) ) ;
#29660=ORIENTED_EDGE ( 'NONE', *, *, #41775, .T. ) ;
#29664=CARTESIAN_POINT ( 'NONE',  ( 8.250000000000005329, 7.250000000000000888, -26.00000000000001066 ) ) ;
#29667=VECTOR ( 'NONE', #26835, 1000.000000000000000 ) ;
#29668=DIRECTION ( 'NONE',  ( -0.000000000000000000, 0.000000000000000000, 1.000000000000000000 ) ) ;
#29675=LINE ( 'NONE', #50895, #54963 ) ;
#29678=ORIENTED_EDGE ( 'NONE', *, *, #8467, .T. ) ;
#29690=CARTESIAN_POINT ( 'NONE',  ( 7.250000000000005329, -7.449999999999998401, -16.50000000000000000 ) ) ;
#29706=CARTESIAN_POINT ( 'NONE',  ( -8.250000000000001776, -7.249999999999998224, -14.00000000000000000 ) ) ;
#29707=CARTESIAN_POINT ( 'NONE',  ( -9.690000000000001279, -8.750000000000000000, -5.000000000000000000 ) ) ;
#29708=VECTOR ( 'NONE', #31571, 1000.000000000000000 ) ;
#29713=VECTOR ( 'NONE', #41352, 1000.000000000000000 ) ;
#29721=EDGE_LOOP ( 'NONE', ( #8873, #5568, #56481, #64153 ) ) ;
#29726=ADVANCED_FACE ( 'NONE', ( #42990 ), #59258, .T. ) ;
#29733=FACE_OUTER_BOUND ( 'NONE', #54956, .T. ) ;
#29752=CARTESIAN_POINT ( 'NONE',  ( 7.450000000000006395, 7.250000000000000888, -10.50000000000000000 ) ) ;
#29758=ORIENTED_EDGE ( 'NONE', *, *, #61674, .F. ) ;
#29763=DIRECTION ( 'NONE',  ( 0.000000000000000000, 0.000000000000000000, 1.000000000000000000 ) ) ;
#29765=DIRECTION ( 'NONE',  ( 0.000000000000000000, 1.000000000000000000, 0.000000000000000000 ) ) ;
#29767=AXIS2_PLACEMENT_3D ( 'NONE', #16819, #38382, #11490 ) ;
#29779=VERTEX_POINT ( 'NONE', #5522 ) ;
#29780=ADVANCED_FACE ( 'NONE', ( #16478 ), #11158, .F. ) ;
#29787=EDGE_CURVE ( 'NONE', #58661, #25681, #50023, .T. ) ;
#29792=VERTEX_POINT ( 'NONE', #49002 ) ;
#29793=ORIENTED_EDGE ( 'NONE', *, *, #50771, .T. ) ;
#29794=LINE ( 'NONE', #60920, #69049 ) ;
#29814=VECTOR ( 'NONE', #20136, 1000.000000000000000 ) ;
#29821=ORIENTED_EDGE ( 'NONE', *, *, #7910, .T. ) ;
#29832=CARTESIAN_POINT ( 'NONE',  ( -8.250000000000001776, 0.000000000000000000, -19.00000000000000000 ) ) ;
#29834=AXIS2_PLACEMENT_3D ( 'NONE', #44108, #60360, #44789 ) ;
#29838=AXIS2_PLACEMENT_3D ( 'NONE', #13107, #50598, #55898 ) ;
#29840=DIRECTION ( 'NONE',  ( -0.000000000000000000, -0.000000000000000000, 1.000000000000000000 ) ) ;
#29841=LINE ( 'NONE', #45049, #51477 ) ;
#29842=CARTESIAN_POINT ( 'NONE',  ( -2.500000000000000000, 0.000000000000000000, -30.00000000000001066 ) ) ;
#29846=CARTESIAN_POINT ( 'NONE',  ( -9.750000000000001776, 9.690000000000001279, -4.250000000000000000 ) ) ;
#29861=VECTOR ( 'NONE', #29169, 1000.000000000000000 ) ;
#29872=CARTESIAN_POINT ( 'NONE',  ( 7.250000000000004441, 7.450000000000001954, -24.00000000000000000 ) ) ;
#29874=CARTESIAN_POINT ( 'NONE',  ( 4.456444791733522252E-16, 7.450000000000002842, -17.50000000000000000 ) ) ;
#29879=ORIENTED_EDGE ( 'NONE', *, *, #35478, .F. ) ;
#29880=CARTESIAN_POINT ( 'NONE',  ( 0.000000000000000000, 8.250000000000001776, -22.00000000000000000 ) ) ;
#29881=ORIENTED_EDGE ( 'NONE', *, *, #46867, .T. ) ;
#29897=ORIENTED_EDGE ( 'NONE', *, *, #3537, .T. ) ;
#29900=EDGE_CURVE ( 'NONE', #66278, #46124, #35147, .T. ) ;
#29901=DIRECTION ( 'NONE',  ( 1.000000000000000000, 0.000000000000000000, 0.000000000000000000 ) ) ;
#29905=ORIENTED_EDGE ( 'NONE', *, *, #37699, .T. ) ;
#29908=LINE ( 'NONE', #51127, #13442 ) ;
#29910=CARTESIAN_POINT ( 'NONE',  ( 7.250000000000005329, -7.449999999999998401, -15.50000000000000000 ) ) ;
#29913=CARTESIAN_POINT ( 'NONE',  ( 7.250000000000005329, 7.250000000000000888, -20.00000000000000000 ) ) ;
#29917=CIRCLE ( 'NONE', #69456, 0.2000000000000005107 ) ;
#29922=ADVANCED_FACE ( 'NONE', ( #2289, #47094 ), #40101, .T. ) ;
#29929=PLANE ( 'NONE',  #5017 ) ;
#29936=EDGE_CURVE ( 'NONE', #69235, #190, #14918, .T. ) ;
#29937=VERTEX_POINT ( 'NONE', #18904 ) ;
#29938=DIRECTION ( 'NONE',  ( 0.000000000000000000, 0.000000000000000000, 1.000000000000000000 ) ) ;
#29940=FACE_BOUND ( 'NONE', #7334, .T. ) ;
#29963=ORIENTED_EDGE ( 'NONE', *, *, #45715, .T. ) ;
#29970=EDGE_LOOP ( 'NONE', ( #61927, #26556, #24069, #50352 ) ) ;
#29977=ORIENTED_EDGE ( 'NONE', *, *, #8300, .T. ) ;
#29984=VECTOR ( 'NONE', #63707, 1000.000000000000000 ) ;
#29986=EDGE_CURVE ( 'NONE', #11455, #6920, #47775, .T. ) ;
#29991=ORIENTED_EDGE ( 'NONE', *, *, #55268, .T. ) ;
#30000=ORIENTED_EDGE ( 'NONE', *, *, #9600, .F. ) ;
#30005=ORIENTED_EDGE ( 'NONE', *, *, #11901, .T. ) ;
#30018=ORIENTED_EDGE ( 'NONE', *, *, #30137, .T. ) ;
#30023=DIRECTION ( 'NONE',  ( -1.000000000000000000, 0.000000000000000000, 0.000000000000000000 ) ) ;
#30024=CARTESIAN_POINT ( 'NONE',  ( 0.000000000000000000, -8.249999999999998224, -20.00000000000000000 ) ) ;
#30025=AXIS2_PLACEMENT_3D ( 'NONE', #11143, #59930, #32714 ) ;
#30029=EDGE_CURVE ( 'NONE', #31517, #50228, #63713, .T. ) ;
#30032=DIRECTION ( 'NONE',  ( 1.000000000000000000, 0.000000000000000000, 0.000000000000000000 ) ) ;
#30034=CIRCLE ( 'NONE', #16472, 1.000000000000000000 ) ;
#30050=EDGE_LOOP ( 'NONE', ( #58705, #11197, #49815, #38875 ) ) ;
#30063=DIRECTION ( 'NONE',  ( -1.000000000000000000, 0.000000000000000000, 0.000000000000000000 ) ) ;
#30064=ORIENTED_EDGE ( 'NONE', *, *, #25391, .F. ) ;
#30067=CYLINDRICAL_SURFACE ( 'NONE', #6688, 0.1999999999999996503 ) ;
#30074=AXIS2_PLACEMENT_3D ( 'NONE', #32617, #54188, #27310 ) ;
#30075=AXIS2_PLACEMENT_3D ( 'NONE', #39538, #18672, #8404 ) ;
#30091=LINE ( 'NONE', #68973, #27418 ) ;
#30092=DIRECTION ( 'NONE',  ( 1.000000000000000000, 0.000000000000000000, 0.000000000000000000 ) ) ;
#30095=DIRECTION ( 'NONE',  ( -0.000000000000000000, 0.000000000000000000, -1.000000000000000000 ) ) ;
#30097=CARTESIAN_POINT ( 'NONE',  ( 7.450000000000003730, -7.249999999999997335, -13.50000000000000178 ) ) ;
#30103=ORIENTED_EDGE ( 'NONE', *, *, #26617, .T. ) ;
#30108=DIRECTION ( 'NONE',  ( 0.000000000000000000, 0.000000000000000000, 1.000000000000000000 ) ) ;
#30110=CARTESIAN_POINT ( 'NONE',  ( -7.250000000000000000, -7.449999999999998401, -13.00000000000000178 ) ) ;
#30111=VECTOR ( 'NONE', #69330, 1000.000000000000000 ) ;
#30132=ORIENTED_EDGE ( 'NONE', *, *, #4303, .T. ) ;
#30133=EDGE_CURVE ( 'NONE', #36865, #7150, #5987, .T. ) ;
#30134=VECTOR ( 'NONE', #47674, 1000.000000000000000 ) ;
#30137=EDGE_CURVE ( 'NONE', #51421, #31198, #15025, .T. ) ;
#30148=PLANE ( 'NONE',  #66747 ) ;
#30150=ORIENTED_EDGE ( 'NONE', *, *, #55581, .F. ) ;
#30154=DIRECTION ( 'NONE',  ( 0.000000000000000000, 1.000000000000000000, 0.000000000000000000 ) ) ;
#30158=PLANE ( 'NONE',  #4901 ) ;
#30167=AXIS2_PLACEMENT_3D ( 'NONE', #46898, #51517, #35951 ) ;
#30173=AXIS2_PLACEMENT_3D ( 'NONE', #497, #60573, #44642 ) ;
#30175=CARTESIAN_POINT ( 'NONE',  ( 8.250000000000005329, 8.250000000000001776, -26.00000000000001066 ) ) ;
#30178=VERTEX_POINT ( 'NONE', #51573 ) ;
#30180=VECTOR ( 'NONE', #36639, 1000.000000000000000 ) ;
#30185=ORIENTED_EDGE ( 'NONE', *, *, #67951, .F. ) ;
#30189=EDGE_LOOP ( 'NONE', ( #42771, #8988, #50645, #63099 ) ) ;
#30192=VECTOR ( 'NONE', #68207, 1000.000000000000000 ) ;
#30195=EDGE_CURVE ( 'NONE', #2261, #24784, #11724, .T. ) ;
#30198=EDGE_CURVE ( 'NONE', #61047, #58319, #14796, .T. ) ;
#30202=CARTESIAN_POINT ( 'NONE',  ( 7.450000000000004619, -1.336933437520057563E-15, -17.50000000000000000 ) ) ;
#30209=EDGE_CURVE ( 'NONE', #27966, #43050, #61324, .T. ) ;
#30230=ORIENTED_EDGE ( 'NONE', *, *, #10610, .T. ) ;
#30241=FACE_OUTER_BOUND ( 'NONE', #50196, .T. ) ;
#30245=CARTESIAN_POINT ( 'NONE',  ( -7.450000000000001954, -7.249999999999998224, -16.50000000000000000 ) ) ;
#30252=PLANE ( 'NONE',  #64599 ) ;
#30257=PLANE ( 'NONE',  #18281 ) ;
#30263=VERTEX_POINT ( 'NONE', #57920 ) ;
#30265=EDGE_CURVE ( 'NONE', #39386, #50504, #41657, .T. ) ;
#30278=VECTOR ( 'NONE', #64341, 1000.000000000000000 ) ;
#30284=AXIS2_PLACEMENT_3D ( 'NONE', #66681, #39793, #62066 ) ;
#30293=ORIENTED_EDGE ( 'NONE', *, *, #24672, .F. ) ;
#30295=DIRECTION ( 'NONE',  ( -1.000000000000000000, 1.794541526872559352E-16, 0.000000000000000000 ) ) ;
#30296=CYLINDRICAL_SURFACE ( 'NONE', #34658, 1.000000000000000000 ) ;
#30316=DIRECTION ( 'NONE',  ( -1.000000000000000000, 0.000000000000000000, 0.000000000000000000 ) ) ;
#30318=CARTESIAN_POINT ( 'NONE',  ( 7.250000000000005329, -7.249999999999998224, -22.00000000000000000 ) ) ;
#30319=VERTEX_POINT ( 'NONE', #16881 ) ;
#30320=VECTOR ( 'NONE', #36151, 1000.000000000000000 ) ;
#30332=FACE_BOUND ( 'NONE', #2557, .T. ) ;
#30335=CIRCLE ( 'NONE', #68717, 0.2000000000000005107 ) ;
#30339=CARTESIAN_POINT ( 'NONE',  ( 8.250000000000005329, -7.249999999999998224, -22.00000000000000000 ) ) ;
#30345=ORIENTED_EDGE ( 'NONE', *, *, #66979, .T. ) ;
#30349=ORIENTED_EDGE ( 'NONE', *, *, #17680, .T. ) ;
#30352=EDGE_CURVE ( 'NONE', #5855, #7022, #17213, .T. ) ;
#30362=PLANE ( 'NONE',  #49271 ) ;
#30367=CARTESIAN_POINT ( 'NONE',  ( 7.250000000000005329, 7.250000000000000888, -16.50000000000000000 ) ) ;
#30380=PLANE ( 'NONE',  #49765 ) ;
#30383=ORIENTED_EDGE ( 'NONE', *, *, #15984, .F. ) ;
#30400=ADVANCED_FACE ( 'NONE', ( #69924 ), #22190, .F. ) ;
#30412=AXIS2_PLACEMENT_3D ( 'NONE', #37542, #17011, #11351 ) ;
#30413=DIRECTION ( 'NONE',  ( -1.000000000000000000, 2.602085213965213008E-15, 0.000000000000000000 ) ) ;
#30416=ORIENTED_EDGE ( 'NONE', *, *, #51801, .T. ) ;
#30418=VECTOR ( 'NONE', #26772, 1000.000000000000000 ) ;
#30421=EDGE_LOOP ( 'NONE', ( #28310, #46331, #13475, #55720 ) ) ;
#30430=CARTESIAN_POINT ( 'NONE',  ( 7.450000000000006395, 7.250000000000000888, -11.00000000000000000 ) ) ;
#30440=CARTESIAN_POINT ( 'NONE',  ( 7.250000000000005329, -7.449999999999998401, -9.000000000000001776 ) ) ;
#30441=CIRCLE ( 'NONE', #69962, 0.2000000000000005107 ) ;
#30442=DIRECTION ( 'NONE',  ( -0.000000000000000000, 0.000000000000000000, 1.000000000000000000 ) ) ;
#30443=EDGE_CURVE ( 'NONE', #19389, #11295, #4782, .T. ) ;
#30448=CYLINDRICAL_SURFACE ( 'NONE', #66155, 0.1999999999999996503 ) ;
#30453=ORIENTED_EDGE ( 'NONE', *, *, #13336, .F. ) ;
#30459=CARTESIAN_POINT ( 'NONE',  ( 0.000000000000000000, -7.449999999999998401, -21.50000000000000000 ) ) ;
#30461=DIRECTION ( 'NONE',  ( 1.000000000000000000, 0.000000000000000000, 0.000000000000000000 ) ) ;
#30469=ORIENTED_EDGE ( 'NONE', *, *, #63697, .F. ) ;
#30483=AXIS2_PLACEMENT_3D ( 'NONE', #36134, #9984, #3624 ) ;
#30489=CARTESIAN_POINT ( 'NONE',  ( 7.250000000000005329, -7.249999999999998224, -12.50000000000000000 ) ) ;
#30503=LINE ( 'NONE', #52075, #422 ) ;
#30504=CARTESIAN_POINT ( 'NONE',  ( 0.000000000000000000, -7.449999999999998401, -13.00000000000000178 ) ) ;
#30505=AXIS2_PLACEMENT_3D ( 'NONE', #39804, #61372, #16268 ) ;
#30506=CARTESIAN_POINT ( 'NONE',  ( -7.250000000000000888, -8.249999999999998224, -22.50000000000000000 ) ) ;
#30515=CARTESIAN_POINT ( 'NONE',  ( -8.250000000000001776, -7.249999999999998224, -10.50000000000000000 ) ) ;
#30526=VECTOR ( 'NONE', #20388, 1000.000000000000000 ) ;
#30529=EDGE_CURVE ( 'NONE', #61999, #61464, #32497, .T. ) ;
#30531=DIRECTION ( 'NONE',  ( -5.981805089575196197E-17, -1.000000000000000000, 0.000000000000000000 ) ) ;
#30544=CARTESIAN_POINT ( 'NONE',  ( 7.250000000000004441, 7.450000000000001954, -24.50000000000000000 ) ) ;
#30548=VECTOR ( 'NONE', #25165, 1000.000000000000000 ) ;
#30555=DIRECTION ( 'NONE',  ( -0.000000000000000000, -0.000000000000000000, 1.000000000000000000 ) ) ;
#30568=PLANE ( 'NONE',  #48509 ) ;
#30572=LINE ( 'NONE', #53213, #34190 ) ;
#30573=AXIS2_PLACEMENT_3D ( 'NONE', #10925, #53722, #42751 ) ;
#30575=CARTESIAN_POINT ( 'NONE',  ( -7.250000000000000888, 8.250000000000001776, -26.00000000000001066 ) ) ;
#30579=FACE_OUTER_BOUND ( 'NONE', #33358, .T. ) ;
#30581=AXIS2_PLACEMENT_3D ( 'NONE', #60668, #585, #22503 ) ;
#30582=AXIS2_PLACEMENT_3D ( 'NONE', #21896, #69295, #26173 ) ;
#30591=DIRECTION ( 'NONE',  ( 0.000000000000000000, -0.000000000000000000, 1.000000000000000000 ) ) ;
#30598=EDGE_CURVE ( 'NONE', #381, #52765, #23253, .T. ) ;
#30599=ORIENTED_EDGE ( 'NONE', *, *, #8918, .T. ) ;
#30602=DIRECTION ( 'NONE',  ( 0.000000000000000000, 0.000000000000000000, -1.000000000000000000 ) ) ;
#30605=AXIS2_PLACEMENT_3D ( 'NONE', #16539, #33819, #6271 ) ;
#30606=EDGE_CURVE ( 'NONE', #1029, #16636, #27348, .T. ) ;
#30608=EDGE_LOOP ( 'NONE', ( #53032, #14850, #32886, #54356 ) ) ;
#30619=ORIENTED_EDGE ( 'NONE', *, *, #55873, .T. ) ;
#30627=EDGE_CURVE ( 'NONE', #35155, #56406, #30716, .T. ) ;
#30628=CIRCLE ( 'NONE', #44142, 0.1999999999999996503 ) ;
#30629=AXIS2_PLACEMENT_3D ( 'NONE', #38095, #47644, #43027 ) ;
#30631=DIRECTION ( 'NONE',  ( 0.000000000000000000, -1.000000000000000000, -0.000000000000000000 ) ) ;
#30634=CIRCLE ( 'NONE', #9191, 1.000000000000000000 ) ;
#30651=VECTOR ( 'NONE', #66695, 1000.000000000000000 ) ;
#30655=CARTESIAN_POINT ( 'NONE',  ( 7.250000000000005329, 7.250000000000000888, -21.00000000000000000 ) ) ;
#30662=CARTESIAN_POINT ( 'NONE',  ( 4.456444791733522252E-16, 7.450000000000002842, -20.50000000000000000 ) ) ;
#30679=CARTESIAN_POINT ( 'NONE',  ( 4.456444791733522252E-16, 7.450000000000002842, -14.50000000000000000 ) ) ;
#30683=ADVANCED_FACE ( 'NONE', ( #45154 ), #67782, .T. ) ;
#30698=FACE_OUTER_BOUND ( 'NONE', #21350, .T. ) ;
#30700=ORIENTED_EDGE ( 'NONE', *, *, #47931, .T. ) ;
#30701=DIRECTION ( 'NONE',  ( 0.000000000000000000, 0.000000000000000000, -1.000000000000000000 ) ) ;
#30709=EDGE_CURVE ( 'NONE', #15085, #59830, #2724, .T. ) ;
#30716=CIRCLE ( 'NONE', #54605, 1.000000000000000000 ) ;
#30718=DIRECTION ( 'NONE',  ( 1.000000000000000000, 0.000000000000000000, 0.000000000000000000 ) ) ;
#30742=AXIS2_PLACEMENT_3D ( 'NONE', #15564, #15891, #42760 ) ;
#30747=ORIENTED_EDGE ( 'NONE', *, *, #43218, .T. ) ;
#30751=EDGE_CURVE ( 'NONE', #14970, #47719, #51528, .T. ) ;
#30760=VERTEX_POINT ( 'NONE', #58229 ) ;
#30767=CARTESIAN_POINT ( 'NONE',  ( -7.450000000000001954, -7.249999999999998224, -24.50000000000000000 ) ) ;
#30768=DIRECTION ( 'NONE',  ( 0.000000000000000000, 0.000000000000000000, -1.000000000000000000 ) ) ;
#30769=EDGE_LOOP ( 'NONE', ( #51841, #45992, #64361, #66176 ) ) ;
#30776=DIRECTION ( 'NONE',  ( 0.000000000000000000, 0.000000000000000000, -1.000000000000000000 ) ) ;
#30781=DIRECTION ( 'NONE',  ( -1.000000000000000000, 0.000000000000000000, 0.000000000000000000 ) ) ;
#30788=LINE ( 'NONE', #56603, #44542 ) ;
#30789=ADVANCED_FACE ( 'NONE', ( #68133 ), #47272, .T. ) ;
#30790=LINE ( 'NONE', #69319, #63160 ) ;
#30791=ORIENTED_EDGE ( 'NONE', *, *, #20370, .F. ) ;
#30801=VECTOR ( 'NONE', #29668, 1000.000000000000000 ) ;
#30805=CARTESIAN_POINT ( 'NONE',  ( 7.250000000000004441, 7.450000000000001954, -9.500000000000001776 ) ) ;
#30807=ORIENTED_EDGE ( 'NONE', *, *, #13798, .T. ) ;
#30811=AXIS2_PLACEMENT_3D ( 'NONE', #69815, #59548, #64509 ) ;
#30814=DIRECTION ( 'NONE',  ( 0.000000000000000000, 0.000000000000000000, 1.000000000000000000 ) ) ;
#30816=AXIS2_PLACEMENT_3D ( 'NONE', #47261, #55012, #45064 ) ;
#30821=EDGE_CURVE ( 'NONE', #59076, #28788, #14748, .T. ) ;
#30824=CARTESIAN_POINT ( 'NONE',  ( -7.250000000000000888, 8.750000000000001776, -26.00000000000001066 ) ) ;
#30834=DIRECTION ( 'NONE',  ( 0.000000000000000000, 0.000000000000000000, 1.000000000000000000 ) ) ;
#30837=DIRECTION ( 'NONE',  ( 1.000000000000000000, -5.981805089575196197E-17, 0.000000000000000000 ) ) ;
#30841=VERTEX_POINT ( 'NONE', #4150 ) ;
#30843=CIRCLE ( 'NONE', #69254, 0.2000000000000005107 ) ;
#30853=ORIENTED_EDGE ( 'NONE', *, *, #62466, .T. ) ;
#30859=DIRECTION ( 'NONE',  ( -0.000000000000000000, -0.000000000000000000, 1.000000000000000000 ) ) ;
#30861=DIRECTION ( 'NONE',  ( 0.000000000000000000, 0.000000000000000000, 1.000000000000000000 ) ) ;
#30881=EDGE_LOOP ( 'NONE', ( #14138, #26447, #16664, #37141, #53964, #10677, #32371, #52453 ) ) ;
#30882=ORIENTED_EDGE ( 'NONE', *, *, #58403, .F. ) ;
#30883=DIRECTION ( 'NONE',  ( 0.000000000000000000, 0.000000000000000000, 1.000000000000000000 ) ) ;
#30904=LINE ( 'NONE', #53530, #60959 ) ;
#30909=CARTESIAN_POINT ( 'NONE',  ( 7.450000000000003730, -7.249999999999997335, -13.00000000000000178 ) ) ;
#30910=DIRECTION ( 'NONE',  ( -1.000000000000000000, 0.000000000000000000, 0.000000000000000000 ) ) ;
#30914=DIRECTION ( 'NONE',  ( 0.000000000000000000, 0.000000000000000000, -1.000000000000000000 ) ) ;
#30915=VERTEX_POINT ( 'NONE', #68496 ) ;
#30916=LINE ( 'NONE', #15359, #62971 ) ;
#30926=FACE_BOUND ( 'NONE', #22418, .T. ) ;
#30927=CARTESIAN_POINT ( 'NONE',  ( -8.250000000000001776, -7.249999999999998224, -13.50000000000000178 ) ) ;
#30931=EDGE_CURVE ( 'NONE', #11798, #31047, #10829, .T. ) ;
#30932=CARTESIAN_POINT ( 'NONE',  ( 7.250000000000004441, 7.450000000000001954, -17.50000000000000000 ) ) ;
#30937=CARTESIAN_POINT ( 'NONE',  ( -7.250000000000001776, -7.249999999999998224, -23.00000000000000000 ) ) ;
#30938=ORIENTED_EDGE ( 'NONE', *, *, #8159, .F. ) ;
#30946=EDGE_LOOP ( 'NONE', ( #56695, #26043, #4190, #12021 ) ) ;
#30949=ORIENTED_EDGE ( 'NONE', *, *, #28802, .T. ) ;
#30950=ORIENTED_EDGE ( 'NONE', *, *, #9775, .T. ) ;
#30958=ORIENTED_EDGE ( 'NONE', *, *, #57209, .F. ) ;
#30965=EDGE_LOOP ( 'NONE', ( #27962, #10645, #64264, #15474 ) ) ;
#30970=ORIENTED_EDGE ( 'NONE', *, *, #57002, .F. ) ;
#30972=DIRECTION ( 'NONE',  ( -1.000000000000000000, 0.000000000000000000, 0.000000000000000000 ) ) ;
#30978=AXIS2_PLACEMENT_3D ( 'NONE', #49458, #11943, #69978 ) ;
#30979=DIRECTION ( 'NONE',  ( 0.000000000000000000, 1.000000000000000000, -0.000000000000000000 ) ) ;
#30982=ORIENTED_EDGE ( 'NONE', *, *, #26617, .F. ) ;
#30983=VECTOR ( 'NONE', #2164, 1000.000000000000000 ) ;
#30986=ORIENTED_EDGE ( 'NONE', *, *, #63649, .F. ) ;
#30989=CIRCLE ( 'NONE', #33267, 1.000000000000000000 ) ;
#30999=DIRECTION ( 'NONE',  ( 0.000000000000000000, 0.000000000000000000, -1.000000000000000000 ) ) ;
#31002=CARTESIAN_POINT ( 'NONE',  ( 8.250000000000005329, 7.250000000000000888, -22.50000000000000000 ) ) ;
#31012=DIRECTION ( 'NONE',  ( 0.000000000000000000, 0.000000000000000000, 1.000000000000000000 ) ) ;
#31016=DIRECTION ( 'NONE',  ( -1.000000000000000000, 0.000000000000000000, 0.000000000000000000 ) ) ;
#31018=ADVANCED_FACE ( 'NONE', ( #39089 ), #7021, .T. ) ;
#31045=CIRCLE ( 'NONE', #27664, 0.2000000000000005107 ) ;
#31047=VERTEX_POINT ( 'NONE', #16138 ) ;
#31056=CYLINDRICAL_SURFACE ( 'NONE', #46933, 1.000000000000000000 ) ;
#31062=CIRCLE ( 'NONE', #573, 0.1999999999999987899 ) ;
#31063=EDGE_CURVE ( 'NONE', #28581, #53820, #61690, .T. ) ;
#31064=CARTESIAN_POINT ( 'NONE',  ( -8.250000000000001776, 7.250000000000000888, -26.00000000000001066 ) ) ;
#31074=EDGE_CURVE ( 'NONE', #6107, #2927, #43176, .T. ) ;
#31076=ORIENTED_EDGE ( 'NONE', *, *, #69219, .T. ) ;
#31079=EDGE_CURVE ( 'NONE', #36053, #24957, #44321, .T. ) ;
#31083=AXIS2_PLACEMENT_3D ( 'NONE', #2567, #1196, #33702 ) ;
#31086=ADVANCED_FACE ( 'NONE', ( #40477 ), #56740, .T. ) ;
#31087=CARTESIAN_POINT ( 'NONE',  ( -7.250000000000001776, -7.249999999999998224, -26.00000000000001066 ) ) ;
#31109=FACE_OUTER_BOUND ( 'NONE', #2085, .T. ) ;
#31115=CARTESIAN_POINT ( 'NONE',  ( -8.250000000000001776, -7.249999999999998224, -9.500000000000001776 ) ) ;
#31130=ORIENTED_EDGE ( 'NONE', *, *, #49001, .F. ) ;
#31131=ORIENTED_EDGE ( 'NONE', *, *, #49526, .T. ) ;
#31137=CYLINDRICAL_SURFACE ( 'NONE', #58055, 0.7499999999999997780 ) ;
#31143=VERTEX_POINT ( 'NONE', #50734 ) ;
#31144=DIRECTION ( 'NONE',  ( 0.000000000000000000, 1.000000000000000000, -0.000000000000000000 ) ) ;
#31148=CIRCLE ( 'NONE', #646, 1.000000000000000000 ) ;
#31157=EDGE_CURVE ( 'NONE', #56057, #46124, #69454, .T. ) ;
#31159=CIRCLE ( 'NONE', #67277, 1.000000000000000000 ) ;
#31161=DIRECTION ( 'NONE',  ( 0.000000000000000000, -1.000000000000000000, 0.000000000000000000 ) ) ;
#31162=ADVANCED_FACE ( 'NONE', ( #52144 ), #41538, .T. ) ;
#31163=LINE ( 'NONE', #52736, #52652 ) ;
#31165=VERTEX_POINT ( 'NONE', #30927 ) ;
#31166=CARTESIAN_POINT ( 'NONE',  ( -7.250000000000000888, 7.250000000000001776, -24.00000000000000000 ) ) ;
#31175=VECTOR ( 'NONE', #7670, 1000.000000000000000 ) ;
#31177=ORIENTED_EDGE ( 'NONE', *, *, #18873, .T. ) ;
#31198=VERTEX_POINT ( 'NONE', #15721 ) ;
#31210=ORIENTED_EDGE ( 'NONE', *, *, #49726, .T. ) ;
#31212=VERTEX_POINT ( 'NONE', #36573 ) ;
#31218=FACE_OUTER_BOUND ( 'NONE', #10149, .T. ) ;
#31226=EDGE_LOOP ( 'NONE', ( #5725, #58276, #44679, #60256 ) ) ;
#31227=CIRCLE ( 'NONE', #35737, 0.2000000000000005107 ) ;
#31232=CARTESIAN_POINT ( 'NONE',  ( 0.000000000000000000, -8.249999999999998224, -14.00000000000000000 ) ) ;
#31235=ORIENTED_EDGE ( 'NONE', *, *, #12463, .F. ) ;
#31236=VERTEX_POINT ( 'NONE', #3706 ) ;
#31253=VERTEX_POINT ( 'NONE', #14662 ) ;
#31257=DIRECTION ( 'NONE',  ( -1.000000000000000000, 0.000000000000000000, 0.000000000000000000 ) ) ;
#31259=EDGE_CURVE ( 'NONE', #68411, #38943, #58148, .T. ) ;
#31264=AXIS2_PLACEMENT_3D ( 'NONE', #17945, #12976, #60737 ) ;
#31268=DIRECTION ( 'NONE',  ( -1.000000000000000000, 0.000000000000000000, 0.000000000000000000 ) ) ;
#31278=VECTOR ( 'NONE', #57236, 1000.000000000000000 ) ;
#31287=ORIENTED_EDGE ( 'NONE', *, *, #51801, .F. ) ;
#31290=EDGE_CURVE ( 'NONE', #48836, #36185, #4877, .T. ) ;
#31319=ORIENTED_EDGE ( 'NONE', *, *, #12644, .F. ) ;
#31332=ADVANCED_FACE ( 'NONE', ( #32670 ), #49295, .F. ) ;
#31335=DIRECTION ( 'NONE',  ( 1.000000000000000000, 0.000000000000000000, 0.000000000000000000 ) ) ;
#31342=ADVANCED_FACE ( 'NONE', ( #59198 ), #21368, .F. ) ;
#31363=ORIENTED_EDGE ( 'NONE', *, *, #61152, .T. ) ;
#31365=LINE ( 'NONE', #48305, #41491 ) ;
#31369=FACE_OUTER_BOUND ( 'NONE', #56350, .T. ) ;
#31379=EDGE_CURVE ( 'NONE', #47728, #28426, #48939, .T. ) ;
#31380=PLANE ( 'NONE',  #61703 ) ;
#31382=VERTEX_POINT ( 'NONE', #65541 ) ;
#31383=CARTESIAN_POINT ( 'NONE',  ( -7.250000000000001776, -7.249999999999998224, -8.500000000000000000 ) ) ;
#31423=AXIS2_PLACEMENT_3D ( 'NONE', #3342, #9347, #52487 ) ;
#31426=EDGE_CURVE ( 'NONE', #7623, #31930, #48243, .T. ) ;
#31428=EDGE_CURVE ( 'NONE', #6920, #29479, #43966, .T. ) ;
#31430=CARTESIAN_POINT ( 'NONE',  ( -7.250000000000001776, -7.249999999999998224, -26.00000000000001066 ) ) ;
#31445=CARTESIAN_POINT ( 'NONE',  ( -8.250000000000001776, -8.249999999999998224, -26.00000000000001066 ) ) ;
#31446=EDGE_LOOP ( 'NONE', ( #40783, #34333, #59100, #9301, #50971, #36104, #48446, #58974 ) ) ;
#31454=CARTESIAN_POINT ( 'NONE',  ( 4.456444791733522252E-16, 7.450000000000002842, -15.50000000000000000 ) ) ;
#31456=CIRCLE ( 'NONE', #11095, 0.2000000000000005107 ) ;
#31457=DIRECTION ( 'NONE',  ( 0.000000000000000000, 0.000000000000000000, 1.000000000000000000 ) ) ;
#31459=FACE_OUTER_BOUND ( 'NONE', #54404, .T. ) ;
#31460=ADVANCED_FACE ( 'NONE', ( #10412 ), #53552, .F. ) ;
#31462=DIRECTION ( 'NONE',  ( 0.000000000000000000, 0.000000000000000000, 1.000000000000000000 ) ) ;
#31463=CIRCLE ( 'NONE', #54022, 1.000000000000000000 ) ;
#31466=CARTESIAN_POINT ( 'NONE',  ( 7.450000000000006395, 7.250000000000000888, -9.000000000000001776 ) ) ;
#31472=AXIS2_PLACEMENT_3D ( 'NONE', #51706, #59008, #58328 ) ;
#31473=DIRECTION ( 'NONE',  ( 0.000000000000000000, -0.000000000000000000, 1.000000000000000000 ) ) ;
#31476=CYLINDRICAL_SURFACE ( 'NONE', #51011, 0.2000000000000005107 ) ;
#31478=VERTEX_POINT ( 'NONE', #29433 ) ;
#31479=LINE ( 'NONE', #15207, #68699 ) ;
#31481=ADVANCED_FACE ( 'NONE', ( #34036 ), #67626, .T. ) ;
#31483=ORIENTED_EDGE ( 'NONE', *, *, #56984, .F. ) ;
#31496=EDGE_LOOP ( 'NONE', ( #58629, #34981, #45212, #27551, #53343, #57030, #24224, #180 ) ) ;
#31505=ADVANCED_FACE ( 'NONE', ( #7163 ), #23788, .T. ) ;
#31506=VERTEX_POINT ( 'NONE', #39694 ) ;
#31509=DIRECTION ( 'NONE',  ( -1.000000000000000000, 0.000000000000000000, 0.000000000000000000 ) ) ;
#31517=VERTEX_POINT ( 'NONE', #40400 ) ;
#31522=CARTESIAN_POINT ( 'NONE',  ( -7.250000000000000888, 8.250000000000001776, -15.50000000000000000 ) ) ;
#31526=LINE ( 'NONE', #59077, #12473 ) ;
#31527=VECTOR ( 'NONE', #55171, 1000.000000000000000 ) ;
#31529=EDGE_CURVE ( 'NONE', #2927, #62127, #60574, .T. ) ;
#31537=EDGE_LOOP ( 'NONE', ( #45712, #24573, #62234, #47667 ) ) ;
#31550=ADVANCED_FACE ( 'NONE', ( #29093 ), #50657, .T. ) ;
#31551=LINE ( 'NONE', #26239, #68194 ) ;
#31563=CARTESIAN_POINT ( 'NONE',  ( -6.749999999999998224, 7.750000000000001776, 5.000000000000000000 ) ) ;
#31570=CARTESIAN_POINT ( 'NONE',  ( 7.250000000000005329, -7.249999999999998224, -14.00000000000000000 ) ) ;
#31571=DIRECTION ( 'NONE',  ( 1.000000000000000000, -0.000000000000000000, 0.000000000000000000 ) ) ;
#31574=CARTESIAN_POINT ( 'NONE',  ( 4.456444791733522252E-16, 7.450000000000002842, -21.00000000000000000 ) ) ;
#31578=VERTEX_POINT ( 'NONE', #3978 ) ;
#31587=LINE ( 'NONE', #21668, #32019 ) ;
#31595=ORIENTED_EDGE ( 'NONE', *, *, #38828, .F. ) ;
#31600=VERTEX_POINT ( 'NONE', #46748 ) ;
#31603=AXIS2_PLACEMENT_3D ( 'NONE', #48436, #11962, #39201 ) ;
#31616=CARTESIAN_POINT ( 'NONE',  ( 7.450000000000003730, -7.249999999999997335, -22.50000000000000000 ) ) ;
#31621=DIRECTION ( 'NONE',  ( 1.000000000000000000, -0.000000000000000000, 0.000000000000000000 ) ) ;
#31631=DIRECTION ( 'NONE',  ( 0.000000000000000000, -0.000000000000000000, 1.000000000000000000 ) ) ;
#31633=CIRCLE ( 'NONE', #67746, 1.000000000000000888 ) ;
#31638=CARTESIAN_POINT ( 'NONE',  ( -7.250000000000000888, 7.250000000000001776, -26.00000000000001066 ) ) ;
#31639=DIRECTION ( 'NONE',  ( -0.000000000000000000, 0.000000000000000000, -1.000000000000000000 ) ) ;
#31647=CARTESIAN_POINT ( 'NONE',  ( 7.250000000000005329, -7.249999999999998224, -25.00000000000000000 ) ) ;
#31650=VECTOR ( 'NONE', #54609, 1000.000000000000000 ) ;
#31658=ORIENTED_EDGE ( 'NONE', *, *, #48565, .F. ) ;
#31662=ORIENTED_EDGE ( 'NONE', *, *, #32290, .F. ) ;
#31663=ORIENTED_EDGE ( 'NONE', *, *, #13662, .T. ) ;
#31675=VECTOR ( 'NONE', #49407, 1000.000000000000000 ) ;
#31686=CARTESIAN_POINT ( 'NONE',  ( -7.250000000000000888, 7.450000000000003730, -17.50000000000000000 ) ) ;
#31698=CARTESIAN_POINT ( 'NONE',  ( 7.450000000000004619, -1.336933437520057563E-15, -16.50000000000000000 ) ) ;
#31722=CARTESIAN_POINT ( 'NONE',  ( -8.250000000000001776, -7.249999999999998224, -13.00000000000000178 ) ) ;
#31725=CARTESIAN_POINT ( 'NONE',  ( 8.250000000000005329, 7.250000000000000888, -26.00000000000001066 ) ) ;
#31732=ADVANCED_FACE ( 'NONE', ( #54855 ), #65129, .T. ) ;
#31739=ORIENTED_EDGE ( 'NONE', *, *, #26347, .F. ) ;
#31757=ORIENTED_EDGE ( 'NONE', *, *, #8892, .F. ) ;
#31758=ORIENTED_EDGE ( 'NONE', *, *, #22005, .T. ) ;
#31759=AXIS2_PLACEMENT_3D ( 'NONE', #18133, #61609, #8220 ) ;
#31763=CARTESIAN_POINT ( 'NONE',  ( -7.250000000000000000, -7.449999999999998401, -20.50000000000000000 ) ) ;
#31766=VECTOR ( 'NONE', #41547, 1000.000000000000000 ) ;
#31774=VECTOR ( 'NONE', #26477, 1000.000000000000000 ) ;
#31775=DIRECTION ( 'NONE',  ( -0.000000000000000000, 0.000000000000000000, 1.000000000000000000 ) ) ;
#31783=AXIS2_PLACEMENT_3D ( 'NONE', #29913, #19649, #67043 ) ;
#31785=ORIENTED_EDGE ( 'NONE', *, *, #50874, .F. ) ;
#31788=CARTESIAN_POINT ( 'NONE',  ( -7.250000000000000888, 7.250000000000001776, -19.50000000000000000 ) ) ;
#31791=CARTESIAN_POINT ( 'NONE',  ( 0.000000000000000000, 0.000000000000000000, -5.000000000000000000 ) ) ;
#31793=ORIENTED_EDGE ( 'NONE', *, *, #30606, .T. ) ;
#31796=AXIS2_PLACEMENT_3D ( 'NONE', #42901, #16040, #37610 ) ;
#31799=ORIENTED_EDGE ( 'NONE', *, *, #69015, .F. ) ;
#31810=CYLINDRICAL_SURFACE ( 'NONE', #39068, 0.1999999999999987899 ) ;
#31816=EDGE_CURVE ( 'NONE', #6182, #48126, #15643, .T. ) ;
#31828=DIRECTION ( 'NONE',  ( 0.000000000000000000, 0.000000000000000000, 1.000000000000000000 ) ) ;
#31842=DIRECTION ( 'NONE',  ( -1.000000000000000000, 0.000000000000000000, 0.000000000000000000 ) ) ;
#31843=DIRECTION ( 'NONE',  ( 0.000000000000000000, 0.000000000000000000, 1.000000000000000000 ) ) ;
#31844=CYLINDRICAL_SURFACE ( 'NONE', #17654, 1.000000000000000888 ) ;
#31853=ORIENTED_EDGE ( 'NONE', *, *, #27644, .T. ) ;
#31854=CARTESIAN_POINT ( 'NONE',  ( -8.250000000000001776, 0.000000000000000000, -19.50000000000000000 ) ) ;
#31871=VECTOR ( 'NONE', #754, 1000.000000000000000 ) ;
#31876=DIRECTION ( 'NONE',  ( 0.000000000000000000, 0.000000000000000000, 1.000000000000000000 ) ) ;
#31880=ORIENTED_EDGE ( 'NONE', *, *, #13183, .F. ) ;
#31895=VECTOR ( 'NONE', #26832, 1000.000000000000000 ) ;
#31906=DIRECTION ( 'NONE',  ( 0.000000000000000000, 0.000000000000000000, 1.000000000000000000 ) ) ;
#31907=DIRECTION ( 'NONE',  ( 0.000000000000000000, -1.000000000000000000, 0.000000000000000000 ) ) ;
#31910=ORIENTED_EDGE ( 'NONE', *, *, #8799, .F. ) ;
#31917=DIRECTION ( 'NONE',  ( 0.000000000000000000, 0.000000000000000000, -1.000000000000000000 ) ) ;
#31928=CARTESIAN_POINT ( 'NONE',  ( 7.450000000000003730, -7.249999999999997335, -8.500000000000000000 ) ) ;
#31930=VERTEX_POINT ( 'NONE', #45879 ) ;
#31931=ORIENTED_EDGE ( 'NONE', *, *, #63074, .T. ) ;
#31934=DIRECTION ( 'NONE',  ( 0.000000000000000000, 0.000000000000000000, -1.000000000000000000 ) ) ;
#31941=AXIS2_PLACEMENT_3D ( 'NONE', #38055, #20382, #16123 ) ;
#31942=DIRECTION ( 'NONE',  ( 0.000000000000000000, 0.000000000000000000, 1.000000000000000000 ) ) ;
#31944=ORIENTED_EDGE ( 'NONE', *, *, #50070, .T. ) ;
#31953=EDGE_CURVE ( 'NONE', #21660, #11628, #38929, .T. ) ;
#31959=CARTESIAN_POINT ( 'NONE',  ( -7.450000000000001954, -7.249999999999998224, -11.50000000000000000 ) ) ;
#31960=VERTEX_POINT ( 'NONE', #17712 ) ;
#31969=CIRCLE ( 'NONE', #61300, 1.000000000000000000 ) ;
#31979=EDGE_LOOP ( 'NONE', ( #52906, #52103, #47437, #7809 ) ) ;
#31983=DIRECTION ( 'NONE',  ( 0.000000000000000000, 0.000000000000000000, 1.000000000000000000 ) ) ;
#31988=LINE ( 'NONE', #43276, #44583 ) ;
#31994=AXIS2_PLACEMENT_3D ( 'NONE', #1818, #44951, #66521 ) ;
#31997=LINE ( 'NONE', #6152, #28305 ) ;
#31999=EDGE_CURVE ( 'NONE', #16443, #24527, #68856, .T. ) ;
#32003=EDGE_LOOP ( 'NONE', ( #9915, #13531, #68092, #36261 ) ) ;
#32011=CARTESIAN_POINT ( 'NONE',  ( 7.250000000000005329, 7.250000000000000888, -26.00000000000001066 ) ) ;
#32019=VECTOR ( 'NONE', #9309, 1000.000000000000000 ) ;
#32020=ORIENTED_EDGE ( 'NONE', *, *, #1685, .F. ) ;
#32027=ORIENTED_EDGE ( 'NONE', *, *, #33651, .T. ) ;
#32029=DIRECTION ( 'NONE',  ( -1.000000000000000000, 0.000000000000000000, 0.000000000000000000 ) ) ;
#32032=ADVANCED_FACE ( 'NONE', ( #58246 ), #36319, .T. ) ;
#32038=CARTESIAN_POINT ( 'NONE',  ( -7.250000000000000888, 8.250000000000001776, -22.50000000000000000 ) ) ;
#32051=CARTESIAN_POINT ( 'NONE',  ( -9.690000000000001279, 10.50000000000000000, -5.000000000000000000 ) ) ;
#32053=CARTESIAN_POINT ( 'NONE',  ( -8.250000000000000000, 7.250000000000001776, -23.00000000000000000 ) ) ;
#32054=CARTESIAN_POINT ( 'NONE',  ( 8.250000000000005329, 7.250000000000000888, -26.00000000000001066 ) ) ;
#32055=DIRECTION ( 'NONE',  ( 0.000000000000000000, -1.000000000000000000, 0.000000000000000000 ) ) ;
#32068=EDGE_CURVE ( 'NONE', #25480, #27416, #37379, .T. ) ;
#32071=ORIENTED_EDGE ( 'NONE', *, *, #40717, .T. ) ;
#32074=ORIENTED_EDGE ( 'NONE', *, *, #56535, .T. ) ;
#32079=CARTESIAN_POINT ( 'NONE',  ( 0.000000000000000000, -8.249999999999998224, -20.50000000000000000 ) ) ;
#32103=CARTESIAN_POINT ( 'NONE',  ( 7.250000000000004441, 7.450000000000001954, -7.500000000000000000 ) ) ;
#32107=AXIS2_PLACEMENT_3D ( 'NONE', #47725, #47373, #35703 ) ;
#32120=DIRECTION ( 'NONE',  ( -1.000000000000000000, 0.000000000000000000, 0.000000000000000000 ) ) ;
#32140=CARTESIAN_POINT ( 'NONE',  ( -7.250000000000001776, -7.249999999999998224, -19.50000000000000000 ) ) ;
#32145=VERTEX_POINT ( 'NONE', #39444 ) ;
#32154=DIRECTION ( 'NONE',  ( -1.000000000000000000, 0.000000000000000000, -0.000000000000000000 ) ) ;
#32155=VERTEX_POINT ( 'NONE', #28479 ) ;
#32167=FACE_OUTER_BOUND ( 'NONE', #67471, .T. ) ;
#32170=DIRECTION ( 'NONE',  ( -1.794541526872559352E-16, -1.000000000000000000, 0.000000000000000000 ) ) ;
#32183=ORIENTED_EDGE ( 'NONE', *, *, #13898, .F. ) ;
#32187=ORIENTED_EDGE ( 'NONE', *, *, #55583, .T. ) ;
#32189=DIRECTION ( 'NONE',  ( -1.000000000000000000, 0.000000000000000000, -0.000000000000000000 ) ) ;
#32197=ADVANCED_FACE ( 'NONE', ( #6915 ), #44386, .F. ) ;
#32200=CIRCLE ( 'NONE', #8453, 0.9999999999999991118 ) ;
#32205=FACE_OUTER_BOUND ( 'NONE', #58966, .T. ) ;
#32210=VECTOR ( 'NONE', #9128, 1000.000000000000000 ) ;
#32217=PLANE ( 'NONE',  #42814 ) ;
#32220=EDGE_CURVE ( 'NONE', #20561, #58160, #65629, .T. ) ;
#32221=DIRECTION ( 'NONE',  ( 0.000000000000000000, -1.000000000000000000, 0.000000000000000000 ) ) ;
#32234=EDGE_LOOP ( 'NONE', ( #32020, #38699, #16023, #14042 ) ) ;
#32237=ORIENTED_EDGE ( 'NONE', *, *, #61731, .F. ) ;
#32245=ORIENTED_EDGE ( 'NONE', *, *, #424, .F. ) ;
#32246=ORIENTED_EDGE ( 'NONE', *, *, #26238, .F. ) ;
#32249=ORIENTED_EDGE ( 'NONE', *, *, #66981, .F. ) ;
#32253=DIRECTION ( 'NONE',  ( -1.000000000000000000, 1.794541526872559352E-16, 0.000000000000000000 ) ) ;
#32256=FACE_OUTER_BOUND ( 'NONE', #65061, .T. ) ;
#32257=VECTOR ( 'NONE', #63565, 1000.000000000000000 ) ;
#32259=EDGE_CURVE ( 'NONE', #41478, #59416, #44055, .T. ) ;
#32265=ORIENTED_EDGE ( 'NONE', *, *, #47778, .F. ) ;
#32282=EDGE_LOOP ( 'NONE', ( #60851, #2225, #35300, #45509 ) ) ;
#32290=EDGE_CURVE ( 'NONE', #43546, #42345, #61346, .T. ) ;
#32293=EDGE_LOOP ( 'NONE', ( #43105, #56641, #59971, #44298 ) ) ;
#32295=DIRECTION ( 'NONE',  ( -1.794541526872559352E-16, -1.000000000000000000, 0.000000000000000000 ) ) ;
#32308=EDGE_LOOP ( 'NONE', ( #58464, #29276, #18684, #20497 ) ) ;
#32309=CIRCLE ( 'NONE', #28889, 1.000000000000000000 ) ;
#32313=DIRECTION ( 'NONE',  ( -1.000000000000000000, 0.000000000000000000, 0.000000000000000000 ) ) ;
#32315=VECTOR ( 'NONE', #55556, 1000.000000000000000 ) ;
#32320=LINE ( 'NONE', #54938, #25732 ) ;
#32321=CARTESIAN_POINT ( 'NONE',  ( -8.250000000000001776, 7.250000000000000888, -14.50000000000000000 ) ) ;
#32327=CIRCLE ( 'NONE', #40171, 0.2000000000000005107 ) ;
#32329=DIRECTION ( 'NONE',  ( 0.000000000000000000, 0.000000000000000000, 1.000000000000000000 ) ) ;
#32332=CARTESIAN_POINT ( 'NONE',  ( 4.456444791733522252E-16, 7.450000000000002842, -15.50000000000000000 ) ) ;
#32333=LINE ( 'NONE', #69113, #52647 ) ;
#32334=EDGE_CURVE ( 'NONE', #26265, #57216, #50412, .T. ) ;
#32337=EDGE_LOOP ( 'NONE', ( #26800, #29660, #28226, #6536 ) ) ;
#32339=ORIENTED_EDGE ( 'NONE', *, *, #39635, .F. ) ;
#32354=CARTESIAN_POINT ( 'NONE',  ( 7.250000000000005329, -7.249999999999998224, -21.00000000000000000 ) ) ;
#32355=DIRECTION ( 'NONE',  ( 1.000000000000000000, 0.000000000000000000, 0.000000000000000000 ) ) ;
#32371=ORIENTED_EDGE ( 'NONE', *, *, #64056, .T. ) ;
#32372=VECTOR ( 'NONE', #46104, 1000.000000000000000 ) ;
#32373=DIRECTION ( 'NONE',  ( -1.000000000000000000, 0.000000000000000000, 0.000000000000000000 ) ) ;
#32381=LINE ( 'NONE', #53950, #44168 ) ;
#32392=CARTESIAN_POINT ( 'NONE',  ( 7.250000000000005329, -7.249999999999998224, -12.00000000000000000 ) ) ;
#32399=VECTOR ( 'NONE', #2114, 1000.000000000000000 ) ;
#32407=VECTOR ( 'NONE', #23308, 1000.000000000000000 ) ;
#32409=ORIENTED_EDGE ( 'NONE', *, *, #52574, .T. ) ;
#32420=CIRCLE ( 'NONE', #56119, 1.000000000000000000 ) ;
#32421=CARTESIAN_POINT ( 'NONE',  ( -9.690000000000001279, 9.690000000000001279, -4.250000000000000000 ) ) ;
#32426=AXIS2_PLACEMENT_3D ( 'NONE', #8812, #57248, #39917 ) ;
#32427=ORIENTED_EDGE ( 'NONE', *, *, #50077, .T. ) ;
#32448=DIRECTION ( 'NONE',  ( 1.000000000000000000, 0.000000000000000000, 0.000000000000000000 ) ) ;
#32459=DIRECTION ( 'NONE',  ( 0.000000000000000000, 0.000000000000000000, 1.000000000000000000 ) ) ;
#32464=FACE_OUTER_BOUND ( 'NONE', #4884, .T. ) ;
#32480=CARTESIAN_POINT ( 'NONE',  ( -8.250000000000001776, -7.249999999999998224, -20.50000000000000000 ) ) ;
#32484=CARTESIAN_POINT ( 'NONE',  ( 7.250000000000005329, -8.249999999999998224, -8.000000000000000000 ) ) ;
#32486=CYLINDRICAL_SURFACE ( 'NONE', #53233, 0.8100000000000017186 ) ;
#32490=CARTESIAN_POINT ( 'NONE',  ( 7.450000000000006395, 7.250000000000000888, -7.000000000000000000 ) ) ;
#32496=CARTESIAN_POINT ( 'NONE',  ( 8.250000000000005329, 7.250000000000000888, -22.00000000000000000 ) ) ;
#32497=LINE ( 'NONE', #32830, #33131 ) ;
#32498=VERTEX_POINT ( 'NONE', #25284 ) ;
#32501=VERTEX_POINT ( 'NONE', #47895 ) ;
#32502=DIRECTION ( 'NONE',  ( 0.000000000000000000, 0.000000000000000000, 1.000000000000000000 ) ) ;
#32509=AXIS2_PLACEMENT_3D ( 'NONE', #57762, #4392, #68733 ) ;
#32512=VERTEX_POINT ( 'NONE', #9729 ) ;
#32514=EDGE_LOOP ( 'NONE', ( #26569, #59805, #21166, #58551, #41133, #45229, #12637, #31931 ) ) ;
#32554=ORIENTED_EDGE ( 'NONE', *, *, #12025, .T. ) ;
#32558=CARTESIAN_POINT ( 'NONE',  ( 7.250000000000005329, -7.249999999999998224, -19.00000000000000000 ) ) ;
#32566=EDGE_LOOP ( 'NONE', ( #2243, #6372, #47570, #11043 ) ) ;
#32572=CARTESIAN_POINT ( 'NONE',  ( -7.450000000000001954, 7.250000000000000000, -10.50000000000000000 ) ) ;
#32574=CARTESIAN_POINT ( 'NONE',  ( -6.749999999999998224, 7.750000000000001776, 0.000000000000000000 ) ) ;
#32575=EDGE_CURVE ( 'NONE', #21671, #11939, #44312, .T. ) ;
#32576=CARTESIAN_POINT ( 'NONE',  ( -7.250000000000000888, 7.250000000000001776, -26.00000000000001066 ) ) ;
#32583=EDGE_LOOP ( 'NONE', ( #56662, #52911, #22211, #49619 ) ) ;
#32585=DIRECTION ( 'NONE',  ( -1.000000000000000000, 0.000000000000000000, 0.000000000000000000 ) ) ;
#32586=VERTEX_POINT ( 'NONE', #11114 ) ;
#32594=ORIENTED_EDGE ( 'NONE', *, *, #6732, .T. ) ;
#32601=DIRECTION ( 'NONE',  ( 0.000000000000000000, 0.000000000000000000, 1.000000000000000000 ) ) ;
#32602=ORIENTED_EDGE ( 'NONE', *, *, #64840, .F. ) ;
#32605=EDGE_CURVE ( 'NONE', #26123, #7845, #59212, .T. ) ;
#32614=VECTOR ( 'NONE', #52479, 1000.000000000000000 ) ;
#32617=CARTESIAN_POINT ( 'NONE',  ( -7.250000000000000888, 7.250000000000001776, -11.00000000000000000 ) ) ;
#32624=FACE_OUTER_BOUND ( 'NONE', #52705, .T. ) ;
#32633=ORIENTED_EDGE ( 'NONE', *, *, #31063, .F. ) ;
#32649=AXIS2_PLACEMENT_3D ( 'NONE', #68080, #9746, #57468 ) ;
#32650=LINE ( 'NONE', #65187, #55334 ) ;
#32668=VERTEX_POINT ( 'NONE', #38680 ) ;
#32670=FACE_OUTER_BOUND ( 'NONE', #22445, .T. ) ;
#32677=DIRECTION ( 'NONE',  ( 8.951101527228104953E-17, 1.000000000000000000, 0.000000000000000000 ) ) ;
#32685=VERTEX_POINT ( 'NONE', #39706 ) ;
#32692=ADVANCED_FACE ( 'NONE', ( #67639 ), #55631, .T. ) ;
#32699=DIRECTION ( 'NONE',  ( 0.000000000000000000, 0.000000000000000000, -1.000000000000000000 ) ) ;
#32710=DIRECTION ( 'NONE',  ( 0.000000000000000000, 0.000000000000000000, 1.000000000000000000 ) ) ;
#32714=DIRECTION ( 'NONE',  ( -1.000000000000000000, 2.602085213965213008E-15, 0.000000000000000000 ) ) ;
#32716=DIRECTION ( 'NONE',  ( 0.000000000000000000, -1.000000000000000000, 0.000000000000000000 ) ) ;
#32722=DIRECTION ( 'NONE',  ( 0.000000000000000000, 0.000000000000000000, -1.000000000000000000 ) ) ;
#32723=CARTESIAN_POINT ( 'NONE',  ( -7.250000000000000888, 7.450000000000003730, -15.50000000000000000 ) ) ;
#32737=LINE ( 'NONE', #49368, #63900 ) ;
#32738=VECTOR ( 'NONE', #45508, 1000.000000000000000 ) ;
#32740=DIRECTION ( 'NONE',  ( -1.794541526872559352E-16, -1.000000000000000000, 0.000000000000000000 ) ) ;
#32745=DIRECTION ( 'NONE',  ( 1.000000000000000000, 0.000000000000000000, 0.000000000000000000 ) ) ;
#32746=ORIENTED_EDGE ( 'NONE', *, *, #52435, .T. ) ;
#32747=LINE ( 'NONE', #21795, #59252 ) ;
#32750=LINE ( 'NONE', #54331, #43540 ) ;
#32754=CARTESIAN_POINT ( 'NONE',  ( 7.250000000000004441, 7.450000000000001954, -25.00000000000000000 ) ) ;
#32790=DIRECTION ( 'NONE',  ( -1.000000000000000000, 1.334402673828312846E-16, 0.000000000000000000 ) ) ;
#32791=VECTOR ( 'NONE', #55366, 1000.000000000000000 ) ;
#32794=EDGE_LOOP ( 'NONE', ( #38955, #46292, #224, #20509 ) ) ;
#32796=CIRCLE ( 'NONE', #23760, 0.2000000000000005107 ) ;
#32797=EDGE_CURVE ( 'NONE', #7192, #54414, #56327, .T. ) ;
#32798=DIRECTION ( 'NONE',  ( 0.000000000000000000, -0.000000000000000000, 1.000000000000000000 ) ) ;
#32799=DIRECTION ( 'NONE',  ( -1.000000000000000000, 0.000000000000000000, 0.000000000000000000 ) ) ;
#32801=ORIENTED_EDGE ( 'NONE', *, *, #35697, .T. ) ;
#32805=CARTESIAN_POINT ( 'NONE',  ( -7.450000000000001954, -7.249999999999998224, -10.00000000000000000 ) ) ;
#32818=VERTEX_POINT ( 'NONE', #69383 ) ;
#32819=CARTESIAN_POINT ( 'NONE',  ( 7.450000000000006395, 7.250000000000000888, -24.50000000000000000 ) ) ;
#32830=CARTESIAN_POINT ( 'NONE',  ( -8.250000000000001776, 7.250000000000000888, -26.00000000000001066 ) ) ;
#32836=EDGE_CURVE ( 'NONE', #44658, #1276, #42516, .T. ) ;
#32845=ORIENTED_EDGE ( 'NONE', *, *, #55267, .T. ) ;
#32847=CARTESIAN_POINT ( 'NONE',  ( -8.250000000000001776, 7.250000000000000888, -21.50000000000000000 ) ) ;
#32862=VECTOR ( 'NONE', #50664, 1000.000000000000000 ) ;
#32867=DIRECTION ( 'NONE',  ( 0.000000000000000000, 0.000000000000000000, 1.000000000000000000 ) ) ;
#32878=DIRECTION ( 'NONE',  ( -0.000000000000000000, -0.000000000000000000, 1.000000000000000000 ) ) ;
#32880=EDGE_CURVE ( 'NONE', #42553, #56334, #12851, .T. ) ;
#32883=EDGE_LOOP ( 'NONE', ( #65461, #45293, #12655, #58945 ) ) ;
#32886=ORIENTED_EDGE ( 'NONE', *, *, #46551, .T. ) ;
#32894=DIRECTION ( 'NONE',  ( 0.000000000000000000, -1.000000000000000000, 0.000000000000000000 ) ) ;
#32899=ORIENTED_EDGE ( 'NONE', *, *, #68999, .F. ) ;
#32901=DIRECTION ( 'NONE',  ( 0.000000000000000000, -1.000000000000000000, 0.000000000000000000 ) ) ;
#32906=VECTOR ( 'NONE', #24844, 1000.000000000000000 ) ;
#32909=EDGE_CURVE ( 'NONE', #41339, #2734, #30503, .T. ) ;
#32912=DIRECTION ( 'NONE',  ( 0.000000000000000000, 0.000000000000000000, 1.000000000000000000 ) ) ;
#32915=EDGE_LOOP ( 'NONE', ( #13787, #61000, #9042, #37593 ) ) ;
#32918=CARTESIAN_POINT ( 'NONE',  ( 8.250000000000005329, 0.000000000000000000, -8.000000000000000000 ) ) ;
#32920=VERTEX_POINT ( 'NONE', #47812 ) ;
#32921=LINE ( 'NONE', #33941, #15091 ) ;
#32924=CARTESIAN_POINT ( 'NONE',  ( 7.250000000000005329, -7.249999999999998224, -15.00000000000000000 ) ) ;
#32927=DIRECTION ( 'NONE',  ( 1.000000000000000000, -0.000000000000000000, 0.000000000000000000 ) ) ;
#32928=EDGE_LOOP ( 'NONE', ( #32427, #63684, #64871, #68549 ) ) ;
#32935=DIRECTION ( 'NONE',  ( 0.000000000000000000, 0.000000000000000000, 1.000000000000000000 ) ) ;
#32938=VERTEX_POINT ( 'NONE', #36152 ) ;
#32942=ORIENTED_EDGE ( 'NONE', *, *, #32259, .F. ) ;
#32945=EDGE_CURVE ( 'NONE', #36321, #15671, #4968, .T. ) ;
#32952=DIRECTION ( 'NONE',  ( -0.000000000000000000, 0.000000000000000000, 1.000000000000000000 ) ) ;
#32953=CARTESIAN_POINT ( 'NONE',  ( 0.000000000000000000, 8.250000000000001776, -18.50000000000000000 ) ) ;
#32954=VERTEX_POINT ( 'NONE', #10682 ) ;
#32959=VECTOR ( 'NONE', #55200, 1000.000000000000000 ) ;
#32960=AXIS2_PLACEMENT_3D ( 'NONE', #14500, #9195, #24400 ) ;
#32961=CARTESIAN_POINT ( 'NONE',  ( 7.450000000000003730, -7.249999999999997335, -25.50000000000000355 ) ) ;
#32962=CARTESIAN_POINT ( 'NONE',  ( 7.250000000000005329, 7.250000000000000888, -9.500000000000001776 ) ) ;
#32964=DIRECTION ( 'NONE',  ( -1.000000000000000000, 0.000000000000000000, 0.000000000000000000 ) ) ;
#32967=ORIENTED_EDGE ( 'NONE', *, *, #45199, .T. ) ;
#32978=VECTOR ( 'NONE', #58113, 1000.000000000000000 ) ;
#32983=DIRECTION ( 'NONE',  ( -1.000000000000000000, 0.000000000000000000, 0.000000000000000000 ) ) ;
#32994=ORIENTED_EDGE ( 'NONE', *, *, #29288, .F. ) ;
#32995=CARTESIAN_POINT ( 'NONE',  ( 7.250000000000005329, -7.249999999999998224, -10.50000000000000000 ) ) ;
#32996=DIRECTION ( 'NONE',  ( -1.000000000000000000, 0.000000000000000000, 0.000000000000000000 ) ) ;
#33000=ADVANCED_FACE ( 'NONE', ( #16338 ), #88, .F. ) ;
#33009=LINE ( 'NONE', #12804, #53681 ) ;
#33014=DIRECTION ( 'NONE',  ( 1.000000000000000000, -5.981805089575194965E-17, 0.000000000000000000 ) ) ;
#33016=VECTOR ( 'NONE', #6643, 1000.000000000000000 ) ;
#33019=ORIENTED_EDGE ( 'NONE', *, *, #35866, .F. ) ;
#33027=CARTESIAN_POINT ( 'NONE',  ( -7.250000000000000000, -7.449999999999998401, -9.500000000000001776 ) ) ;
#33029=DIRECTION ( 'NONE',  ( -1.000000000000000000, 0.000000000000000000, 0.000000000000000000 ) ) ;
#33032=EDGE_CURVE ( 'NONE', #67047, #33736, #5034, .T. ) ;
#33045=ORIENTED_EDGE ( 'NONE', *, *, #4491, .T. ) ;
#33048=EDGE_LOOP ( 'NONE', ( #53562, #48384, #29037, #44353, #11306, #7693, #3311, #63736 ) ) ;
#33064=DIRECTION ( 'NONE',  ( 0.000000000000000000, 0.000000000000000000, -1.000000000000000000 ) ) ;
#33067=ORIENTED_EDGE ( 'NONE', *, *, #8643, .T. ) ;
#33068=DIRECTION ( 'NONE',  ( -0.000000000000000000, -0.000000000000000000, 1.000000000000000000 ) ) ;
#33073=ADVANCED_FACE ( 'NONE', ( #15997 ), #43897, .F. ) ;
#33090=CARTESIAN_POINT ( 'NONE',  ( 7.250000000000005329, -7.449999999999998401, -24.00000000000000000 ) ) ;
#33105=VERTEX_POINT ( 'NONE', #39284 ) ;
#33108=FACE_OUTER_BOUND ( 'NONE', #13687, .T. ) ;
#33109=ORIENTED_EDGE ( 'NONE', *, *, #53761, .F. ) ;
#33113=CIRCLE ( 'NONE', #35371, 0.1999999999999987899 ) ;
#33120=ORIENTED_EDGE ( 'NONE', *, *, #38584, .F. ) ;
#33121=EDGE_LOOP ( 'NONE', ( #29583, #51039, #61203, #51105 ) ) ;
#33123=DIRECTION ( 'NONE',  ( 0.000000000000000000, 0.000000000000000000, -1.000000000000000000 ) ) ;
#33125=ORIENTED_EDGE ( 'NONE', *, *, #51835, .T. ) ;
#33131=VECTOR ( 'NONE', #27526, 1000.000000000000000 ) ;
#33134=LINE ( 'NONE', #65993, #57082 ) ;
#33138=EDGE_CURVE ( 'NONE', #30841, #3133, #45270, .T. ) ;
#33139=ORIENTED_EDGE ( 'NONE', *, *, #38536, .F. ) ;
#33143=AXIS2_PLACEMENT_3D ( 'NONE', #43871, #33610, #17006 ) ;
#33145=CARTESIAN_POINT ( 'NONE',  ( 7.250000000000005329, 7.250000000000000888, -26.00000000000001066 ) ) ;
#33163=EDGE_CURVE ( 'NONE', #17506, #2261, #17724, .T. ) ;
#33164=ORIENTED_EDGE ( 'NONE', *, *, #2282, .F. ) ;
#33171=CYLINDRICAL_SURFACE ( 'NONE', #3281, 0.2000000000000005107 ) ;
#33178=ORIENTED_EDGE ( 'NONE', *, *, #48561, .T. ) ;
#33182=CARTESIAN_POINT ( 'NONE',  ( -7.450000000000001954, -7.249999999999998224, -24.00000000000000000 ) ) ;
#33192=CARTESIAN_POINT ( 'NONE',  ( -7.250000000000000000, -7.449999999999998401, -14.50000000000000000 ) ) ;
#33197=FACE_OUTER_BOUND ( 'NONE', #8285, .T. ) ;
#33202=FACE_OUTER_BOUND ( 'NONE', #67415, .T. ) ;
#33208=EDGE_CURVE ( 'NONE', #10507, #44658, #37770, .T. ) ;
#33210=DIRECTION ( 'NONE',  ( 1.000000000000000000, 0.000000000000000000, 0.000000000000000000 ) ) ;
#33213=CIRCLE ( 'NONE', #2705, 0.2000000000000005107 ) ;
#33214=VECTOR ( 'NONE', #27772, 1000.000000000000000 ) ;
#33218=VERTEX_POINT ( 'NONE', #50594 ) ;
#33220=EDGE_CURVE ( 'NONE', #42042, #22300, #35472, .T. ) ;
#33228=LINE ( 'NONE', #56525, #35770 ) ;
#33252=DIRECTION ( 'NONE',  ( -0.000000000000000000, -0.000000000000000000, -1.000000000000000000 ) ) ;
#33260=ORIENTED_EDGE ( 'NONE', *, *, #48709, .F. ) ;
#33263=AXIS2_PLACEMENT_3D ( 'NONE', #31383, #35592, #8740 ) ;
#33267=AXIS2_PLACEMENT_3D ( 'NONE', #33286, #11700, #26949 ) ;
#33271=CARTESIAN_POINT ( 'NONE',  ( -8.250000000000001776, -7.249999999999998224, -26.00000000000001066 ) ) ;
#33277=FACE_OUTER_BOUND ( 'NONE', #15494, .T. ) ;
#33282=ORIENTED_EDGE ( 'NONE', *, *, #28704, .T. ) ;
#33284=DIRECTION ( 'NONE',  ( -1.000000000000000000, 0.000000000000000000, 0.000000000000000000 ) ) ;
#33285=DIRECTION ( 'NONE',  ( 0.000000000000000000, 0.000000000000000000, 1.000000000000000000 ) ) ;
#33286=CARTESIAN_POINT ( 'NONE',  ( 7.250000000000005329, -7.249999999999998224, -24.50000000000000000 ) ) ;
#33293=EDGE_CURVE ( 'NONE', #5400, #52304, #68615, .T. ) ;
#33295=CARTESIAN_POINT ( 'NONE',  ( 8.250000000000005329, -8.249999999999998224, -26.00000000000001066 ) ) ;
#33298=DIRECTION ( 'NONE',  ( 0.000000000000000000, 0.000000000000000000, 1.000000000000000000 ) ) ;
#33301=ORIENTED_EDGE ( 'NONE', *, *, #24406, .T. ) ;
#33305=AXIS2_PLACEMENT_3D ( 'NONE', #2044, #66733, #2731 ) ;
#33311=CIRCLE ( 'NONE', #1693, 2.500000000000000000 ) ;
#33314=CARTESIAN_POINT ( 'NONE',  ( -7.250000000000001776, -7.249999999999998224, -18.00000000000000000 ) ) ;
#33321=ADVANCED_FACE ( 'NONE', ( #51649 ), #31137, .T. ) ;
#33323=DIRECTION ( 'NONE',  ( 1.000000000000000000, -5.981805089575196197E-17, 0.000000000000000000 ) ) ;
#33326=VERTEX_POINT ( 'NONE', #19798 ) ;
#33330=DIRECTION ( 'NONE',  ( -1.000000000000000000, 0.000000000000000000, 0.000000000000000000 ) ) ;
#33342=ADVANCED_FACE ( 'NONE', ( #69303 ), #42777, .F. ) ;
#33353=DIRECTION ( 'NONE',  ( 1.000000000000000000, 0.000000000000000000, 0.000000000000000000 ) ) ;
#33355=CIRCLE ( 'NONE', #64961, 0.1999999999999987899 ) ;
#33358=EDGE_LOOP ( 'NONE', ( #16955, #61153, #39137, #38711, #45268, #2286, #35116, #23997 ) ) ;
#33363=CARTESIAN_POINT ( 'NONE',  ( 8.250000000000005329, -8.249999999999998224, -26.00000000000001066 ) ) ;
#33366=ORIENTED_EDGE ( 'NONE', *, *, #39943, .T. ) ;
#33370=CARTESIAN_POINT ( 'NONE',  ( 7.250000000000005329, -8.249999999999998224, -26.00000000000001066 ) ) ;
#33378=DIRECTION ( 'NONE',  ( 1.334402673828313093E-16, 1.000000000000000000, 0.000000000000000000 ) ) ;
#33379=ORIENTED_EDGE ( 'NONE', *, *, #44876, .F. ) ;
#33380=VECTOR ( 'NONE', #43513, 1000.000000000000000 ) ;
#33399=DIRECTION ( 'NONE',  ( 1.000000000000000000, -5.981805089575196197E-17, 0.000000000000000000 ) ) ;
#33404=ORIENTED_EDGE ( 'NONE', *, *, #61052, .F. ) ;
#33433=ADVANCED_FACE ( 'NONE', ( #1046 ), #3, .F. ) ;
#33435=DIRECTION ( 'NONE',  ( -1.000000000000000000, 0.000000000000000000, 0.000000000000000000 ) ) ;
#33440=DIRECTION ( 'NONE',  ( -1.000000000000000000, 0.000000000000000000, 0.000000000000000000 ) ) ;
#33448=DIRECTION ( 'NONE',  ( 0.000000000000000000, -0.000000000000000000, 1.000000000000000000 ) ) ;
#33453=AXIS2_PLACEMENT_3D ( 'NONE', #49873, #1428, #24033 ) ;
#33458=EDGE_LOOP ( 'NONE', ( #12358, #50442, #1677, #58133 ) ) ;
#33459=VECTOR ( 'NONE', #58831, 1000.000000000000000 ) ;
#33460=AXIS2_PLACEMENT_3D ( 'NONE', #39625, #23380, #17039 ) ;
#33466=ORIENTED_EDGE ( 'NONE', *, *, #47052, .T. ) ;
#33476=ORIENTED_EDGE ( 'NONE', *, *, #3767, .F. ) ;
#33480=EDGE_LOOP ( 'NONE', ( #53083, #65396, #42937, #36175 ) ) ;
#33484=ORIENTED_EDGE ( 'NONE', *, *, #14237, .F. ) ;
#33485=DIRECTION ( 'NONE',  ( -1.000000000000000000, 0.000000000000000000, 0.000000000000000000 ) ) ;
#33500=CARTESIAN_POINT ( 'NONE',  ( 10.50000000000000178, 9.690000000000001279, -5.000000000000000000 ) ) ;
#33504=CARTESIAN_POINT ( 'NONE',  ( -7.250000000000000888, -8.249999999999998224, -10.50000000000000000 ) ) ;
#33517=PRODUCT_DEFINITION_SHAPE ( 'NONE', 'NONE',  #20553 ) ;
#33530=CARTESIAN_POINT ( 'NONE',  ( 4.456444791733522252E-16, 7.450000000000002842, -11.50000000000000000 ) ) ;
#33535=ORIENTED_EDGE ( 'NONE', *, *, #62305, .T. ) ;
#33540=ORIENTED_EDGE ( 'NONE', *, *, #11507, .F. ) ;
#33544=EDGE_LOOP ( 'NONE', ( #28318, #45207, #37670, #64888 ) ) ;
#33547=DIRECTION ( 'NONE',  ( 1.000000000000000000, 0.000000000000000000, 0.000000000000000000 ) ) ;
#33552=ORIENTED_EDGE ( 'NONE', *, *, #14439, .F. ) ;
#33556=LINE ( 'NONE', #19033, #60359 ) ;
#33558=ORIENTED_EDGE ( 'NONE', *, *, #35423, .T. ) ;
#33560=EDGE_CURVE ( 'NONE', #67897, #58614, #21966, .T. ) ;
#33563=EDGE_CURVE ( 'NONE', #53573, #9491, #39876, .T. ) ;
#33568=AXIS2_PLACEMENT_3D ( 'NONE', #34966, #2109, #62538 ) ;
#33569=PLANE ( 'NONE',  #38224 ) ;
#33570=ORIENTED_EDGE ( 'NONE', *, *, #50259, .F. ) ;
#33571=ORIENTED_EDGE ( 'NONE', *, *, #30195, .T. ) ;
#33572=DIRECTION ( 'NONE',  ( 0.000000000000000000, 1.000000000000000000, 0.000000000000000000 ) ) ;
#33579=CARTESIAN_POINT ( 'NONE',  ( 7.250000000000005329, -7.249999999999998224, -26.00000000000001066 ) ) ;
#33583=DIRECTION ( 'NONE',  ( 0.000000000000000000, -0.000000000000000000, 1.000000000000000000 ) ) ;
#33584=ORIENTED_EDGE ( 'NONE', *, *, #42887, .F. ) ;
#33593=AXIS2_PLACEMENT_3D ( 'NONE', #41245, #14392, #52209 ) ;
#33596=LINE ( 'NONE', #27951, #31527 ) ;
#33603=ORIENTED_EDGE ( 'NONE', *, *, #51451, .F. ) ;
#33605=LINE ( 'NONE', #50566, #67941 ) ;
#33607=VECTOR ( 'NONE', #69911, 1000.000000000000000 ) ;
#33610=DIRECTION ( 'NONE',  ( -0.000000000000000000, -0.000000000000000000, 1.000000000000000000 ) ) ;
#33612=ORIENTED_EDGE ( 'NONE', *, *, #2409, .F. ) ;
#33613=FACE_OUTER_BOUND ( 'NONE', #22234, .T. ) ;
#33622=VERTEX_POINT ( 'NONE', #67112 ) ;
#33633=CARTESIAN_POINT ( 'NONE',  ( 9.690000000000001279, -8.750000000000000000, -5.000000000000000000 ) ) ;
#33637=DIRECTION ( 'NONE',  ( -0.000000000000000000, -0.000000000000000000, 1.000000000000000000 ) ) ;
#33641=DIRECTION ( 'NONE',  ( 1.000000000000000000, 0.000000000000000000, 0.000000000000000000 ) ) ;
#33642=CARTESIAN_POINT ( 'NONE',  ( -7.250000000000000888, 7.450000000000003730, -23.50000000000000000 ) ) ;
#33651=EDGE_CURVE ( 'NONE', #25947, #31047, #20426, .T. ) ;
#33665=AXIS2_PLACEMENT_3D ( 'NONE', #17858, #22815, #44362 ) ;
#33673=DIRECTION ( 'NONE',  ( 0.000000000000000000, -1.000000000000000000, -0.000000000000000000 ) ) ;
#33674=EDGE_CURVE ( 'NONE', #8412, #6993, #9474, .T. ) ;
#33687=ORIENTED_EDGE ( 'NONE', *, *, #51159, .T. ) ;
#33690=EDGE_CURVE ( 'NONE', #20305, #6090, #68163, .T. ) ;
#33692=VERTEX_POINT ( 'NONE', #35265 ) ;
#33696=EDGE_LOOP ( 'NONE', ( #18283, #4034, #44672, #44267 ) ) ;
#33698=AXIS2_PLACEMENT_3D ( 'NONE', #66291, #6880, #13234 ) ;
#33702=DIRECTION ( 'NONE',  ( -1.000000000000000000, 0.000000000000000000, 0.000000000000000000 ) ) ;
#33708=ORIENTED_EDGE ( 'NONE', *, *, #28704, .F. ) ;
#33710=VERTEX_POINT ( 'NONE', #30339 ) ;
#33713=CARTESIAN_POINT ( 'NONE',  ( 7.250000000000004441, 7.450000000000001954, -14.50000000000000000 ) ) ;
#33716=DIRECTION ( 'NONE',  ( 0.000000000000000000, 0.000000000000000000, -1.000000000000000000 ) ) ;
#33722=ORIENTED_EDGE ( 'NONE', *, *, #14439, .T. ) ;
#33735=ORIENTED_EDGE ( 'NONE', *, *, #47380, .T. ) ;
#33736=VERTEX_POINT ( 'NONE', #1542 ) ;
#33739=CARTESIAN_POINT ( 'NONE',  ( 4.456444791733522252E-16, 7.450000000000002842, -16.00000000000000000 ) ) ;
#33741=VERTEX_POINT ( 'NONE', #63923 ) ;
#33747=VECTOR ( 'NONE', #63352, 1000.000000000000000 ) ;
#33751=CARTESIAN_POINT ( 'NONE',  ( -7.250000000000000000, -7.449999999999998401, -24.00000000000000000 ) ) ;
#33758=CARTESIAN_POINT ( 'NONE',  ( -8.250000000000001776, -7.249999999999998224, -26.00000000000001066 ) ) ;
#33775=CARTESIAN_POINT ( 'NONE',  ( -8.750000000000001776, -7.249999999999998224, -26.00000000000001066 ) ) ;
#33781=LINE ( 'NONE', #60664, #29861 ) ;
#33794=DIRECTION ( 'NONE',  ( 0.000000000000000000, 0.000000000000000000, 1.000000000000000000 ) ) ;
#33795=VERTEX_POINT ( 'NONE', #12156 ) ;
#33800=DIRECTION ( 'NONE',  ( 0.000000000000000000, 0.000000000000000000, 1.000000000000000000 ) ) ;
#33801=DIRECTION ( 'NONE',  ( -0.000000000000000000, -0.000000000000000000, -1.000000000000000000 ) ) ;
#33804=DIRECTION ( 'NONE',  ( -0.000000000000000000, -0.000000000000000000, 1.000000000000000000 ) ) ;
#33809=DIRECTION ( 'NONE',  ( -1.000000000000000000, 0.000000000000000000, -0.000000000000000000 ) ) ;
#33816=LINE ( 'NONE', #45117, #36060 ) ;
#33819=DIRECTION ( 'NONE',  ( -0.000000000000000000, -0.000000000000000000, 1.000000000000000000 ) ) ;
#33843=EDGE_CURVE ( 'NONE', #69756, #9056, #64920, .T. ) ;
#33845=CARTESIAN_POINT ( 'NONE',  ( 7.450000000000003730, -7.249999999999997335, -25.00000000000000000 ) ) ;
#33851=EDGE_CURVE ( 'NONE', #66073, #24192, #1648, .T. ) ;
#33852=DIRECTION ( 'NONE',  ( 1.000000000000000000, 0.000000000000000000, 0.000000000000000000 ) ) ;
#33870=LINE ( 'NONE', #38506, #1733 ) ;
#33875=VERTEX_POINT ( 'NONE', #43656 ) ;
#33879=EDGE_LOOP ( 'NONE', ( #38468, #11578, #34495, #40600 ) ) ;
#33889=CARTESIAN_POINT ( 'NONE',  ( 10.50000000000000178, 9.690000000000001279, 0.000000000000000000 ) ) ;
#33899=CARTESIAN_POINT ( 'NONE',  ( 4.456444791733522252E-16, 7.450000000000002842, -18.50000000000000000 ) ) ;
#33900=AXIS2_PLACEMENT_3D ( 'NONE', #64134, #48544, #31257 ) ;
#33909=LINE ( 'NONE', #54121, #56783 ) ;
#33935=EDGE_CURVE ( 'NONE', #60008, #21483, #34763, .T. ) ;
#33941=CARTESIAN_POINT ( 'NONE',  ( 8.250000000000005329, 0.000000000000000000, -15.00000000000000000 ) ) ;
#33947=DIRECTION ( 'NONE',  ( 0.000000000000000000, 0.000000000000000000, 1.000000000000000000 ) ) ;
#33949=CARTESIAN_POINT ( 'NONE',  ( 0.000000000000000000, 0.000000000000000000, -30.00000000000001066 ) ) ;
#33956=VERTEX_POINT ( 'NONE', #40055 ) ;
#33961=DIRECTION ( 'NONE',  ( 0.000000000000000000, 1.000000000000000000, 0.000000000000000000 ) ) ;
#33962=ORIENTED_EDGE ( 'NONE', *, *, #36009, .T. ) ;
#33971=LINE ( 'NONE', #51291, #26473 ) ;
#33973=VERTEX_POINT ( 'NONE', #66595 ) ;
#33988=DIRECTION ( 'NONE',  ( 0.000000000000000000, 0.000000000000000000, 1.000000000000000000 ) ) ;
#33992=VECTOR ( 'NONE', #22517, 1000.000000000000000 ) ;
#34000=CARTESIAN_POINT ( 'NONE',  ( -7.250000000000001776, -7.249999999999998224, -18.50000000000000000 ) ) ;
#34008=CARTESIAN_POINT ( 'NONE',  ( 7.250000000000004441, 7.450000000000001954, -10.50000000000000000 ) ) ;
#34012=VERTEX_POINT ( 'NONE', #51380 ) ;
#34015=VERTEX_POINT ( 'NONE', #67303 ) ;
#34016=CARTESIAN_POINT ( 'NONE',  ( 7.250000000000005329, -7.249999999999998224, -23.50000000000000000 ) ) ;
#34030=DIRECTION ( 'NONE',  ( -1.000000000000000000, 0.000000000000000000, -0.000000000000000000 ) ) ;
#34036=FACE_OUTER_BOUND ( 'NONE', #47463, .T. ) ;
#34040=VECTOR ( 'NONE', #44566, 1000.000000000000000 ) ;
#34044=CARTESIAN_POINT ( 'NONE',  ( -7.250000000000000000, -7.449999999999998401, -18.50000000000000000 ) ) ;
#34052=CYLINDRICAL_SURFACE ( 'NONE', #10443, 0.2000000000000005107 ) ;
#34060=LINE ( 'NONE', #29469, #24758 ) ;
#34062=ORIENTED_EDGE ( 'NONE', *, *, #40140, .T. ) ;
#34063=ORIENTED_EDGE ( 'NONE', *, *, #52654, .T. ) ;
#34074=VECTOR ( 'NONE', #67944, 1000.000000000000000 ) ;
#34077=CARTESIAN_POINT ( 'NONE',  ( 7.450000000000004619, -1.336933437520057563E-15, -13.50000000000000178 ) ) ;
#34080=DIRECTION ( 'NONE',  ( 0.000000000000000000, 0.000000000000000000, 1.000000000000000000 ) ) ;
#34092=ORIENTED_EDGE ( 'NONE', *, *, #4511, .T. ) ;
#34106=CARTESIAN_POINT ( 'NONE',  ( 7.250000000000004441, 7.450000000000001954, -12.00000000000000000 ) ) ;
#34130=CARTESIAN_POINT ( 'NONE',  ( -7.450000000000001954, 7.250000000000000000, -9.500000000000001776 ) ) ;
#34135=EDGE_LOOP ( 'NONE', ( #22309, #57223, #68500, #15382 ) ) ;
#34137=DIRECTION ( 'NONE',  ( 0.000000000000000000, 0.000000000000000000, 1.000000000000000000 ) ) ;
#34140=LINE ( 'NONE', #44405, #43761 ) ;
#34145=DIRECTION ( 'NONE',  ( 1.000000000000000000, 0.000000000000000000, 0.000000000000000000 ) ) ;
#34146=VECTOR ( 'NONE', #52583, 1000.000000000000000 ) ;
#34148=ORIENTED_EDGE ( 'NONE', *, *, #29278, .F. ) ;
#34150=EDGE_CURVE ( 'NONE', #6078, #2415, #47824, .T. ) ;
#34151=EDGE_LOOP ( 'NONE', ( #41617, #41653, #2505, #65992, #67631, #6439 ) ) ;
#34158=DIRECTION ( 'NONE',  ( -0.000000000000000000, -1.000000000000000000, -0.000000000000000000 ) ) ;
#34165=DIRECTION ( 'NONE',  ( -0.000000000000000000, -0.000000000000000000, 1.000000000000000000 ) ) ;
#34169=CYLINDRICAL_SURFACE ( 'NONE', #60647, 1.000000000000000888 ) ;
#34174=CARTESIAN_POINT ( 'NONE',  ( -7.450000000000001954, -7.249999999999998224, -7.500000000000000000 ) ) ;
#34178=CARTESIAN_POINT ( 'NONE',  ( -7.250000000000000888, 7.250000000000001776, -22.00000000000000000 ) ) ;
#34183=CARTESIAN_POINT ( 'NONE',  ( 7.250000000000004441, 7.450000000000001954, -16.50000000000000000 ) ) ;
#34184=CARTESIAN_POINT ( 'NONE',  ( 7.250000000000004441, 7.450000000000001954, -7.000000000000000000 ) ) ;
#34186=AXIS2_PLACEMENT_3D ( 'NONE', #63038, #61977, #62675 ) ;
#34188=ADVANCED_FACE ( 'NONE', ( #37931 ), #11385, .T. ) ;
#34190=VECTOR ( 'NONE', #31983, 1000.000000000000000 ) ;
#34193=DIRECTION ( 'NONE',  ( 0.000000000000000000, 1.000000000000000000, 0.000000000000000000 ) ) ;
#34196=DIRECTION ( 'NONE',  ( -1.000000000000000000, 0.000000000000000000, 0.000000000000000000 ) ) ;
#34201=ORIENTED_EDGE ( 'NONE', *, *, #28912, .T. ) ;
#34202=CARTESIAN_POINT ( 'NONE',  ( 7.250000000000005329, -7.249999999999998224, -19.00000000000000000 ) ) ;
#34209=PLANE ( 'NONE',  #9706 ) ;
#34213=LINE ( 'NONE', #17963, #52039 ) ;
#34216=EDGE_CURVE ( 'NONE', #19389, #15739, #48531, .T. ) ;
#34218=CARTESIAN_POINT ( 'NONE',  ( -7.250000000000000888, -8.249999999999998224, -26.00000000000001066 ) ) ;
#34220=ORIENTED_EDGE ( 'NONE', *, *, #19906, .F. ) ;
#34222=EDGE_CURVE ( 'NONE', #64750, #15828, #10694, .T. ) ;
#34245=AXIS2_PLACEMENT_3D ( 'NONE', #7951, #39774, #45432 ) ;
#34251=DIRECTION ( 'NONE',  ( -1.000000000000000000, 0.000000000000000000, -0.000000000000000000 ) ) ;
#34253=VECTOR ( 'NONE', #28803, 1000.000000000000000 ) ;
#34259=VERTEX_POINT ( 'NONE', #22363 ) ;
#34276=LINE ( 'NONE', #12708, #66810 ) ;
#34286=CARTESIAN_POINT ( 'NONE',  ( 7.250000000000005329, 7.250000000000000888, -11.50000000000000000 ) ) ;
#34298=FACE_OUTER_BOUND ( 'NONE', #64557, .T. ) ;
#34302=ORIENTED_EDGE ( 'NONE', *, *, #50214, .T. ) ;
#34308=DIRECTION ( 'NONE',  ( -0.000000000000000000, -0.000000000000000000, -1.000000000000000000 ) ) ;
#34309=VECTOR ( 'NONE', #26608, 1000.000000000000000 ) ;
#34314=PLANE ( 'NONE',  #60092 ) ;
#34317=VERTEX_POINT ( 'NONE', #5283 ) ;
#34320=DIRECTION ( 'NONE',  ( 1.000000000000000000, 0.000000000000000000, 0.000000000000000000 ) ) ;
#34321=EDGE_CURVE ( 'NONE', #64534, #67047, #27718, .T. ) ;
#34333=ORIENTED_EDGE ( 'NONE', *, *, #57053, .F. ) ;
#34345=CYLINDRICAL_SURFACE ( 'NONE', #10917, 0.1999999999999996503 ) ;
#34349=DIRECTION ( 'NONE',  ( -0.000000000000000000, 0.000000000000000000, -1.000000000000000000 ) ) ;
#34354=FACE_OUTER_BOUND ( 'NONE', #52132, .T. ) ;
#34359=CARTESIAN_POINT ( 'NONE',  ( -7.450000000000001954, -7.249999999999998224, -21.00000000000000000 ) ) ;
#34364=DIRECTION ( 'NONE',  ( -1.794541526872559352E-16, -1.000000000000000000, 0.000000000000000000 ) ) ;
#34365=FACE_OUTER_BOUND ( 'NONE', #14520, .T. ) ;
#34388=DIRECTION ( 'NONE',  ( 0.000000000000000000, -1.000000000000000000, -0.000000000000000000 ) ) ;
#34395=AXIS2_PLACEMENT_3D ( 'NONE', #4526, #69578, #6528 ) ;
#34400=EDGE_CURVE ( 'NONE', #34593, #14316, #36759, .T. ) ;
#34402=VECTOR ( 'NONE', #32295, 1000.000000000000000 ) ;
#34406=VERTEX_POINT ( 'NONE', #25803 ) ;
#34410=EDGE_CURVE ( 'NONE', #52575, #43309, #10227, .T. ) ;
#34415=LINE ( 'NONE', #1560, #1169 ) ;
#34425=ORIENTED_EDGE ( 'NONE', *, *, #1433, .T. ) ;
#34430=ORIENTED_EDGE ( 'NONE', *, *, #54332, .F. ) ;
#34440=AXIS2_PLACEMENT_3D ( 'NONE', #34926, #19715, #3478 ) ;
#34443=CARTESIAN_POINT ( 'NONE',  ( -7.250000000000000888, 7.450000000000003730, -19.50000000000000000 ) ) ;
#34454=DIRECTION ( 'NONE',  ( -0.000000000000000000, -0.000000000000000000, 1.000000000000000000 ) ) ;
#34457=CARTESIAN_POINT ( 'NONE',  ( 0.000000000000000000, 8.750000000000001776, -30.00000000000001066 ) ) ;
#34459=ORIENTED_EDGE ( 'NONE', *, *, #23038, .T. ) ;
#34464=EDGE_CURVE ( 'NONE', #51045, #25235, #9851, .T. ) ;
#34467=FACE_OUTER_BOUND ( 'NONE', #25155, .T. ) ;
#34468=ORIENTED_EDGE ( 'NONE', *, *, #60590, .F. ) ;
#34471=EDGE_CURVE ( 'NONE', #28850, #40508, #41659, .T. ) ;
#34476=EDGE_CURVE ( 'NONE', #26023, #15117, #20099, .T. ) ;
#34484=ORIENTED_EDGE ( 'NONE', *, *, #49525, .T. ) ;
#34487=EDGE_CURVE ( 'NONE', #50215, #12761, #6315, .T. ) ;
#34491=CIRCLE ( 'NONE', #44688, 1.000000000000000000 ) ;
#34495=ORIENTED_EDGE ( 'NONE', *, *, #48959, .F. ) ;
#34496=PLANE ( 'NONE',  #9806 ) ;
#34497=EDGE_CURVE ( 'NONE', #2339, #64155, #53726, .T. ) ;
#34500=AXIS2_PLACEMENT_3D ( 'NONE', #27818, #16162, #11875 ) ;
#34502=EDGE_LOOP ( 'NONE', ( #48884, #46393, #16639, #56840 ) ) ;
#34504=ORIENTED_EDGE ( 'NONE', *, *, #23179, .T. ) ;
#34505=VECTOR ( 'NONE', #18249, 1000.000000000000000 ) ;
#34507=ADVANCED_FACE ( 'NONE', ( #32464 ), #31056, .T. ) ;
#34511=DIRECTION ( 'NONE',  ( -0.000000000000000000, -0.000000000000000000, -1.000000000000000000 ) ) ;
#34518=FACE_OUTER_BOUND ( 'NONE', #35462, .T. ) ;
#34521=DIRECTION ( 'NONE',  ( 1.000000000000000000, 0.000000000000000000, 0.000000000000000000 ) ) ;
#34523=ORIENTED_EDGE ( 'NONE', *, *, #66667, .T. ) ;
#34524=ORIENTED_EDGE ( 'NONE', *, *, #18513, .F. ) ;
#34526=CARTESIAN_POINT ( 'NONE',  ( 7.450000000000003730, -7.249999999999997335, -21.50000000000000000 ) ) ;
#34527=AXIS2_PLACEMENT_3D ( 'NONE', #59974, #48336, #54686 ) ;
#34542=EDGE_CURVE ( 'NONE', #24957, #56406, #53337, .T. ) ;
#34543=VECTOR ( 'NONE', #4813, 1000.000000000000000 ) ;
#34546=DIRECTION ( 'NONE',  ( -1.000000000000000000, 0.000000000000000000, 0.000000000000000000 ) ) ;
#34555=DIRECTION ( 'NONE',  ( -1.000000000000000000, 0.000000000000000000, 0.000000000000000000 ) ) ;
#34557=EDGE_CURVE ( 'NONE', #35196, #24794, #55969, .T. ) ;
#34560=DIRECTION ( 'NONE',  ( 1.000000000000000000, -0.000000000000000000, 0.000000000000000000 ) ) ;
#34571=VERTEX_POINT ( 'NONE', #27487 ) ;
#34573=DIRECTION ( 'NONE',  ( -1.000000000000000000, 0.000000000000000000, 0.000000000000000000 ) ) ;
#34575=ORIENTED_EDGE ( 'NONE', *, *, #44102, .F. ) ;
#34578=LINE ( 'NONE', #40590, #44908 ) ;
#34583=DIRECTION ( 'NONE',  ( 0.000000000000000000, 0.000000000000000000, 1.000000000000000000 ) ) ;
#34585=EDGE_LOOP ( 'NONE', ( #40774, #24054, #51912, #45745, #13281, #37952, #28180, #18212 ) ) ;
#34588=ORIENTED_EDGE ( 'NONE', *, *, #5347, .F. ) ;
#34592=EDGE_CURVE ( 'NONE', #22518, #68972, #981, .T. ) ;
#34593=VERTEX_POINT ( 'NONE', #12245 ) ;
#34594=EDGE_CURVE ( 'NONE', #29779, #47728, #48063, .T. ) ;
#34609=CARTESIAN_POINT ( 'NONE',  ( -7.450000000000001954, 0.000000000000000000, -13.50000000000000178 ) ) ;
#34612=AXIS2_PLACEMENT_3D ( 'NONE', #47081, #20901, #64060 ) ;
#34620=CYLINDRICAL_SURFACE ( 'NONE', #38645, 1.000000000000000000 ) ;
#34634=AXIS2_PLACEMENT_3D ( 'NONE', #27161, #63956, #42025 ) ;
#34639=EDGE_CURVE ( 'NONE', #43197, #46964, #11899, .T. ) ;
#34645=CYLINDRICAL_SURFACE ( 'NONE', #64858, 0.2000000000000005107 ) ;
#34650=AXIS2_PLACEMENT_3D ( 'NONE', #67502, #37681, #10452 ) ;
#34652=EDGE_CURVE ( 'NONE', #31047, #64750, #33134, .T. ) ;
#34658=AXIS2_PLACEMENT_3D ( 'NONE', #51862, #66109, #40185 ) ;
#34662=DIRECTION ( 'NONE',  ( -1.000000000000000000, 0.000000000000000000, 0.000000000000000000 ) ) ;
#34671=DIRECTION ( 'NONE',  ( 0.000000000000000000, 0.000000000000000000, -1.000000000000000000 ) ) ;
#34677=ORIENTED_EDGE ( 'NONE', *, *, #24203, .F. ) ;
#34680=EDGE_CURVE ( 'NONE', #21563, #40613, #67281, .T. ) ;
#34681=CARTESIAN_POINT ( 'NONE',  ( -8.250000000000001776, 0.000000000000000000, -16.00000000000000000 ) ) ;
#34683=EDGE_LOOP ( 'NONE', ( #64478, #42002, #20547, #1897 ) ) ;
#34685=CYLINDRICAL_SURFACE ( 'NONE', #62525, 0.1999999999999996503 ) ;
#34689=ADVANCED_FACE ( 'NONE', ( #61741 ), #19648, .F. ) ;
#34703=ORIENTED_EDGE ( 'NONE', *, *, #15466, .F. ) ;
#34709=LINE ( 'NONE', #7486, #4162 ) ;
#34713=VERTEX_POINT ( 'NONE', #29910 ) ;
#34716=VERTEX_POINT ( 'NONE', #45829 ) ;
#34717=CIRCLE ( 'NONE', #60711, 1.000000000000000000 ) ;
#34719=LINE ( 'NONE', #7839, #519 ) ;
#34724=ORIENTED_EDGE ( 'NONE', *, *, #13180, .T. ) ;
#34731=FACE_OUTER_BOUND ( 'NONE', #52861, .T. ) ;
#34739=DIRECTION ( 'NONE',  ( 1.000000000000000000, 0.000000000000000000, 0.000000000000000000 ) ) ;
#34745=ORIENTED_EDGE ( 'NONE', *, *, #22465, .T. ) ;
#34755=CIRCLE ( 'NONE', #40369, 0.9999999999999991118 ) ;
#34759=ORIENTED_EDGE ( 'NONE', *, *, #60777, .T. ) ;
#34761=ORIENTED_EDGE ( 'NONE', *, *, #66650, .T. ) ;
#34763=LINE ( 'NONE', #2944, #43456 ) ;
#34771=EDGE_CURVE ( 'NONE', #6534, #14806, #23912, .T. ) ;
#34772=EDGE_CURVE ( 'NONE', #57470, #47184, #66693, .T. ) ;
#34776=ORIENTED_EDGE ( 'NONE', *, *, #25034, .F. ) ;
#34783=ORIENTED_EDGE ( 'NONE', *, *, #32945, .F. ) ;
#34784=CARTESIAN_POINT ( 'NONE',  ( -10.50000000000000178, -9.690000000000001279, -4.250000000000000000 ) ) ;
#34786=LINE ( 'NONE', #18519, #7596 ) ;
#34794=ORIENTED_EDGE ( 'NONE', *, *, #6861, .F. ) ;
#34795=CARTESIAN_POINT ( 'NONE',  ( 0.000000000000000000, -7.449999999999998401, -23.00000000000000000 ) ) ;
#34799=ORIENTED_EDGE ( 'NONE', *, *, #37390, .T. ) ;
#34801=VECTOR ( 'NONE', #54456, 1000.000000000000000 ) ;
#34803=VERTEX_POINT ( 'NONE', #8701 ) ;
#34816=DIRECTION ( 'NONE',  ( -1.000000000000000000, 0.000000000000000000, 0.000000000000000000 ) ) ;
#34818=DIRECTION ( 'NONE',  ( 0.000000000000000000, 0.000000000000000000, 1.000000000000000000 ) ) ;
#34819=CARTESIAN_POINT ( 'NONE',  ( -7.250000000000000888, 8.250000000000001776, -10.00000000000000000 ) ) ;
#34820=EDGE_CURVE ( 'NONE', #12839, #19794, #12937, .T. ) ;
#34837=ORIENTED_EDGE ( 'NONE', *, *, #34680, .T. ) ;
#34842=CARTESIAN_POINT ( 'NONE',  ( 0.000000000000000000, -7.449999999999998401, -7.500000000000000000 ) ) ;
#34846=DIRECTION ( 'NONE',  ( 0.000000000000000000, 0.000000000000000000, -1.000000000000000000 ) ) ;
#34855=VERTEX_POINT ( 'NONE', #15417 ) ;
#34871=ORIENTED_EDGE ( 'NONE', *, *, #9065, .F. ) ;
#34872=CARTESIAN_POINT ( 'NONE',  ( -7.250000000000001776, -7.249999999999998224, -26.00000000000001066 ) ) ;
#34874=LINE ( 'NONE', #62099, #54507 ) ;
#34879=ORIENTED_EDGE ( 'NONE', *, *, #50619, .F. ) ;
#34893=VERTEX_POINT ( 'NONE', #41580 ) ;
#34902=EDGE_CURVE ( 'NONE', #17827, #14810, #69849, .T. ) ;
#34903=AXIS2_PLACEMENT_3D ( 'NONE', #38735, #59269, #33440 ) ;
#34907=VERTEX_POINT ( 'NONE', #4464 ) ;
#34914=VERTEX_POINT ( 'NONE', #52913 ) ;
#34926=CARTESIAN_POINT ( 'NONE',  ( 7.250000000000005329, 7.250000000000000888, -19.50000000000000000 ) ) ;
#34940=ORIENTED_EDGE ( 'NONE', *, *, #51424, .F. ) ;
#34949=CARTESIAN_POINT ( 'NONE',  ( 7.250000000000005329, 8.250000000000001776, -26.00000000000001066 ) ) ;
#34951=CARTESIAN_POINT ( 'NONE',  ( -7.250000000000000000, -7.449999999999998401, -10.00000000000000000 ) ) ;
#34954=DIRECTION ( 'NONE',  ( -1.000000000000000000, 0.000000000000000000, 0.000000000000000000 ) ) ;
#34956=EDGE_CURVE ( 'NONE', #18717, #25138, #64211, .T. ) ;
#34957=DIRECTION ( 'NONE',  ( 0.000000000000000000, 0.000000000000000000, 1.000000000000000000 ) ) ;
#34959=CARTESIAN_POINT ( 'NONE',  ( -7.250000000000000000, -7.449999999999998401, -17.50000000000000000 ) ) ;
#34962=CARTESIAN_POINT ( 'NONE',  ( 2.500000000000000000, 3.061616997868383141E-16, -30.00000000000001066 ) ) ;
#34965=EDGE_CURVE ( 'NONE', #27411, #69858, #50367, .T. ) ;
#34966=CARTESIAN_POINT ( 'NONE',  ( -7.250000000000001776, -7.249999999999998224, -11.50000000000000000 ) ) ;
#34980=CARTESIAN_POINT ( 'NONE',  ( -7.450000000000001954, -7.249999999999998224, -18.00000000000000000 ) ) ;
#34981=ORIENTED_EDGE ( 'NONE', *, *, #20893, .F. ) ;
#34985=ORIENTED_EDGE ( 'NONE', *, *, #37549, .F. ) ;
#34987=CARTESIAN_POINT ( 'NONE',  ( 7.250000000000005329, 7.250000000000000888, -25.50000000000000355 ) ) ;
#34988=EDGE_CURVE ( 'NONE', #68972, #11705, #4110, .T. ) ;
#34993=DIRECTION ( 'NONE',  ( -1.000000000000000000, 0.000000000000000000, 0.000000000000000000 ) ) ;
#34999=AXIS2_PLACEMENT_3D ( 'NONE', #67439, #46547, #41246 ) ;
#35001=CIRCLE ( 'NONE', #46318, 0.1999999999999996503 ) ;
#35007=CARTESIAN_POINT ( 'NONE',  ( -7.250000000000000000, -7.449999999999998401, -13.50000000000000178 ) ) ;
#35010=CARTESIAN_POINT ( 'NONE',  ( -10.50000000000000000, -9.690000000000001279, -4.250000000000000000 ) ) ;
#35017=AXIS2_PLACEMENT_3D ( 'NONE', #15750, #9395, #42262 ) ;
#35019=CARTESIAN_POINT ( 'NONE',  ( -7.250000000000000888, 7.250000000000001776, -21.00000000000000000 ) ) ;
#35021=CARTESIAN_POINT ( 'NONE',  ( 7.250000000000005329, -7.249999999999998224, -11.50000000000000000 ) ) ;
#35033=EDGE_CURVE ( 'NONE', #8834, #59416, #45824, .T. ) ;
#35036=ORIENTED_EDGE ( 'NONE', *, *, #65663, .T. ) ;
#35040=AXIS2_PLACEMENT_3D ( 'NONE', #9948, #10982, #36819 ) ;
#35045=VERTEX_POINT ( 'NONE', #55329 ) ;
#35046=ORIENTED_EDGE ( 'NONE', *, *, #12729, .F. ) ;
#35048=PLANE ( 'NONE',  #9565 ) ;
#35052=DIRECTION ( 'NONE',  ( -1.000000000000000000, 0.000000000000000000, 0.000000000000000000 ) ) ;
#35069=ORIENTED_EDGE ( 'NONE', *, *, #19568, .T. ) ;
#35070=CARTESIAN_POINT ( 'NONE',  ( -9.689999999999999503, -10.50000000000000178, -5.000000000000000000 ) ) ;
#35077=ORIENTED_EDGE ( 'NONE', *, *, #42792, .F. ) ;
#35084=CARTESIAN_POINT ( 'NONE',  ( 7.250000000000005329, -8.249999999999998224, -26.00000000000001066 ) ) ;
#35085=CARTESIAN_POINT ( 'NONE',  ( -7.250000000000000888, 7.250000000000001776, -23.00000000000000000 ) ) ;
#35095=CARTESIAN_POINT ( 'NONE',  ( -7.250000000000000888, 8.250000000000001776, -15.00000000000000000 ) ) ;
#35099=ORIENTED_EDGE ( 'NONE', *, *, #50077, .F. ) ;
#35107=VECTOR ( 'NONE', #67634, 1000.000000000000000 ) ;
#35116=ORIENTED_EDGE ( 'NONE', *, *, #52389, .T. ) ;
#35122=EDGE_LOOP ( 'NONE', ( #67322, #25963, #33584, #52743 ) ) ;
#35132=LINE ( 'NONE', #46449, #49370 ) ;
#35136=CARTESIAN_POINT ( 'NONE',  ( 4.456444791733522252E-16, 7.450000000000002842, -23.00000000000000000 ) ) ;
#35138=DIRECTION ( 'NONE',  ( 0.000000000000000000, 0.000000000000000000, -1.000000000000000000 ) ) ;
#35145=EDGE_LOOP ( 'NONE', ( #7219, #35046, #61826, #57328 ) ) ;
#35147=LINE ( 'NONE', #63359, #338 ) ;
#35149=VECTOR ( 'NONE', #25372, 1000.000000000000000 ) ;
#35152=CARTESIAN_POINT ( 'NONE',  ( -8.250000000000001776, 7.250000000000000888, -16.50000000000000000 ) ) ;
#35153=DIRECTION ( 'NONE',  ( 0.000000000000000000, 0.000000000000000000, 1.000000000000000000 ) ) ;
#35155=VERTEX_POINT ( 'NONE', #39733 ) ;
#35165=CARTESIAN_POINT ( 'NONE',  ( -7.250000000000000000, -7.449999999999998401, -12.50000000000000000 ) ) ;
#35168=EDGE_CURVE ( 'NONE', #11455, #37156, #50353, .T. ) ;
#35170=DIRECTION ( 'NONE',  ( 0.000000000000000000, 0.000000000000000000, 1.000000000000000000 ) ) ;
#35171=VERTEX_POINT ( 'NONE', #17837 ) ;
#35174=DIRECTION ( 'NONE',  ( 1.000000000000000000, -0.000000000000000000, 0.000000000000000000 ) ) ;
#35179=ORIENTED_EDGE ( 'NONE', *, *, #2100, .T. ) ;
#35184=VECTOR ( 'NONE', #55848, 1000.000000000000000 ) ;
#35188=ORIENTED_EDGE ( 'NONE', *, *, #48734, .F. ) ;
#35196=VERTEX_POINT ( 'NONE', #34784 ) ;
#35200=ORIENTED_EDGE ( 'NONE', *, *, #14701, .T. ) ;
#35204=ADVANCED_FACE ( 'NONE', ( #18171 ), #2269, .F. ) ;
#35205=EDGE_CURVE ( 'NONE', #33956, #24794, #52667, .T. ) ;
#35221=CARTESIAN_POINT ( 'NONE',  ( -10.50000000000000178, 9.690000000000001279, 0.000000000000000000 ) ) ;
#35222=AXIS2_PLACEMENT_3D ( 'NONE', #61780, #45504, #24654 ) ;
#35226=DIRECTION ( 'NONE',  ( 0.000000000000000000, 0.000000000000000000, -1.000000000000000000 ) ) ;
#35232=AXIS2_PLACEMENT_3D ( 'NONE', #45993, #49900, #24070 ) ;
#35236=DIRECTION ( 'NONE',  ( -1.000000000000000000, 0.000000000000000000, 0.000000000000000000 ) ) ;
#35238=FACE_OUTER_BOUND ( 'NONE', #12722, .T. ) ;
#35242=CARTESIAN_POINT ( 'NONE',  ( 7.250000000000004441, 7.450000000000001954, -13.00000000000000178 ) ) ;
#35254=EDGE_CURVE ( 'NONE', #56770, #14563, #8256, .T. ) ;
#35265=CARTESIAN_POINT ( 'NONE',  ( 7.250000000000005329, 8.250000000000001776, -11.50000000000000000 ) ) ;
#35266=CIRCLE ( 'NONE', #46588, 1.000000000000003553 ) ;
#35273=VERTEX_POINT ( 'NONE', #21931 ) ;
#35287=FACE_OUTER_BOUND ( 'NONE', #57751, .T. ) ;
#35289=EDGE_LOOP ( 'NONE', ( #56355, #9098, #14226, #53515, #9006, #7441, #17276, #44903 ) ) ;
#35292=EDGE_CURVE ( 'NONE', #58614, #37156, #58728, .T. ) ;
#35294=ORIENTED_EDGE ( 'NONE', *, *, #62355, .T. ) ;
#35300=ORIENTED_EDGE ( 'NONE', *, *, #25751, .T. ) ;
#35301=CARTESIAN_POINT ( 'NONE',  ( -8.250000000000001776, -7.249999999999998224, -25.50000000000000355 ) ) ;
#35306=DIRECTION ( 'NONE',  ( 1.000000000000000000, 0.000000000000000000, 0.000000000000000000 ) ) ;
#35310=DIRECTION ( 'NONE',  ( 1.000000000000000000, -0.000000000000000000, 0.000000000000000000 ) ) ;
#35313=DIRECTION ( 'NONE',  ( -1.000000000000000000, 2.602085213965213008E-15, 0.000000000000000000 ) ) ;
#35333=CARTESIAN_POINT ( 'NONE',  ( 7.450000000000006395, 7.250000000000000888, -8.000000000000000000 ) ) ;
#35335=CARTESIAN_POINT ( 'NONE',  ( 7.450000000000003730, -7.249999999999997335, -18.50000000000000000 ) ) ;
#35339=DIRECTION ( 'NONE',  ( 0.000000000000000000, 0.000000000000000000, -1.000000000000000000 ) ) ;
#35340=DIRECTION ( 'NONE',  ( -5.981805089575196197E-17, -1.000000000000000000, 0.000000000000000000 ) ) ;
#35346=ORIENTED_EDGE ( 'NONE', *, *, #60434, .F. ) ;
#35359=LINE ( 'NONE', #57650, #7452 ) ;
#35371=AXIS2_PLACEMENT_3D ( 'NONE', #48312, #219, #10472 ) ;
#35389=CARTESIAN_POINT ( 'NONE',  ( -9.690000000000001279, 9.690000000000001279, 0.000000000000000000 ) ) ;
#35397=LINE ( 'NONE', #25519, #39682 ) ;
#35400=LINE ( 'NONE', #61219, #59464 ) ;
#35403=ORIENTED_EDGE ( 'NONE', *, *, #9346, .F. ) ;
#35405=CARTESIAN_POINT ( 'NONE',  ( 7.250000000000005329, 8.250000000000001776, -18.50000000000000000 ) ) ;
#35412=CARTESIAN_POINT ( 'NONE',  ( -7.250000000000000888, 7.250000000000001776, -12.50000000000000000 ) ) ;
#35423=EDGE_CURVE ( 'NONE', #21985, #59322, #67386, .T. ) ;
#35439=DIRECTION ( 'NONE',  ( 1.000000000000000000, 0.000000000000000000, 0.000000000000000000 ) ) ;
#35442=CARTESIAN_POINT ( 'NONE',  ( -7.250000000000000888, 7.250000000000001776, -23.00000000000000000 ) ) ;
#35445=DIRECTION ( 'NONE',  ( 1.000000000000000000, -5.981805089575194965E-17, 0.000000000000000000 ) ) ;
#35446=CIRCLE ( 'NONE', #494, 1.000000000000000000 ) ;
#35451=EDGE_LOOP ( 'NONE', ( #20679, #36125, #1820, #68858 ) ) ;
#35462=EDGE_LOOP ( 'NONE', ( #49386, #69154, #55959, #38159 ) ) ;
#35471=DIRECTION ( 'NONE',  ( -1.000000000000000000, 0.000000000000000000, 0.000000000000000000 ) ) ;
#35472=CIRCLE ( 'NONE', #11754, 0.9999999999999991118 ) ;
#35473=ADVANCED_FACE ( 'NONE', ( #1736, #66445 ), #13030, .F. ) ;
#35478=EDGE_CURVE ( 'NONE', #23929, #34893, #7382, .T. ) ;
#35485=VERTEX_POINT ( 'NONE', #727 ) ;
#35492=CARTESIAN_POINT ( 'NONE',  ( 8.250000000000005329, -7.249999999999998224, -8.000000000000000000 ) ) ;
#35504=ORIENTED_EDGE ( 'NONE', *, *, #47440, .F. ) ;
#35508=ADVANCED_FACE ( 'NONE', ( #7733 ), #2986, .T. ) ;
#35530=AXIS2_PLACEMENT_3D ( 'NONE', #23054, #44608, #12774 ) ;
#35534=CYLINDRICAL_SURFACE ( 'NONE', #16052, 0.1999999999999987899 ) ;
#35555=EDGE_CURVE ( 'NONE', #3823, #67986, #51935, .T. ) ;
#35565=AXIS2_PLACEMENT_3D ( 'NONE', #68605, #63295, #30413 ) ;
#35575=ORIENTED_EDGE ( 'NONE', *, *, #55268, .F. ) ;
#35578=LINE ( 'NONE', #68115, #29009 ) ;
#35583=CARTESIAN_POINT ( 'NONE',  ( 7.450000000000006395, 7.250000000000000888, -14.50000000000000000 ) ) ;
#35585=LINE ( 'NONE', #15088, #8469 ) ;
#35588=CARTESIAN_POINT ( 'NONE',  ( -7.250000000000000888, 7.450000000000003730, -10.50000000000000000 ) ) ;
#35592=DIRECTION ( 'NONE',  ( 0.000000000000000000, 0.000000000000000000, -1.000000000000000000 ) ) ;
#35598=LINE ( 'NONE', #46562, #16346 ) ;
#35614=ORIENTED_EDGE ( 'NONE', *, *, #67993, .T. ) ;
#35618=EDGE_LOOP ( 'NONE', ( #66126, #60868, #20844, #55491 ) ) ;
#35620=VERTEX_POINT ( 'NONE', #14460 ) ;
#35627=VERTEX_POINT ( 'NONE', #9149 ) ;
#35631=FACE_OUTER_BOUND ( 'NONE', #60334, .T. ) ;
#35632=ORIENTED_EDGE ( 'NONE', *, *, #41819, .T. ) ;
#35641=DIRECTION ( 'NONE',  ( -0.000000000000000000, -0.000000000000000000, -1.000000000000000000 ) ) ;
#35665=CIRCLE ( 'NONE', #57129, 0.2000000000000005107 ) ;
#35666=VECTOR ( 'NONE', #36795, 1000.000000000000000 ) ;
#35687=PLANE ( 'NONE',  #54805 ) ;
#35692=VERTEX_POINT ( 'NONE', #43065 ) ;
#35696=EDGE_LOOP ( 'NONE', ( #63369, #40453, #22025, #1097, #26517, #10405, #25576, #20135 ) ) ;
#35697=EDGE_CURVE ( 'NONE', #11798, #6104, #21164, .T. ) ;
#35700=CARTESIAN_POINT ( 'NONE',  ( 7.250000000000005329, 8.250000000000001776, -26.00000000000001066 ) ) ;
#35703=DIRECTION ( 'NONE',  ( 1.000000000000000000, 0.000000000000000000, 0.000000000000000000 ) ) ;
#35705=AXIS2_PLACEMENT_3D ( 'NONE', #66620, #56016, #50702 ) ;
#35719=LINE ( 'NONE', #57293, #14384 ) ;
#35721=DIRECTION ( 'NONE',  ( -1.000000000000000000, 0.000000000000000000, 0.000000000000000000 ) ) ;
#35724=AXIS2_PLACEMENT_3D ( 'NONE', #11080, #48913, #27685 ) ;
#35726=VECTOR ( 'NONE', #15134, 1000.000000000000000 ) ;
#35731=ORIENTED_EDGE ( 'NONE', *, *, #26139, .T. ) ;
#35732=ORIENTED_EDGE ( 'NONE', *, *, #49581, .F. ) ;
#35733=ORIENTED_EDGE ( 'NONE', *, *, #66074, .T. ) ;
#35737=AXIS2_PLACEMENT_3D ( 'NONE', #2272, #56017, #44691 ) ;
#35740=VERTEX_POINT ( 'NONE', #53345 ) ;
#35744=ORIENTED_EDGE ( 'NONE', *, *, #32334, .T. ) ;
#35758=LINE ( 'NONE', #39659, #56081 ) ;
#35762=CIRCLE ( 'NONE', #12086, 0.2000000000000005107 ) ;
#35770=VECTOR ( 'NONE', #33572, 1000.000000000000000 ) ;
#35775=VECTOR ( 'NONE', #35052, 1000.000000000000000 ) ;
#35794=DIRECTION ( 'NONE',  ( 0.000000000000000000, 0.000000000000000000, -1.000000000000000000 ) ) ;
#35801=EDGE_CURVE ( 'NONE', #69217, #28788, #10540, .T. ) ;
#35802=ORIENTED_EDGE ( 'NONE', *, *, #68790, .T. ) ;
#35816=VERTEX_POINT ( 'NONE', #69935 ) ;
#35830=ORIENTED_EDGE ( 'NONE', *, *, #26146, .F. ) ;
#35835=ORIENTED_EDGE ( 'NONE', *, *, #20407, .F. ) ;
#35837=DIRECTION ( 'NONE',  ( 1.000000000000000000, 0.000000000000000000, 0.000000000000000000 ) ) ;
#35838=ORIENTED_EDGE ( 'NONE', *, *, #44572, .T. ) ;
#35848=ORIENTED_EDGE ( 'NONE', *, *, #13141, .T. ) ;
#35850=EDGE_CURVE ( 'NONE', #9996, #23638, #53886, .T. ) ;
#35851=CARTESIAN_POINT ( 'NONE',  ( 7.450000000000003730, -7.249999999999997335, -12.00000000000000000 ) ) ;
#35860=EDGE_CURVE ( 'NONE', #47318, #61277, #22882, .T. ) ;
#35862=EDGE_CURVE ( 'NONE', #69570, #60745, #28866, .T. ) ;
#35864=CARTESIAN_POINT ( 'NONE',  ( 8.750000000000005329, 0.000000000000000000, -26.00000000000001066 ) ) ;
#35866=EDGE_CURVE ( 'NONE', #26202, #5400, #39161, .T. ) ;
#35874=CIRCLE ( 'NONE', #2000, 1.000000000000000000 ) ;
#35875=AXIS2_PLACEMENT_3D ( 'NONE', #23411, #55582, #18084 ) ;
#35882=DIRECTION ( 'NONE',  ( 0.000000000000000000, 0.000000000000000000, 1.000000000000000000 ) ) ;
#35885=EDGE_CURVE ( 'NONE', #30319, #59322, #28186, .T. ) ;
#35889=CYLINDRICAL_SURFACE ( 'NONE', #65065, 1.000000000000000000 ) ;
#35897=EDGE_CURVE ( 'NONE', #33105, #47162, #32420, .T. ) ;
#35904=ORIENTED_EDGE ( 'NONE', *, *, #58330, .F. ) ;
#35905=ORIENTED_EDGE ( 'NONE', *, *, #41642, .F. ) ;
#35911=LINE ( 'NONE', #50761, #21218 ) ;
#35922=CARTESIAN_POINT ( 'NONE',  ( 7.250000000000005329, -7.449999999999998401, -25.00000000000000000 ) ) ;
#35941=DIRECTION ( 'NONE',  ( 1.000000000000000000, 0.000000000000000000, 0.000000000000000000 ) ) ;
#35951=DIRECTION ( 'NONE',  ( 0.000000000000000000, 0.000000000000000000, -1.000000000000000000 ) ) ;
#35957=PLANE ( 'NONE',  #25648 ) ;
#35961=CARTESIAN_POINT ( 'NONE',  ( 7.250000000000005329, 8.250000000000001776, -10.50000000000000000 ) ) ;
#35962=ORIENTED_EDGE ( 'NONE', *, *, #60009, .F. ) ;
#35965=CARTESIAN_POINT ( 'NONE',  ( -7.250000000000001776, -7.249999999999998224, -12.00000000000000000 ) ) ;
#35967=DIRECTION ( 'NONE',  ( 0.000000000000000000, 0.000000000000000000, -1.000000000000000000 ) ) ;
#35974=CARTESIAN_POINT ( 'NONE',  ( 8.250000000000005329, 0.000000000000000000, -9.000000000000001776 ) ) ;
#35977=DIRECTION ( 'NONE',  ( 0.000000000000000000, 0.000000000000000000, 1.000000000000000000 ) ) ;
#35978=VECTOR ( 'NONE', #38381, 1000.000000000000000 ) ;
#35997=EDGE_LOOP ( 'NONE', ( #69477, #63489, #27744, #50934 ) ) ;
#35998=PRODUCT_CONTEXT ( 'NONE', #21429, 'mechanical' ) ;
#36002=ADVANCED_FACE ( 'NONE', ( #7994 ), #18971, .F. ) ;
#36004=PLANE ( 'NONE',  #66682 ) ;
#36005=EDGE_LOOP ( 'NONE', ( #33282, #19321, #42263, #22846 ) ) ;
#36006=EDGE_LOOP ( 'NONE', ( #56504, #40515, #62785, #68944 ) ) ;
#36007=DIRECTION ( 'NONE',  ( 0.000000000000000000, 0.000000000000000000, 1.000000000000000000 ) ) ;
#36009=EDGE_CURVE ( 'NONE', #19769, #47162, #45475, .T. ) ;
#36014=ADVANCED_FACE ( 'NONE', ( #34518 ), #12945, .F. ) ;
#36025=LINE ( 'NONE', #46627, #28353 ) ;
#36029=CARTESIAN_POINT ( 'NONE',  ( 8.250000000000005329, -8.249999999999998224, -26.00000000000001066 ) ) ;
#36031=ORIENTED_EDGE ( 'NONE', *, *, #14633, .T. ) ;
#36037=DIRECTION ( 'NONE',  ( 0.000000000000000000, 0.000000000000000000, 1.000000000000000000 ) ) ;
#36039=CARTESIAN_POINT ( 'NONE',  ( 7.250000000000005329, -7.249999999999998224, -30.00000000000001066 ) ) ;
#36043=DIRECTION ( 'NONE',  ( 1.000000000000000000, 0.000000000000000000, 0.000000000000000000 ) ) ;
#36044=CARTESIAN_POINT ( 'NONE',  ( 4.456444791733522252E-16, 7.450000000000002842, -21.50000000000000000 ) ) ;
#36053=VERTEX_POINT ( 'NONE', #24273 ) ;
#36060=VECTOR ( 'NONE', #61374, 1000.000000000000000 ) ;
#36065=DIRECTION ( 'NONE',  ( 0.000000000000000000, 0.000000000000000000, 1.000000000000000000 ) ) ;
#36069=ORIENTED_EDGE ( 'NONE', *, *, #11588, .F. ) ;
#36076=CARTESIAN_POINT ( 'NONE',  ( -9.690000000000001279, -9.750000000000001776, -5.000000000000000000 ) ) ;
#36079=VERTEX_POINT ( 'NONE', #19654 ) ;
#36081=VERTEX_POINT ( 'NONE', #41226 ) ;
#36104=ORIENTED_EDGE ( 'NONE', *, *, #54064, .F. ) ;
#36117=ADVANCED_FACE ( 'NONE', ( #15070 ), #58201, .F. ) ;
#36119=PLANE ( 'NONE',  #48074 ) ;
#36123=CARTESIAN_POINT ( 'NONE',  ( 7.450000000000006395, 7.250000000000000888, -9.500000000000001776 ) ) ;
#36125=ORIENTED_EDGE ( 'NONE', *, *, #10129, .F. ) ;
#36128=EDGE_LOOP ( 'NONE', ( #60770, #32265, #21319, #55105 ) ) ;
#36134=CARTESIAN_POINT ( 'NONE',  ( 7.250000000000005329, -7.249999999999998224, -26.00000000000001066 ) ) ;
#36136=ORIENTED_EDGE ( 'NONE', *, *, #3423, .T. ) ;
#36142=EDGE_CURVE ( 'NONE', #58160, #17842, #8564, .T. ) ;
#36148=ORIENTED_EDGE ( 'NONE', *, *, #17667, .F. ) ;
#36151=DIRECTION ( 'NONE',  ( -0.000000000000000000, -0.000000000000000000, -1.000000000000000000 ) ) ;
#36152=CARTESIAN_POINT ( 'NONE',  ( 8.250000000000005329, -7.249999999999998224, -10.00000000000000000 ) ) ;
#36154=CIRCLE ( 'NONE', #21473, 0.2000000000000005107 ) ;
#36168=VECTOR ( 'NONE', #15724, 1000.000000000000000 ) ;
#36175=ORIENTED_EDGE ( 'NONE', *, *, #23179, .F. ) ;
#36185=VERTEX_POINT ( 'NONE', #58565 ) ;
#36186=FACE_OUTER_BOUND ( 'NONE', #8334, .T. ) ;
#36187=EDGE_CURVE ( 'NONE', #17538, #46187, #35665, .T. ) ;
#36196=PLANE ( 'NONE',  #21593 ) ;
#36199=EDGE_CURVE ( 'NONE', #48129, #40508, #41585, .T. ) ;
#36211=ORIENTED_EDGE ( 'NONE', *, *, #21737, .F. ) ;
#36216=CARTESIAN_POINT ( 'NONE',  ( 8.250000000000005329, 8.250000000000001776, -26.00000000000001066 ) ) ;
#36219=EDGE_CURVE ( 'NONE', #14260, #5244, #55337, .T. ) ;
#36222=CIRCLE ( 'NONE', #14780, 1.000000000000000000 ) ;
#36224=CARTESIAN_POINT ( 'NONE',  ( 8.689999999999999503, -9.750000000000001776, -7.000000000000000000 ) ) ;
#36226=CARTESIAN_POINT ( 'NONE',  ( -8.250000000000001776, 7.250000000000000888, -19.50000000000000000 ) ) ;
#36231=EDGE_CURVE ( 'NONE', #5578, #50, #59411, .T. ) ;
#36232=DIRECTION ( 'NONE',  ( -0.000000000000000000, -0.000000000000000000, -1.000000000000000000 ) ) ;
#36238=DIRECTION ( 'NONE',  ( -1.000000000000000000, 0.000000000000000000, 0.000000000000000000 ) ) ;
#36239=DIRECTION ( 'NONE',  ( -1.000000000000000000, 0.000000000000000000, -0.000000000000000000 ) ) ;
#36247=VERTEX_POINT ( 'NONE', #28111 ) ;
#36249=ADVANCED_FACE ( 'NONE', ( #6551 ), #23138, .F. ) ;
#36257=ORIENTED_EDGE ( 'NONE', *, *, #64605, .F. ) ;
#36261=ORIENTED_EDGE ( 'NONE', *, *, #62466, .F. ) ;
#36274=AXIS2_PLACEMENT_3D ( 'NONE', #3590, #25864, #57675 ) ;
#36291=LINE ( 'NONE', #37350, #12444 ) ;
#36301=DIRECTION ( 'NONE',  ( 0.000000000000000000, 1.000000000000000000, 0.000000000000000000 ) ) ;
#36307=ORIENTED_EDGE ( 'NONE', *, *, #68604, .T. ) ;
#36309=DIRECTION ( 'NONE',  ( 0.000000000000000000, -1.000000000000000000, 0.000000000000000000 ) ) ;
#36314=CYLINDRICAL_SURFACE ( 'NONE', #40721, 1.000000000000000000 ) ;
#36319=CYLINDRICAL_SURFACE ( 'NONE', #5592, 1.000000000000000000 ) ;
#36321=VERTEX_POINT ( 'NONE', #28441 ) ;
#36325=EDGE_CURVE ( 'NONE', #7579, #20433, #19586, .T. ) ;
#36336=CARTESIAN_POINT ( 'NONE',  ( 7.450000000000006395, 7.250000000000000888, -22.00000000000000000 ) ) ;
#36340=CARTESIAN_POINT ( 'NONE',  ( -7.250000000000000888, 7.250000000000001776, -26.00000000000001066 ) ) ;
#36344=VERTEX_POINT ( 'NONE', #19239 ) ;
#36348=ADVANCED_FACE ( 'NONE', ( #67677 ), #23498, .T. ) ;
#36351=DIRECTION ( 'NONE',  ( 0.000000000000000000, 0.000000000000000000, -1.000000000000000000 ) ) ;
#36353=CARTESIAN_POINT ( 'NONE',  ( -8.750000000000001776, 7.250000000000000000, -30.00000000000001066 ) ) ;
#36371=EDGE_CURVE ( 'NONE', #23372, #21475, #29841, .T. ) ;
#36373=DIRECTION ( 'NONE',  ( 0.000000000000000000, 1.000000000000000000, 0.000000000000000000 ) ) ;
#36382=EDGE_LOOP ( 'NONE', ( #47654, #7304, #56694, #21948 ) ) ;
#36396=CARTESIAN_POINT ( 'NONE',  ( 7.250000000000005329, 7.250000000000000888, -26.00000000000001066 ) ) ;
#36399=CARTESIAN_POINT ( 'NONE',  ( -9.750000000000001776, 9.690000000000001279, -5.000000000000000000 ) ) ;
#36404=ORIENTED_EDGE ( 'NONE', *, *, #55581, .T. ) ;
#36405=CARTESIAN_POINT ( 'NONE',  ( 7.450000000000004619, -1.336933437520057563E-15, -10.00000000000000000 ) ) ;
#36419=VERTEX_POINT ( 'NONE', #67337 ) ;
#36422=CARTESIAN_POINT ( 'NONE',  ( -6.500000000000002665, -6.500000000000002665, 0.000000000000000000 ) ) ;
#36424=ORIENTED_EDGE ( 'NONE', *, *, #36883, .T. ) ;
#36432=DIRECTION ( 'NONE',  ( 1.000000000000000000, -5.981805089575194965E-17, 0.000000000000000000 ) ) ;
#36434=CARTESIAN_POINT ( 'NONE',  ( 8.750000000000005329, -7.249999999999997335, -30.00000000000001066 ) ) ;
#36435=VERTEX_POINT ( 'NONE', #51411 ) ;
#36437=DIRECTION ( 'NONE',  ( 1.000000000000000000, -5.981805089575196197E-17, 0.000000000000000000 ) ) ;
#36440=EDGE_LOOP ( 'NONE', ( #13252, #9909, #10228, #23339 ) ) ;
#36444=PLANE ( 'NONE',  #66916 ) ;
#36447=EDGE_LOOP ( 'NONE', ( #3896, #20176, #58941, #31177 ) ) ;
#36451=ORIENTED_EDGE ( 'NONE', *, *, #57319, .F. ) ;
#36464=CARTESIAN_POINT ( 'NONE',  ( 0.000000000000000000, 8.250000000000001776, -8.500000000000000000 ) ) ;
#36468=DIRECTION ( 'NONE',  ( -1.794541526872559352E-16, -1.000000000000000000, 0.000000000000000000 ) ) ;
#36471=CARTESIAN_POINT ( 'NONE',  ( -7.250000000000000888, 7.450000000000003730, -25.00000000000000000 ) ) ;
#36478=PLANE ( 'NONE',  #38574 ) ;
#36496=LINE ( 'NONE', #53139, #25337 ) ;
#36497=VECTOR ( 'NONE', #68121, 1000.000000000000000 ) ;
#36503=ORIENTED_EDGE ( 'NONE', *, *, #53507, .T. ) ;
#36506=DIRECTION ( 'NONE',  ( 0.000000000000000000, 0.000000000000000000, -1.000000000000000000 ) ) ;
#36511=LINE ( 'NONE', #68708, #42504 ) ;
#36522=LINE ( 'NONE', #31928, #63672 ) ;
#36523=ORIENTED_EDGE ( 'NONE', *, *, #63443, .T. ) ;
#36531=ORIENTED_EDGE ( 'NONE', *, *, #4552, .F. ) ;
#36539=CARTESIAN_POINT ( 'NONE',  ( 7.250000000000005329, 8.250000000000001776, -26.00000000000001066 ) ) ;
#36552=CARTESIAN_POINT ( 'NONE',  ( 7.250000000000004441, 7.450000000000001954, -8.000000000000000000 ) ) ;
#36559=DIRECTION ( 'NONE',  ( -1.000000000000000000, 0.000000000000000000, 0.000000000000000000 ) ) ;
#36573=CARTESIAN_POINT ( 'NONE',  ( 8.250000000000005329, -7.249999999999998224, -13.00000000000000178 ) ) ;
#36590=ORIENTED_EDGE ( 'NONE', *, *, #1847, .T. ) ;
#36591=EDGE_CURVE ( 'NONE', #20264, #51421, #63785, .T. ) ;
#36595=AXIS2_PLACEMENT_3D ( 'NONE', #65270, #923, #17153 ) ;
#36604=ADVANCED_FACE ( 'NONE', ( #21342 ), #22036, .F. ) ;
#36615=ORIENTED_EDGE ( 'NONE', *, *, #59645, .T. ) ;
#36616=LINE ( 'NONE', #25315, #3403 ) ;
#36634=CYLINDRICAL_SURFACE ( 'NONE', #8542, 0.1999999999999987899 ) ;
#36637=ORIENTED_EDGE ( 'NONE', *, *, #15210, .F. ) ;
#36638=DIRECTION ( 'NONE',  ( -1.000000000000000000, 0.000000000000000000, 0.000000000000000000 ) ) ;
#36639=DIRECTION ( 'NONE',  ( 0.000000000000000000, 1.000000000000000000, 0.000000000000000000 ) ) ;
#36640=VECTOR ( 'NONE', #4961, 1000.000000000000000 ) ;
#36651=DIRECTION ( 'NONE',  ( -0.000000000000000000, 0.000000000000000000, 1.000000000000000000 ) ) ;
#36652=CARTESIAN_POINT ( 'NONE',  ( 7.450000000000006395, 7.250000000000000888, -23.50000000000000000 ) ) ;
#36656=ADVANCED_FACE ( 'NONE', ( #49260 ), #65851, .T. ) ;
#36660=DIRECTION ( 'NONE',  ( -0.000000000000000000, -0.000000000000000000, -1.000000000000000000 ) ) ;
#36670=CARTESIAN_POINT ( 'NONE',  ( -7.250000000000001776, -7.249999999999998224, -13.50000000000000178 ) ) ;
#36691=ORIENTED_EDGE ( 'NONE', *, *, #61585, .F. ) ;
#36699=CARTESIAN_POINT ( 'NONE',  ( -7.250000000000000888, 8.250000000000001776, -13.00000000000000178 ) ) ;
#36701=DIRECTION ( 'NONE',  ( -0.000000000000000000, -0.000000000000000000, -1.000000000000000000 ) ) ;
#36708=EDGE_LOOP ( 'NONE', ( #2714, #34220, #532, #3050 ) ) ;
#36711=DIRECTION ( 'NONE',  ( 1.000000000000000000, -5.981805089575194965E-17, 0.000000000000000000 ) ) ;
#36717=ORIENTED_EDGE ( 'NONE', *, *, #49004, .T. ) ;
#36724=CARTESIAN_POINT ( 'NONE',  ( -7.450000000000001954, 7.250000000000000000, -12.50000000000000000 ) ) ;
#36733=VERTEX_POINT ( 'NONE', #40000 ) ;
#36749=CIRCLE ( 'NONE', #48048, 1.500000000000001332 ) ;
#36759=LINE ( 'NONE', #57959, #25449 ) ;
#36762=DIRECTION ( 'NONE',  ( 1.000000000000000000, 0.000000000000000000, 0.000000000000000000 ) ) ;
#36765=EDGE_CURVE ( 'NONE', #32155, #5314, #35400, .T. ) ;
#36768=AXIS2_PLACEMENT_3D ( 'NONE', #63938, #58972, #57923 ) ;
#36774=ORIENTED_EDGE ( 'NONE', *, *, #61997, .F. ) ;
#36783=ORIENTED_EDGE ( 'NONE', *, *, #50860, .F. ) ;
#36789=EDGE_CURVE ( 'NONE', #42345, #25681, #61663, .T. ) ;
#36790=CARTESIAN_POINT ( 'NONE',  ( 0.000000000000000000, -8.249999999999998224, -25.50000000000000355 ) ) ;
#36795=DIRECTION ( 'NONE',  ( -1.794541526872559352E-16, -1.000000000000000000, 0.000000000000000000 ) ) ;
#36796=CARTESIAN_POINT ( 'NONE',  ( 7.250000000000005329, 7.250000000000000888, -26.00000000000001066 ) ) ;
#36806=AXIS2_PLACEMENT_3D ( 'NONE', #19332, #39837, #3088 ) ;
#36814=DIRECTION ( 'NONE',  ( 0.000000000000000000, 0.000000000000000000, 1.000000000000000000 ) ) ;
#36819=DIRECTION ( 'NONE',  ( 0.000000000000000000, 0.000000000000000000, -1.000000000000000000 ) ) ;
#36824=DIRECTION ( 'NONE',  ( 0.000000000000000000, 0.000000000000000000, -1.000000000000000000 ) ) ;
#36826=VECTOR ( 'NONE', #27520, 1000.000000000000000 ) ;
#36829=EDGE_CURVE ( 'NONE', #43764, #29937, #18093, .T. ) ;
#36834=ADVANCED_FACE ( 'NONE', ( #29066 ), #67244, .F. ) ;
#36838=EDGE_CURVE ( 'NONE', #36344, #34855, #22213, .T. ) ;
#36839=CARTESIAN_POINT ( 'NONE',  ( 7.450000000000004619, -1.336933437520057563E-15, -12.00000000000000000 ) ) ;
#36843=CARTESIAN_POINT ( 'NONE',  ( 7.450000000000004619, -1.336933437520057563E-15, -24.50000000000000000 ) ) ;
#36847=CARTESIAN_POINT ( 'NONE',  ( 8.750000000000005329, 7.250000000000000888, -30.00000000000001066 ) ) ;
#36848=AXIS2_PLACEMENT_3D ( 'NONE', #62806, #14377, #35941 ) ;
#36851=ORIENTED_EDGE ( 'NONE', *, *, #68107, .F. ) ;
#36863=DIRECTION ( 'NONE',  ( 0.000000000000000000, 0.000000000000000000, -1.000000000000000000 ) ) ;
#36865=VERTEX_POINT ( 'NONE', #61932 ) ;
#36866=CARTESIAN_POINT ( 'NONE',  ( -7.450000000000001954, 7.250000000000000000, -10.50000000000000000 ) ) ;
#36869=AXIS2_PLACEMENT_3D ( 'NONE', #29270, #46246, #7710 ) ;
#36871=DIRECTION ( 'NONE',  ( 0.000000000000000000, 0.000000000000000000, -1.000000000000000000 ) ) ;
#36876=ORIENTED_EDGE ( 'NONE', *, *, #48346, .F. ) ;
#36883=EDGE_CURVE ( 'NONE', #10391, #47005, #51582, .T. ) ;
#36895=ORIENTED_EDGE ( 'NONE', *, *, #16992, .F. ) ;
#36905=LINE ( 'NONE', #48205, #66663 ) ;
#36906=LINE ( 'NONE', #4026, #51470 ) ;
#36912=CIRCLE ( 'NONE', #16615, 0.9999999999999991118 ) ;
#36919=CARTESIAN_POINT ( 'NONE',  ( 7.450000000000004619, -1.336933437520057563E-15, -22.50000000000000000 ) ) ;
#36920=VECTOR ( 'NONE', #6711, 1000.000000000000000 ) ;
#36923=DIRECTION ( 'NONE',  ( 0.000000000000000000, 0.000000000000000000, 1.000000000000000000 ) ) ;
#36929=VERTEX_POINT ( 'NONE', #42115 ) ;
#36933=DIRECTION ( 'NONE',  ( 0.000000000000000000, 0.000000000000000000, 1.000000000000000000 ) ) ;
#36934=FACE_OUTER_BOUND ( 'NONE', #33121, .T. ) ;
#36938=CARTESIAN_POINT ( 'NONE',  ( 0.000000000000000000, -7.449999999999998401, -19.50000000000000000 ) ) ;
#36940=DIRECTION ( 'NONE',  ( 0.000000000000000000, -0.000000000000000000, 1.000000000000000000 ) ) ;
#36960=ORIENTED_EDGE ( 'NONE', *, *, #50523, .F. ) ;
#36962=AXIS2_PLACEMENT_3D ( 'NONE', #44690, #45740, #55665 ) ;
#36966=ORIENTED_EDGE ( 'NONE', *, *, #22849, .T. ) ;
#36968=EDGE_CURVE ( 'NONE', #63525, #36419, #52037, .T. ) ;
#36970=AXIS2_PLACEMENT_3D ( 'NONE', #69520, #69864, #21425 ) ;
#36978=FACE_OUTER_BOUND ( 'NONE', #4900, .T. ) ;
#36985=EDGE_LOOP ( 'NONE', ( #57509, #49521, #4972, #21522 ) ) ;
#36996=ORIENTED_EDGE ( 'NONE', *, *, #30606, .F. ) ;
#36999=AXIS2_PLACEMENT_3D ( 'NONE', #64565, #5518, #27075 ) ;
#37005=CARTESIAN_POINT ( 'NONE',  ( -8.250000000000001776, -8.249999999999998224, -26.00000000000001066 ) ) ;
#37011=ORIENTED_EDGE ( 'NONE', *, *, #29392, .T. ) ;
#37021=ORIENTED_EDGE ( 'NONE', *, *, #24085, .F. ) ;
#37025=CARTESIAN_POINT ( 'NONE',  ( -7.250000000000000888, 7.250000000000001776, -11.00000000000000000 ) ) ;
#37043=AXIS2_PLACEMENT_3D ( 'NONE', #66562, #55609, #40019 ) ;
#37048=CARTESIAN_POINT ( 'NONE',  ( -7.250000000000000888, 8.750000000000001776, -30.00000000000001066 ) ) ;
#37050=EDGE_LOOP ( 'NONE', ( #40495, #45266, #16533, #46417 ) ) ;
#37079=CARTESIAN_POINT ( 'NONE',  ( -7.250000000000000888, 8.250000000000001776, -7.500000000000000000 ) ) ;
#37083=DIRECTION ( 'NONE',  ( -1.000000000000000000, 1.334402673828312846E-16, 0.000000000000000000 ) ) ;
#37093=FACE_OUTER_BOUND ( 'NONE', #5425, .T. ) ;
#37098=EDGE_CURVE ( 'NONE', #68282, #21718, #47096, .T. ) ;
#37116=VERTEX_POINT ( 'NONE', #32574 ) ;
#37117=CARTESIAN_POINT ( 'NONE',  ( -7.250000000000000888, 7.450000000000003730, -11.50000000000000000 ) ) ;
#37122=DIRECTION ( 'NONE',  ( -1.000000000000000000, 0.000000000000000000, 0.000000000000000000 ) ) ;
#37126=EDGE_LOOP ( 'NONE', ( #46220, #21072, #34879, #61989 ) ) ;
#37130=CARTESIAN_POINT ( 'NONE',  ( -7.450000000000001954, -7.249999999999998224, -22.00000000000000000 ) ) ;
#37136=EDGE_CURVE ( 'NONE', #41339, #3133, #44191, .T. ) ;
#37141=ORIENTED_EDGE ( 'NONE', *, *, #14654, .T. ) ;
#37143=CARTESIAN_POINT ( 'NONE',  ( -7.450000000000001954, 0.000000000000000000, -14.50000000000000000 ) ) ;
#37146=ORIENTED_EDGE ( 'NONE', *, *, #59856, .F. ) ;
#37147=EDGE_CURVE ( 'NONE', #16300, #25227, #16991, .T. ) ;
#37156=VERTEX_POINT ( 'NONE', #49514 ) ;
#37158=EDGE_CURVE ( 'NONE', #10775, #21736, #64399, .T. ) ;
#37161=DIRECTION ( 'NONE',  ( -1.794541526872559352E-16, -1.000000000000000000, 0.000000000000000000 ) ) ;
#37165=EDGE_CURVE ( 'NONE', #14678, #58971, #62812, .T. ) ;
#37168=CARTESIAN_POINT ( 'NONE',  ( 0.000000000000000000, -7.449999999999998401, -15.50000000000000000 ) ) ;
#37175=DIRECTION ( 'NONE',  ( 1.000000000000000000, 0.000000000000000000, 0.000000000000000000 ) ) ;
#37187=ADVANCED_FACE ( 'NONE', ( #40538 ), #30296, .T. ) ;
#37197=CARTESIAN_POINT ( 'NONE',  ( 7.250000000000004441, 7.450000000000001954, -11.00000000000000000 ) ) ;
#37209=AXIS2_PLACEMENT_3D ( 'NONE', #57422, #30555, #52122 ) ;
#37211=CARTESIAN_POINT ( 'NONE',  ( -7.250000000000001776, -7.249999999999998224, -19.50000000000000000 ) ) ;
#37214=LINE ( 'NONE', #59811, #69044 ) ;
#37230=ADVANCED_FACE ( 'NONE', ( #9422 ), #13671, .T. ) ;
#37234=CARTESIAN_POINT ( 'NONE',  ( -7.250000000000000000, -7.449999999999998401, -11.50000000000000000 ) ) ;
#37235=EDGE_CURVE ( 'NONE', #20433, #66152, #35578, .T. ) ;
#37239=VECTOR ( 'NONE', #69685, 1000.000000000000000 ) ;
#37251=DIRECTION ( 'NONE',  ( 0.000000000000000000, 1.000000000000000000, -0.000000000000000000 ) ) ;
#37261=DIRECTION ( 'NONE',  ( -1.000000000000000000, 0.000000000000000000, 0.000000000000000000 ) ) ;
#37262=FACE_OUTER_BOUND ( 'NONE', #57851, .T. ) ;
#37265=DIRECTION ( 'NONE',  ( -1.000000000000000000, 0.000000000000000000, 0.000000000000000000 ) ) ;
#37266=ADVANCED_FACE ( 'NONE', ( #29575 ), #8355, .F. ) ;
#37280=DIRECTION ( 'NONE',  ( 0.000000000000000000, 0.000000000000000000, -1.000000000000000000 ) ) ;
#37288=DIRECTION ( 'NONE',  ( 1.000000000000000000, 0.000000000000000000, 0.000000000000000000 ) ) ;
#37297=CARTESIAN_POINT ( 'NONE',  ( -7.250000000000000888, -8.249999999999998224, -26.00000000000001066 ) ) ;
#37300=AXIS2_PLACEMENT_3D ( 'NONE', #58152, #63460, #9722 ) ;
#37303=LINE ( 'NONE', #27385, #69197 ) ;
#37311=EDGE_CURVE ( 'NONE', #59150, #10667, #51637, .T. ) ;
#37315=EDGE_CURVE ( 'NONE', #43050, #12421, #58914, .T. ) ;
#37317=CYLINDRICAL_SURFACE ( 'NONE', #19618, 1.000000000000000000 ) ;
#37319=CARTESIAN_POINT ( 'NONE',  ( 7.250000000000005329, 7.250000000000000888, -23.00000000000000000 ) ) ;
#37323=EDGE_LOOP ( 'NONE', ( #57195, #5238, #16449, #49392, #38657, #34799, #4597, #10937 ) ) ;
#37331=DIRECTION ( 'NONE',  ( 0.000000000000000000, 0.000000000000000000, -1.000000000000000000 ) ) ;
#37336=DIRECTION ( 'NONE',  ( -1.000000000000000000, -0.000000000000000000, -0.000000000000000000 ) ) ;
#37350=CARTESIAN_POINT ( 'NONE',  ( 7.250000000000005329, 8.250000000000001776, -26.00000000000001066 ) ) ;
#37352=EDGE_CURVE ( 'NONE', #59223, #19699, #31365, .T. ) ;
#37359=DIRECTION ( 'NONE',  ( -1.000000000000000000, 0.000000000000000000, 0.000000000000000000 ) ) ;
#37371=DIRECTION ( 'NONE',  ( -1.000000000000000000, 0.000000000000000000, 0.000000000000000000 ) ) ;
#37379=LINE ( 'NONE', #42321, #30418 ) ;
#37385=VERTEX_POINT ( 'NONE', #15433 ) ;
#37387=EDGE_LOOP ( 'NONE', ( #22524, #39531, #628, #34425 ) ) ;
#37390=EDGE_CURVE ( 'NONE', #25369, #7124, #20033, .T. ) ;
#37398=ADVANCED_FACE ( 'NONE', ( #48650 ), #21776, .F. ) ;
#37401=VECTOR ( 'NONE', #21531, 1000.000000000000000 ) ;
#37429=CARTESIAN_POINT ( 'NONE',  ( 7.250000000000004441, 7.450000000000001954, -23.50000000000000000 ) ) ;
#37445=DIRECTION ( 'NONE',  ( 0.000000000000000000, 0.000000000000000000, 1.000000000000000000 ) ) ;
#37451=CARTESIAN_POINT ( 'NONE',  ( -8.750000000000003553, 7.750000000000001776, 0.000000000000000000 ) ) ;
#37469=ORIENTED_EDGE ( 'NONE', *, *, #61058, .T. ) ;
#37475=ORIENTED_EDGE ( 'NONE', *, *, #34400, .T. ) ;
#37477=CARTESIAN_POINT ( 'NONE',  ( -7.250000000000001776, -7.249999999999998224, -26.00000000000001066 ) ) ;
#37488=CARTESIAN_POINT ( 'NONE',  ( -7.250000000000000888, 7.450000000000003730, -10.00000000000000000 ) ) ;
#37490=CARTESIAN_POINT ( 'NONE',  ( -7.250000000000000888, 8.250000000000001776, -23.00000000000000000 ) ) ;
#37500=CARTESIAN_POINT ( 'NONE',  ( -9.689999999999999503, -9.750000000000001776, -4.250000000000000000 ) ) ;
#37511=ORIENTED_EDGE ( 'NONE', *, *, #28926, .T. ) ;
#37522=CARTESIAN_POINT ( 'NONE',  ( 7.250000000000005329, -8.249999999999998224, -24.50000000000000000 ) ) ;
#37526=CARTESIAN_POINT ( 'NONE',  ( 10.50000000000000178, 9.690000000000001279, -4.250000000000000000 ) ) ;
#37528=EDGE_LOOP ( 'NONE', ( #56777, #47064, #29549, #40259 ) ) ;
#37539=CARTESIAN_POINT ( 'NONE',  ( -7.250000000000000888, -8.249999999999998224, -26.00000000000001066 ) ) ;
#37542=CARTESIAN_POINT ( 'NONE',  ( 0.000000000000000000, 0.000000000000000000, -10.00000000000000000 ) ) ;
#37544=EDGE_CURVE ( 'NONE', #21483, #47295, #8725, .T. ) ;
#37547=CARTESIAN_POINT ( 'NONE',  ( -7.250000000000000888, 7.250000000000001776, -26.00000000000001066 ) ) ;
#37549=EDGE_CURVE ( 'NONE', #14678, #17991, #17156, .T. ) ;
#37556=ADVANCED_FACE ( 'NONE', ( #28121 ), #49684, .F. ) ;
#37566=CARTESIAN_POINT ( 'NONE',  ( 7.450000000000004619, -1.336933437520057563E-15, -7.500000000000000000 ) ) ;
#37568=DIRECTION ( 'NONE',  ( 1.000000000000000000, -0.000000000000000000, 0.000000000000000000 ) ) ;
#37572=VECTOR ( 'NONE', #57957, 1000.000000000000000 ) ;
#37576=CIRCLE ( 'NONE', #25141, 1.000000000000000888 ) ;
#37579=ORIENTED_EDGE ( 'NONE', *, *, #38098, .F. ) ;
#37593=ORIENTED_EDGE ( 'NONE', *, *, #31157, .F. ) ;
#37601=FACE_OUTER_BOUND ( 'NONE', #25322, .T. ) ;
#37602=EDGE_LOOP ( 'NONE', ( #26153, #16343, #13382, #66821 ) ) ;
#37610=DIRECTION ( 'NONE',  ( 0.000000000000000000, -0.000000000000000000, -1.000000000000000000 ) ) ;
#37617=ORIENTED_EDGE ( 'NONE', *, *, #19700, .T. ) ;
#37618=LINE ( 'NONE', #65193, #58102 ) ;
#37619=CIRCLE ( 'NONE', #13921, 0.2000000000000005107 ) ;
#37621=DIRECTION ( 'NONE',  ( -1.000000000000000000, 0.000000000000000000, 0.000000000000000000 ) ) ;
#37635=DIRECTION ( 'NONE',  ( 0.000000000000000000, 0.000000000000000000, -1.000000000000000000 ) ) ;
#37638=ORIENTED_EDGE ( 'NONE', *, *, #10326, .T. ) ;
#37640=AXIS2_PLACEMENT_3D ( 'NONE', #43274, #64855, #28390 ) ;
#37647=DIRECTION ( 'NONE',  ( -5.981805089575196197E-17, -1.000000000000000000, 0.000000000000000000 ) ) ;
#37648=ORIENTED_EDGE ( 'NONE', *, *, #44624, .T. ) ;
#37650=DIRECTION ( 'NONE',  ( 1.000000000000000000, -5.981805089575196197E-17, 0.000000000000000000 ) ) ;
#37659=EDGE_CURVE ( 'NONE', #19811, #17866, #4259, .T. ) ;
#37670=ORIENTED_EDGE ( 'NONE', *, *, #50536, .F. ) ;
#37674=CARTESIAN_POINT ( 'NONE',  ( -7.250000000000000888, 8.250000000000001776, -11.50000000000000000 ) ) ;
#37676=AXIS2_PLACEMENT_3D ( 'NONE', #6569, #60287, #28126 ) ;
#37681=DIRECTION ( 'NONE',  ( -0.000000000000000000, 0.000000000000000000, -1.000000000000000000 ) ) ;
#37686=CARTESIAN_POINT ( 'NONE',  ( 7.450000000000003730, -7.249999999999997335, -10.50000000000000000 ) ) ;
#37698=LINE ( 'NONE', #59262, #60216 ) ;
#37699=EDGE_CURVE ( 'NONE', #60252, #13864, #63793, .T. ) ;
#37705=AXIS2_PLACEMENT_3D ( 'NONE', #14488, #58333, #36043 ) ;
#37710=DIRECTION ( 'NONE',  ( 0.000000000000000000, 0.000000000000000000, -1.000000000000000000 ) ) ;
#37727=DIRECTION ( 'NONE',  ( -1.794541526872559352E-16, -1.000000000000000000, 0.000000000000000000 ) ) ;
#37728=ORIENTED_EDGE ( 'NONE', *, *, #47975, .T. ) ;
#37732=EDGE_LOOP ( 'NONE', ( #65658, #43641, #43165, #47981 ) ) ;
#37739=DIRECTION ( 'NONE',  ( 0.000000000000000000, 0.000000000000000000, -1.000000000000000000 ) ) ;
#37759=AXIS2_PLACEMENT_3D ( 'NONE', #6908, #56049, #1600 ) ;
#37763=ORIENTED_EDGE ( 'NONE', *, *, #55273, .F. ) ;
#37766=DIRECTION ( 'NONE',  ( 0.000000000000000000, 0.000000000000000000, 1.000000000000000000 ) ) ;
#37770=CIRCLE ( 'NONE', #26465, 0.9999999999999991118 ) ;
#37772=EDGE_CURVE ( 'NONE', #41033, #33622, #34755, .T. ) ;
#37776=VERTEX_POINT ( 'NONE', #48575 ) ;
#37777=ORIENTED_EDGE ( 'NONE', *, *, #34902, .F. ) ;
#37806=DIRECTION ( 'NONE',  ( 1.000000000000000000, -5.981805089575194965E-17, 0.000000000000000000 ) ) ;
#37809=VECTOR ( 'NONE', #58376, 1000.000000000000000 ) ;
#37823=VERTEX_POINT ( 'NONE', #15704 ) ;
#37828=DIRECTION ( 'NONE',  ( -1.000000000000000000, 0.000000000000000000, 0.000000000000000000 ) ) ;
#37836=CARTESIAN_POINT ( 'NONE',  ( -7.250000000000000888, 7.250000000000001776, -26.00000000000001066 ) ) ;
#37842=EDGE_CURVE ( 'NONE', #26123, #40904, #2007, .T. ) ;
#37845=ORIENTED_EDGE ( 'NONE', *, *, #64158, .T. ) ;
#37847=FACE_OUTER_BOUND ( 'NONE', #45114, .T. ) ;
#37855=CARTESIAN_POINT ( 'NONE',  ( -7.250000000000000888, 8.250000000000001776, -14.00000000000000000 ) ) ;
#37866=VECTOR ( 'NONE', #30861, 1000.000000000000000 ) ;
#37867=LINE ( 'NONE', #42815, #29543 ) ;
#37868=CARTESIAN_POINT ( 'NONE',  ( -10.50000000000000178, -9.690000000000001279, -5.000000000000000000 ) ) ;
#37874=DIRECTION ( 'NONE',  ( -1.000000000000000000, 0.000000000000000000, 0.000000000000000000 ) ) ;
#37878=DIRECTION ( 'NONE',  ( 0.000000000000000000, 0.000000000000000000, -1.000000000000000000 ) ) ;
#37883=ADVANCED_FACE ( 'NONE', ( #11424 ), #1178, .T. ) ;
#37887=ORIENTED_EDGE ( 'NONE', *, *, #27632, .F. ) ;
#37890=ORIENTED_EDGE ( 'NONE', *, *, #69803, .F. ) ;
#37892=FACE_OUTER_BOUND ( 'NONE', #16526, .T. ) ;
#37906=CIRCLE ( 'NONE', #54859, 1.000000000000000000 ) ;
#37922=VECTOR ( 'NONE', #68618, 1000.000000000000000 ) ;
#37927=EDGE_LOOP ( 'NONE', ( #66469, #16447 ) ) ;
#37931=FACE_OUTER_BOUND ( 'NONE', #27153, .T. ) ;
#37934=ORIENTED_EDGE ( 'NONE', *, *, #34557, .F. ) ;
#37936=VERTEX_POINT ( 'NONE', #38653 ) ;
#37938=DIRECTION ( 'NONE',  ( -1.000000000000000000, 0.000000000000000000, 0.000000000000000000 ) ) ;
#37948=DIRECTION ( 'NONE',  ( -0.000000000000000000, 0.000000000000000000, -1.000000000000000000 ) ) ;
#37952=ORIENTED_EDGE ( 'NONE', *, *, #4074, .F. ) ;
#37955=DIRECTION ( 'NONE',  ( -0.000000000000000000, -0.000000000000000000, 1.000000000000000000 ) ) ;
#37970=DIRECTION ( 'NONE',  ( 0.000000000000000000, 0.000000000000000000, 1.000000000000000000 ) ) ;
#37971=CARTESIAN_POINT ( 'NONE',  ( 7.250000000000005329, 7.250000000000000888, -7.500000000000000000 ) ) ;
#37980=CARTESIAN_POINT ( 'NONE',  ( -7.250000000000001776, -7.249999999999998224, -20.50000000000000000 ) ) ;
#37982=VECTOR ( 'NONE', #64142, 1000.000000000000000 ) ;
#37987=FACE_OUTER_BOUND ( 'NONE', #38811, .T. ) ;
#38000=FACE_OUTER_BOUND ( 'NONE', #69595, .T. ) ;
#38005=AXIS2_PLACEMENT_3D ( 'NONE', #56676, #23100, #56328 ) ;
#38015=AXIS2_PLACEMENT_3D ( 'NONE', #39596, #45248, #2128 ) ;
#38017=AXIS2_PLACEMENT_3D ( 'NONE', #15239, #40698, #47404 ) ;
#38022=CARTESIAN_POINT ( 'NONE',  ( 7.250000000000005329, -7.249999999999998224, -12.50000000000000000 ) ) ;
#38028=ORIENTED_EDGE ( 'NONE', *, *, #34321, .F. ) ;
#38035=ORIENTED_EDGE ( 'NONE', *, *, #11221, .T. ) ;
#38041=EDGE_CURVE ( 'NONE', #69380, #63685, #50641, .T. ) ;
#38047=ORIENTED_EDGE ( 'NONE', *, *, #54796, .F. ) ;
#38049=EDGE_CURVE ( 'NONE', #7966, #16300, #25754, .T. ) ;
#38055=CARTESIAN_POINT ( 'NONE',  ( -9.690000000000001279, -9.690000000000001279, -5.000000000000000000 ) ) ;
#38056=VECTOR ( 'NONE', #1325, 1000.000000000000000 ) ;
#38063=ADVANCED_FACE ( 'NONE', ( #40013 ), #66555, .T. ) ;
#38074=VECTOR ( 'NONE', #12307, 1000.000000000000000 ) ;
#38078=CARTESIAN_POINT ( 'NONE',  ( 7.250000000000005329, -7.249999999999998224, -26.00000000000001066 ) ) ;
#38080=AXIS2_PLACEMENT_3D ( 'NONE', #55416, #7297, #6955 ) ;
#38088=PLANE ( 'NONE',  #63944 ) ;
#38090=FACE_BOUND ( 'NONE', #19706, .T. ) ;
#38095=CARTESIAN_POINT ( 'NONE',  ( 8.250000000000005329, -8.249999999999998224, -26.00000000000001066 ) ) ;
#38098=EDGE_CURVE ( 'NONE', #50834, #1029, #3252, .T. ) ;
#38102=ORIENTED_EDGE ( 'NONE', *, *, #26047, .F. ) ;
#38106=CARTESIAN_POINT ( 'NONE',  ( 7.250000000000005329, 8.250000000000001776, -25.50000000000000355 ) ) ;
#38124=ORIENTED_EDGE ( 'NONE', *, *, #18363, .F. ) ;
#38131=DIRECTION ( 'NONE',  ( 0.000000000000000000, 0.000000000000000000, 1.000000000000000000 ) ) ;
#38151=VECTOR ( 'NONE', #29425, 1000.000000000000000 ) ;
#38154=LINE ( 'NONE', #66390, #60109 ) ;
#38159=ORIENTED_EDGE ( 'NONE', *, *, #26347, .T. ) ;
#38160=FACE_OUTER_BOUND ( 'NONE', #2604, .T. ) ;
#38163=CARTESIAN_POINT ( 'NONE',  ( -8.250000000000001776, -7.249999999999998224, -17.00000000000000000 ) ) ;
#38165=VECTOR ( 'NONE', #34080, 1000.000000000000000 ) ;
#38168=ORIENTED_EDGE ( 'NONE', *, *, #9925, .T. ) ;
#38181=ORIENTED_EDGE ( 'NONE', *, *, #69219, .F. ) ;
#38196=LINE ( 'NONE', #43829, #22940 ) ;
#38198=ADVANCED_FACE ( 'NONE', ( #54795 ), #33569, .F. ) ;
#38214=FACE_OUTER_BOUND ( 'NONE', #35122, .T. ) ;
#38217=DIRECTION ( 'NONE',  ( -1.000000000000000000, 0.000000000000000000, 0.000000000000000000 ) ) ;
#38224=AXIS2_PLACEMENT_3D ( 'NONE', #39550, #16634, #716 ) ;
#38225=DIRECTION ( 'NONE',  ( -0.000000000000000000, -0.000000000000000000, 1.000000000000000000 ) ) ;
#38227=DIRECTION ( 'NONE',  ( 0.000000000000000000, 0.000000000000000000, 1.000000000000000000 ) ) ;
#38235=PLANE ( 'NONE',  #40039 ) ;
#38236=ORIENTED_EDGE ( 'NONE', *, *, #38584, .T. ) ;
#38241=CARTESIAN_POINT ( 'NONE',  ( -7.450000000000001954, -7.249999999999998224, -16.50000000000000000 ) ) ;
#38243=EDGE_CURVE ( 'NONE', #41058, #59828, #22284, .T. ) ;
#38250=CARTESIAN_POINT ( 'NONE',  ( 0.000000000000000000, 8.250000000000001776, -24.50000000000000000 ) ) ;
#38251=ORIENTED_EDGE ( 'NONE', *, *, #61545, .F. ) ;
#38252=ORIENTED_EDGE ( 'NONE', *, *, #31428, .F. ) ;
#38255=AXIS2_PLACEMENT_3D ( 'NONE', #44071, #37739, #65316 ) ;
#38256=FACE_OUTER_BOUND ( 'NONE', #22837, .T. ) ;
#38257=FACE_OUTER_BOUND ( 'NONE', #66925, .T. ) ;
#38263=VECTOR ( 'NONE', #30154, 1000.000000000000000 ) ;
#38267=VECTOR ( 'NONE', #18533, 1000.000000000000000 ) ;
#38268=DIRECTION ( 'NONE',  ( -5.981805089575196197E-17, -1.000000000000000000, 0.000000000000000000 ) ) ;
#38270=LINE ( 'NONE', #44940, #50362 ) ;
#38271=ORIENTED_EDGE ( 'NONE', *, *, #55995, .F. ) ;
#38273=ORIENTED_EDGE ( 'NONE', *, *, #10390, .T. ) ;
#38277=ADVANCED_FACE ( 'NONE', ( #27924 ), #27572, .T. ) ;
#38282=EDGE_CURVE ( 'NONE', #6090, #190, #21262, .T. ) ;
#38289=EDGE_CURVE ( 'NONE', #31253, #23277, #40257, .T. ) ;
#38297=ORIENTED_EDGE ( 'NONE', *, *, #45715, .F. ) ;
#38309=CARTESIAN_POINT ( 'NONE',  ( 7.450000000000006395, 7.250000000000000888, -17.50000000000000000 ) ) ;
#38310=AXIS2_PLACEMENT_3D ( 'NONE', #55209, #55551, #1123 ) ;
#38316=CIRCLE ( 'NONE', #7793, 1.000000000000000000 ) ;
#38321=CARTESIAN_POINT ( 'NONE',  ( 7.250000000000005329, 7.250000000000000888, -26.00000000000001066 ) ) ;
#38326=DIRECTION ( 'NONE',  ( 0.000000000000000000, 0.000000000000000000, 1.000000000000000000 ) ) ;
#38331=CARTESIAN_POINT ( 'NONE',  ( -7.450000000000001954, 0.000000000000000000, -17.50000000000000000 ) ) ;
#38336=LINE ( 'NONE', #59888, #26405 ) ;
#38338=CARTESIAN_POINT ( 'NONE',  ( -7.250000000000000888, 8.250000000000001776, -26.00000000000001066 ) ) ;
#38340=DIRECTION ( 'NONE',  ( 0.000000000000000000, -0.000000000000000000, 1.000000000000000000 ) ) ;
#38345=EDGE_LOOP ( 'NONE', ( #8089, #66493, #55481, #68097 ) ) ;
#38350=EDGE_CURVE ( 'NONE', #24784, #60224, #31463, .T. ) ;
#38365=ORIENTED_EDGE ( 'NONE', *, *, #2545, .T. ) ;
#38366=AXIS2_PLACEMENT_3D ( 'NONE', #33949, #22334, #12031 ) ;
#38368=CARTESIAN_POINT ( 'NONE',  ( -7.250000000000000888, 7.250000000000001776, -22.00000000000000000 ) ) ;
#38369=EDGE_CURVE ( 'NONE', #6104, #26651, #8788, .T. ) ;
#38378=VECTOR ( 'NONE', #34583, 1000.000000000000000 ) ;
#38381=DIRECTION ( 'NONE',  ( 0.000000000000000000, 1.000000000000000000, 0.000000000000000000 ) ) ;
#38382=DIRECTION ( 'NONE',  ( 1.000000000000000000, 0.000000000000000000, 0.000000000000000000 ) ) ;
#38392=DIRECTION ( 'NONE',  ( -0.000000000000000000, -0.000000000000000000, 1.000000000000000000 ) ) ;
#38402=CARTESIAN_POINT ( 'NONE',  ( 7.450000000000004619, -1.336933437520057563E-15, -19.00000000000000000 ) ) ;
#38410=LINE ( 'NONE', #27450, #44682 ) ;
#38414=LINE ( 'NONE', #16148, #65564 ) ;
#38415=VECTOR ( 'NONE', #55323, 1000.000000000000000 ) ;
#38431=LINE ( 'NONE', #11196, #25498 ) ;
#38433=ORIENTED_EDGE ( 'NONE', *, *, #34639, .F. ) ;
#38454=CARTESIAN_POINT ( 'NONE',  ( -8.250000000000001776, -8.249999999999998224, -26.00000000000001066 ) ) ;
#38457=DIRECTION ( 'NONE',  ( -1.000000000000000000, 0.000000000000000000, 0.000000000000000000 ) ) ;
#38460=ORIENTED_EDGE ( 'NONE', *, *, #23954, .F. ) ;
#38464=VECTOR ( 'NONE', #62754, 1000.000000000000000 ) ;
#38466=DIRECTION ( 'NONE',  ( -1.000000000000000000, 0.000000000000000000, 0.000000000000000000 ) ) ;
#38467=AXIS2_PLACEMENT_3D ( 'NONE', #55577, #16725, #55236 ) ;
#38468=ORIENTED_EDGE ( 'NONE', *, *, #37544, .T. ) ;
#38471=ORIENTED_EDGE ( 'NONE', *, *, #4771, .F. ) ;
#38473=FACE_OUTER_BOUND ( 'NONE', #43154, .T. ) ;
#38474=VECTOR ( 'NONE', #52387, 1000.000000000000000 ) ;
#38482=LINE ( 'NONE', #23241, #4547 ) ;
#38495=ORIENTED_EDGE ( 'NONE', *, *, #11335, .F. ) ;
#38500=ADVANCED_FACE ( 'NONE', ( #7390, #28968 ), #59937, .T. ) ;
#38506=CARTESIAN_POINT ( 'NONE',  ( -8.250000000000001776, 0.000000000000000000, -7.500000000000000000 ) ) ;
#38515=ORIENTED_EDGE ( 'NONE', *, *, #27131, .F. ) ;
#38516=ORIENTED_EDGE ( 'NONE', *, *, #46961, .F. ) ;
#38518=ORIENTED_EDGE ( 'NONE', *, *, #29936, .F. ) ;
#38527=DIRECTION ( 'NONE',  ( 0.000000000000000000, 1.000000000000000000, 0.000000000000000000 ) ) ;
#38536=EDGE_CURVE ( 'NONE', #52304, #69570, #60799, .T. ) ;
#38542=LINE ( 'NONE', #16272, #22206 ) ;
#38559=FACE_OUTER_BOUND ( 'NONE', #2603, .T. ) ;
#38562=VECTOR ( 'NONE', #50424, 1000.000000000000000 ) ;
#38565=VERTEX_POINT ( 'NONE', #42983 ) ;
#38574=AXIS2_PLACEMENT_3D ( 'NONE', #25533, #51337, #57346 ) ;
#38576=LINE ( 'NONE', #60127, #2656 ) ;
#38583=CARTESIAN_POINT ( 'NONE',  ( 8.250000000000005329, 7.250000000000000888, -26.00000000000001066 ) ) ;
#38584=EDGE_CURVE ( 'NONE', #11628, #35155, #14813, .T. ) ;
#38589=ORIENTED_EDGE ( 'NONE', *, *, #49293, .T. ) ;
#38604=CARTESIAN_POINT ( 'NONE',  ( 8.250000000000005329, -7.249999999999998224, -17.00000000000000000 ) ) ;
#38606=PLANE ( 'NONE',  #63604 ) ;
#38607=CARTESIAN_POINT ( 'NONE',  ( 7.250000000000005329, 7.250000000000000888, -26.00000000000001066 ) ) ;
#38608=DIRECTION ( 'NONE',  ( -1.000000000000000000, 2.602085213965213008E-15, 0.000000000000000000 ) ) ;
#38612=VERTEX_POINT ( 'NONE', #37686 ) ;
#38631=ORIENTED_EDGE ( 'NONE', *, *, #11639, .F. ) ;
#38632=CARTESIAN_POINT ( 'NONE',  ( 4.456444791733522252E-16, 7.450000000000002842, -8.500000000000000000 ) ) ;
#38633=DIRECTION ( 'NONE',  ( 0.000000000000000000, 0.000000000000000000, -1.000000000000000000 ) ) ;
#38635=LINE ( 'NONE', #60186, #55071 ) ;
#38641=CARTESIAN_POINT ( 'NONE',  ( 9.750000000000001776, -9.690000000000001279, -5.000000000000000000 ) ) ;
#38645=AXIS2_PLACEMENT_3D ( 'NONE', #56201, #2450, #9512 ) ;
#38653=CARTESIAN_POINT ( 'NONE',  ( 7.450000000000003730, -7.249999999999997335, -21.00000000000000000 ) ) ;
#38656=DIRECTION ( 'NONE',  ( 0.000000000000000000, 1.000000000000000000, 0.000000000000000000 ) ) ;
#38657=ORIENTED_EDGE ( 'NONE', *, *, #13898, .T. ) ;
#38658=AXIS2_PLACEMENT_3D ( 'NONE', #63476, #63121, #68780 ) ;
#38666=CYLINDRICAL_SURFACE ( 'NONE', #2268, 0.1999999999999987899 ) ;
#38668=EDGE_LOOP ( 'NONE', ( #20792, #20428, #49470, #10592 ) ) ;
#38680=CARTESIAN_POINT ( 'NONE',  ( 7.250000000000005329, -8.249999999999998224, -21.00000000000000000 ) ) ;
#38692=CARTESIAN_POINT ( 'NONE',  ( 7.450000000000003730, -7.249999999999997335, -13.50000000000000178 ) ) ;
#38699=ORIENTED_EDGE ( 'NONE', *, *, #66486, .F. ) ;
#38701=EDGE_CURVE ( 'NONE', #54414, #22866, #65596, .T. ) ;
#38711=ORIENTED_EDGE ( 'NONE', *, *, #44824, .T. ) ;
#38717=ORIENTED_EDGE ( 'NONE', *, *, #33935, .T. ) ;
#38722=DIRECTION ( 'NONE',  ( -0.000000000000000000, -0.000000000000000000, -1.000000000000000000 ) ) ;
#38735=CARTESIAN_POINT ( 'NONE',  ( -7.250000000000001776, -7.249999999999998224, -9.000000000000001776 ) ) ;
#38736=EDGE_CURVE ( 'NONE', #60538, #58562, #61671, .T. ) ;
#38738=AXIS2_PLACEMENT_3D ( 'NONE', #57215, #30701, #8411 ) ;
#38742=DIRECTION ( 'NONE',  ( -0.000000000000000000, -0.000000000000000000, -1.000000000000000000 ) ) ;
#38744=ADVANCED_FACE ( 'NONE', ( #44702 ), #40089, .T. ) ;
#38745=DIRECTION ( 'NONE',  ( 0.000000000000000000, 0.000000000000000000, -1.000000000000000000 ) ) ;
#38760=DIRECTION ( 'NONE',  ( 0.000000000000000000, 0.000000000000000000, 1.000000000000000000 ) ) ;
#38776=CARTESIAN_POINT ( 'NONE',  ( -7.450000000000001954, -7.249999999999998224, -11.50000000000000000 ) ) ;
#38781=ORIENTED_EDGE ( 'NONE', *, *, #30352, .T. ) ;
#38786=CARTESIAN_POINT ( 'NONE',  ( -7.250000000000000888, 7.450000000000003730, -17.50000000000000000 ) ) ;
#38787=ORIENTED_EDGE ( 'NONE', *, *, #57738, .F. ) ;
#38791=CARTESIAN_POINT ( 'NONE',  ( -7.250000000000001776, -7.249999999999998224, -8.000000000000000000 ) ) ;
#38792=EDGE_CURVE ( 'NONE', #50861, #35627, #69853, .T. ) ;
#38797=EDGE_CURVE ( 'NONE', #32155, #31478, #24674, .T. ) ;
#38803=CARTESIAN_POINT ( 'NONE',  ( 4.456444791733522252E-16, 7.450000000000002842, -10.50000000000000000 ) ) ;
#38810=CARTESIAN_POINT ( 'NONE',  ( 7.250000000000005329, 7.250000000000000888, -18.00000000000000000 ) ) ;
#38811=EDGE_LOOP ( 'NONE', ( #47240, #35077, #22101, #55396 ) ) ;
#38812=CARTESIAN_POINT ( 'NONE',  ( 4.456444791733522252E-16, 7.450000000000002842, -21.50000000000000000 ) ) ;
#38828=EDGE_CURVE ( 'NONE', #6379, #4689, #63436, .T. ) ;
#38830=EDGE_CURVE ( 'NONE', #16718, #68045, #56720, .T. ) ;
#38853=DIRECTION ( 'NONE',  ( 0.000000000000000000, -1.000000000000000000, 0.000000000000000000 ) ) ;
#38854=DIRECTION ( 'NONE',  ( 0.000000000000000000, 0.000000000000000000, -1.000000000000000000 ) ) ;
#38874=DIRECTION ( 'NONE',  ( -0.000000000000000000, -0.000000000000000000, 1.000000000000000000 ) ) ;
#38875=ORIENTED_EDGE ( 'NONE', *, *, #26487, .T. ) ;
#38878=EDGE_CURVE ( 'NONE', #34893, #18134, #56312, .T. ) ;
#38879=CARTESIAN_POINT ( 'NONE',  ( -7.250000000000000888, 7.450000000000003730, -16.50000000000000000 ) ) ;
#38880=ORIENTED_EDGE ( 'NONE', *, *, #20540, .T. ) ;
#38884=CIRCLE ( 'NONE', #49088, 2.500000000000000000 ) ;
#38885=CYLINDRICAL_SURFACE ( 'NONE', #40855, 1.000000000000000000 ) ;
#38892=CIRCLE ( 'NONE', #44529, 1.000000000000000000 ) ;
#38898=CARTESIAN_POINT ( 'NONE',  ( -8.250000000000001776, -8.249999999999998224, -26.00000000000001066 ) ) ;
#38901=EDGE_CURVE ( 'NONE', #66616, #24826, #5553, .T. ) ;
#38919=DIRECTION ( 'NONE',  ( 0.000000000000000000, 0.000000000000000000, -1.000000000000000000 ) ) ;
#38929=LINE ( 'NONE', #1112, #55254 ) ;
#38932=ORIENTED_EDGE ( 'NONE', *, *, #62257, .F. ) ;
#38936=ORIENTED_EDGE ( 'NONE', *, *, #53804, .F. ) ;
#38939=DIRECTION ( 'NONE',  ( -1.000000000000000000, 0.000000000000000000, 0.000000000000000000 ) ) ;
#38943=VERTEX_POINT ( 'NONE', #11083 ) ;
#38950=EDGE_CURVE ( 'NONE', #38612, #66827, #20229, .T. ) ;
#38951=VECTOR ( 'NONE', #65441, 1000.000000000000000 ) ;
#38955=ORIENTED_EDGE ( 'NONE', *, *, #41301, .T. ) ;
#38957=AXIS2_PLACEMENT_3D ( 'NONE', #60769, #12312, #28589 ) ;
#38968=CARTESIAN_POINT ( 'NONE',  ( -7.450000000000001954, 7.250000000000000000, -8.000000000000000000 ) ) ;
#38974=AXIS2_PLACEMENT_3D ( 'NONE', #40380, #61225, #40009 ) ;
#38979=CARTESIAN_POINT ( 'NONE',  ( 0.000000000000000000, 8.250000000000001776, -9.500000000000001776 ) ) ;
#38981=PLANE ( 'NONE',  #50810 ) ;
#38984=CARTESIAN_POINT ( 'NONE',  ( 7.250000000000005329, -8.249999999999998224, -19.00000000000000000 ) ) ;
#39001=VERTEX_POINT ( 'NONE', #65190 ) ;
#39010=VERTEX_POINT ( 'NONE', #31959 ) ;
#39013=VECTOR ( 'NONE', #14799, 1000.000000000000000 ) ;
#39017=CARTESIAN_POINT ( 'NONE',  ( 4.456444791733522252E-16, 7.450000000000002842, -20.50000000000000000 ) ) ;
#39018=VERTEX_POINT ( 'NONE', #38309 ) ;
#39020=CARTESIAN_POINT ( 'NONE',  ( -7.450000000000001954, 7.250000000000000000, -16.50000000000000000 ) ) ;
#39030=ORIENTED_EDGE ( 'NONE', *, *, #424, .T. ) ;
#39039=CARTESIAN_POINT ( 'NONE',  ( 4.456444791733522252E-16, 7.450000000000002842, -13.00000000000000178 ) ) ;
#39042=ORIENTED_EDGE ( 'NONE', *, *, #26238, .T. ) ;
#39053=VECTOR ( 'NONE', #42302, 1000.000000000000000 ) ;
#39057=DIRECTION ( 'NONE',  ( 0.000000000000000000, 0.000000000000000000, -1.000000000000000000 ) ) ;
#39058=ORIENTED_EDGE ( 'NONE', *, *, #62759, .F. ) ;
#39064=PLANE ( 'NONE',  #18009 ) ;
#39065=VECTOR ( 'NONE', #34511, 1000.000000000000000 ) ;
#39068=AXIS2_PLACEMENT_3D ( 'NONE', #2211, #67267, #7851 ) ;
#39080=FACE_OUTER_BOUND ( 'NONE', #36447, .T. ) ;
#39087=EDGE_CURVE ( 'NONE', #66435, #31212, #45315, .T. ) ;
#39088=DIRECTION ( 'NONE',  ( -0.000000000000000000, -0.000000000000000000, 1.000000000000000000 ) ) ;
#39089=FACE_OUTER_BOUND ( 'NONE', #32308, .T. ) ;
#39094=DIRECTION ( 'NONE',  ( -0.000000000000000000, 0.000000000000000000, -1.000000000000000000 ) ) ;
#39106=ORIENTED_EDGE ( 'NONE', *, *, #23696, .F. ) ;
#39109=CARTESIAN_POINT ( 'NONE',  ( 7.250000000000005329, -7.449999999999998401, -17.50000000000000000 ) ) ;
#39110=ORIENTED_EDGE ( 'NONE', *, *, #50529, .F. ) ;
#39113=ORIENTED_EDGE ( 'NONE', *, *, #67316, .F. ) ;
#39115=LINE ( 'NONE', #7627, #38562 ) ;
#39119=AXIS2_PLACEMENT_3D ( 'NONE', #8967, #62709, #25242 ) ;
#39122=PLANE ( 'NONE',  #41434 ) ;
#39123=DIRECTION ( 'NONE',  ( -1.000000000000000000, 0.000000000000000000, 0.000000000000000000 ) ) ;
#39124=VERTEX_POINT ( 'NONE', #55942 ) ;
#39129=DIRECTION ( 'NONE',  ( 0.000000000000000000, 0.000000000000000000, -1.000000000000000000 ) ) ;
#39131=EDGE_CURVE ( 'NONE', #39415, #69380, #7493, .T. ) ;
#39137=ORIENTED_EDGE ( 'NONE', *, *, #22950, .T. ) ;
#39141=CARTESIAN_POINT ( 'NONE',  ( 8.250000000000005329, -8.249999999999998224, -26.00000000000001066 ) ) ;
#39147=EDGE_CURVE ( 'NONE', #20587, #68282, #27688, .T. ) ;
#39148=VECTOR ( 'NONE', #13608, 1000.000000000000000 ) ;
#39154=ORIENTED_EDGE ( 'NONE', *, *, #29278, .T. ) ;
#39155=DIRECTION ( 'NONE',  ( -0.000000000000000000, 0.000000000000000000, 1.000000000000000000 ) ) ;
#39161=CIRCLE ( 'NONE', #38080, 1.000000000000000000 ) ;
#39174=LINE ( 'NONE', #28899, #51261 ) ;
#39177=DIRECTION ( 'NONE',  ( 0.000000000000000000, 0.000000000000000000, 1.000000000000000000 ) ) ;
#39183=CARTESIAN_POINT ( 'NONE',  ( 7.250000000000005329, -8.249999999999998224, -16.00000000000000000 ) ) ;
#39184=ORIENTED_EDGE ( 'NONE', *, *, #51053, .F. ) ;
#39195=ORIENTED_EDGE ( 'NONE', *, *, #38701, .T. ) ;
#39201=DIRECTION ( 'NONE',  ( -1.000000000000000000, 0.000000000000000000, 0.000000000000000000 ) ) ;
#39209=DIRECTION ( 'NONE',  ( -1.000000000000000000, 0.000000000000000000, 0.000000000000000000 ) ) ;
#39212=ORIENTED_EDGE ( 'NONE', *, *, #44876, .T. ) ;
#39217=DIRECTION ( 'NONE',  ( -1.000000000000000000, 0.000000000000000000, 0.000000000000000000 ) ) ;
#39229=EDGE_CURVE ( 'NONE', #47719, #11735, #1851, .T. ) ;
#39230=DIRECTION ( 'NONE',  ( 0.000000000000000000, -0.000000000000000000, 1.000000000000000000 ) ) ;
#39237=LINE ( 'NONE', #65089, #65273 ) ;
#39238=LINE ( 'NONE', #39573, #23894 ) ;
#39243=CARTESIAN_POINT ( 'NONE',  ( -8.250000000000001776, -7.249999999999998224, -16.50000000000000000 ) ) ;
#39249=CIRCLE ( 'NONE', #44901, 0.8100000000000017186 ) ;
#39260=EDGE_CURVE ( 'NONE', #17912, #24963, #50636, .T. ) ;
#39276=DIRECTION ( 'NONE',  ( 1.000000000000000000, -5.981805089575196197E-17, 0.000000000000000000 ) ) ;
#39284=CARTESIAN_POINT ( 'NONE',  ( -8.250000000000001776, -7.249999999999998224, -8.000000000000000000 ) ) ;
#39292=CARTESIAN_POINT ( 'NONE',  ( -8.250000000000000000, 7.250000000000001776, -20.00000000000000000 ) ) ;
#39295=ORIENTED_EDGE ( 'NONE', *, *, #14197, .T. ) ;
#39307=EDGE_CURVE ( 'NONE', #57216, #31517, #38316, .T. ) ;
#39316=CARTESIAN_POINT ( 'NONE',  ( -7.250000000000000888, 7.250000000000001776, -7.500000000000000000 ) ) ;
#39319=CIRCLE ( 'NONE', #33665, 0.2000000000000005107 ) ;
#39325=CARTESIAN_POINT ( 'NONE',  ( -7.250000000000000888, 8.250000000000001776, -25.00000000000000000 ) ) ;
#39333=ORIENTED_EDGE ( 'NONE', *, *, #2982, .T. ) ;
#39342=DIRECTION ( 'NONE',  ( -0.000000000000000000, -0.000000000000000000, 1.000000000000000000 ) ) ;
#39343=CIRCLE ( 'NONE', #8865, 0.2000000000000005107 ) ;
#39345=LINE ( 'NONE', #66903, #54532 ) ;
#39357=CARTESIAN_POINT ( 'NONE',  ( -7.750000000000001776, 7.750000000000001776, 5.000000000000000000 ) ) ;
#39362=ORIENTED_EDGE ( 'NONE', *, *, #57617, .F. ) ;
#39366=FACE_OUTER_BOUND ( 'NONE', #2587, .T. ) ;
#39380=VERTEX_POINT ( 'NONE', #43166 ) ;
#39383=ORIENTED_EDGE ( 'NONE', *, *, #10820, .T. ) ;
#39385=AXIS2_PLACEMENT_3D ( 'NONE', #27395, #5833, #5133 ) ;
#39386=VERTEX_POINT ( 'NONE', #36471 ) ;
#39395=DIRECTION ( 'NONE',  ( -0.000000000000000000, -0.000000000000000000, 1.000000000000000000 ) ) ;
#39400=FACE_OUTER_BOUND ( 'NONE', #57361, .T. ) ;
#39403=CARTESIAN_POINT ( 'NONE',  ( 8.250000000000005329, -8.249999999999998224, -26.00000000000001066 ) ) ;
#39404=ORIENTED_EDGE ( 'NONE', *, *, #66438, .F. ) ;
#39408=LINE ( 'NONE', #60967, #18506 ) ;
#39411=CARTESIAN_POINT ( 'NONE',  ( 8.250000000000005329, 8.250000000000001776, -26.00000000000001066 ) ) ;
#39415=VERTEX_POINT ( 'NONE', #53104 ) ;
#39419=DIRECTION ( 'NONE',  ( 0.000000000000000000, 0.000000000000000000, -1.000000000000000000 ) ) ;
#39427=DIRECTION ( 'NONE',  ( -1.000000000000000000, 0.000000000000000000, 0.000000000000000000 ) ) ;
#39428=ORIENTED_EDGE ( 'NONE', *, *, #34988, .F. ) ;
#39430=CARTESIAN_POINT ( 'NONE',  ( -7.250000000000000888, -8.249999999999998224, -26.00000000000001066 ) ) ;
#39434=VECTOR ( 'NONE', #39717, 1000.000000000000000 ) ;
#39436=EDGE_CURVE ( 'NONE', #25188, #1043, #63706, .T. ) ;
#39438=EDGE_CURVE ( 'NONE', #28744, #10507, #48837, .T. ) ;
#39439=ORIENTED_EDGE ( 'NONE', *, *, #34542, .T. ) ;
#39444=CARTESIAN_POINT ( 'NONE',  ( -7.450000000000001954, -7.249999999999998224, -19.00000000000000000 ) ) ;
#39466=ORIENTED_EDGE ( 'NONE', *, *, #69655, .T. ) ;
#39467=DIRECTION ( 'NONE',  ( 1.000000000000000000, -0.000000000000000000, 0.000000000000000000 ) ) ;
#39468=CARTESIAN_POINT ( 'NONE',  ( -6.500000000000002665, -6.500000000000002665, -1.000000000000000000 ) ) ;
#39482=CIRCLE ( 'NONE', #9012, 0.1999999999999996503 ) ;
#39484=DIRECTION ( 'NONE',  ( 0.000000000000000000, 0.000000000000000000, 1.000000000000000000 ) ) ;
#39486=ORIENTED_EDGE ( 'NONE', *, *, #5785, .T. ) ;
#39487=EDGE_LOOP ( 'NONE', ( #26883, #67317, #17830, #17831, #51459, #19129, #20482, #43296 ) ) ;
#39494=DIRECTION ( 'NONE',  ( -1.000000000000000000, 0.000000000000000000, 0.000000000000000000 ) ) ;
#39501=LINE ( 'NONE', #1670, #45758 ) ;
#39502=CARTESIAN_POINT ( 'NONE',  ( 7.250000000000004441, 7.450000000000001954, -18.50000000000000000 ) ) ;
#39517=LINE ( 'NONE', #61078, #260 ) ;
#39523=CARTESIAN_POINT ( 'NONE',  ( -7.250000000000000888, 7.250000000000001776, -30.00000000000001066 ) ) ;
#39524=PLANE ( 'NONE',  #52500 ) ;
#39530=ADVANCED_FACE ( 'NONE', ( #49176 ), #16997, .T. ) ;
#39531=ORIENTED_EDGE ( 'NONE', *, *, #49004, .F. ) ;
#39536=DIRECTION ( 'NONE',  ( 0.000000000000000000, 0.000000000000000000, -1.000000000000000000 ) ) ;
#39538=CARTESIAN_POINT ( 'NONE',  ( 7.250000000000005329, -7.249999999999998224, -22.50000000000000000 ) ) ;
#39550=CARTESIAN_POINT ( 'NONE',  ( 8.250000000000005329, -8.249999999999998224, -26.00000000000001066 ) ) ;
#39551=CARTESIAN_POINT ( 'NONE',  ( 7.250000000000005329, 8.250000000000001776, -17.00000000000000000 ) ) ;
#39552=ORIENTED_EDGE ( 'NONE', *, *, #24203, .T. ) ;
#39553=VERTEX_POINT ( 'NONE', #22982 ) ;
#39560=LINE ( 'NONE', #59760, #10514 ) ;
#39573=CARTESIAN_POINT ( 'NONE',  ( 8.250000000000005329, 0.000000000000000000, -20.50000000000000000 ) ) ;
#39578=EDGE_LOOP ( 'NONE', ( #34745, #45059, #39113, #64282 ) ) ;
#39580=DIRECTION ( 'NONE',  ( 0.000000000000000000, -0.000000000000000000, 1.000000000000000000 ) ) ;
#39581=AXIS2_PLACEMENT_3D ( 'NONE', #29142, #45748, #60961 ) ;
#39586=CARTESIAN_POINT ( 'NONE',  ( 10.50000000000000000, -9.690000000000001279, 0.000000000000000000 ) ) ;
#39596=CARTESIAN_POINT ( 'NONE',  ( -7.250000000000000888, 7.250000000000001776, -25.50000000000000355 ) ) ;
#39602=ORIENTED_EDGE ( 'NONE', *, *, #53871, .F. ) ;
#39606=ADVANCED_FACE ( 'NONE', ( #65438 ), #28982, .T. ) ;
#39610=ADVANCED_FACE ( 'NONE', ( #1087 ), #54830, .F. ) ;
#39613=DIRECTION ( 'NONE',  ( 0.000000000000000000, -0.000000000000000000, 1.000000000000000000 ) ) ;
#39625=CARTESIAN_POINT ( 'NONE',  ( 8.250000000000005329, 8.250000000000001776, -26.00000000000001066 ) ) ;
#39633=AXIS2_PLACEMENT_3D ( 'NONE', #828, #60188, #33330 ) ;
#39635=EDGE_CURVE ( 'NONE', #29071, #5578, #12352, .T. ) ;
#39648=EDGE_LOOP ( 'NONE', ( #31076, #7430, #25865, #33366 ) ) ;
#39650=VECTOR ( 'NONE', #45938, 1000.000000000000000 ) ;
#39659=CARTESIAN_POINT ( 'NONE',  ( 7.250000000000005329, -7.449999999999998401, -9.500000000000001776 ) ) ;
#39660=CARTESIAN_POINT ( 'NONE',  ( 0.000000000000000000, 8.250000000000001776, -12.00000000000000000 ) ) ;
#39661=DIRECTION ( 'NONE',  ( 0.000000000000000000, 0.000000000000000000, 1.000000000000000000 ) ) ;
#39664=ORIENTED_EDGE ( 'NONE', *, *, #44412, .T. ) ;
#39676=EDGE_CURVE ( 'NONE', #39553, #127, #41728, .T. ) ;
#39682=VECTOR ( 'NONE', #8529, 1000.000000000000000 ) ;
#39683=CARTESIAN_POINT ( 'NONE',  ( 7.450000000000004619, -1.336933437520057563E-15, -23.50000000000000000 ) ) ;
#39689=DIRECTION ( 'NONE',  ( 0.000000000000000000, -0.000000000000000000, 1.000000000000000000 ) ) ;
#39693=CARTESIAN_POINT ( 'NONE',  ( 7.250000000000005329, -7.449999999999998401, -18.00000000000000000 ) ) ;
#39694=CARTESIAN_POINT ( 'NONE',  ( 7.250000000000005329, 8.250000000000001776, -8.000000000000000000 ) ) ;
#39701=ORIENTED_EDGE ( 'NONE', *, *, #25345, .T. ) ;
#39705=CARTESIAN_POINT ( 'NONE',  ( 7.250000000000005329, -8.249999999999998224, -24.00000000000000000 ) ) ;
#39706=CARTESIAN_POINT ( 'NONE',  ( 7.250000000000004441, 7.450000000000001954, -21.50000000000000000 ) ) ;
#39717=DIRECTION ( 'NONE',  ( -1.000000000000000000, 0.000000000000000000, 0.000000000000000000 ) ) ;
#39723=VERTEX_POINT ( 'NONE', #57254 ) ;
#39727=ORIENTED_EDGE ( 'NONE', *, *, #43594, .F. ) ;
#39733=CARTESIAN_POINT ( 'NONE',  ( 8.250000000000005329, 7.250000000000000888, -20.00000000000000000 ) ) ;
#39741=LINE ( 'NONE', #18178, #50891 ) ;
#39749=AXIS2_PLACEMENT_3D ( 'NONE', #20493, #11265, #26160 ) ;
#39757=EDGE_CURVE ( 'NONE', #4958, #58882, #54055, .T. ) ;
#39765=CARTESIAN_POINT ( 'NONE',  ( -7.250000000000000888, 7.250000000000001776, -9.500000000000001776 ) ) ;
#39767=DIRECTION ( 'NONE',  ( -1.000000000000000000, 0.000000000000000000, 0.000000000000000000 ) ) ;
#39774=DIRECTION ( 'NONE',  ( 0.000000000000000000, 0.000000000000000000, -1.000000000000000000 ) ) ;
#39783=DIRECTION ( 'NONE',  ( 1.000000000000000000, 0.000000000000000000, 0.000000000000000000 ) ) ;
#39786=ORIENTED_EDGE ( 'NONE', *, *, #25751, .F. ) ;
#39792=LINE ( 'NONE', #7969, #14565 ) ;
#39793=DIRECTION ( 'NONE',  ( 0.000000000000000000, 0.000000000000000000, 1.000000000000000000 ) ) ;
#39795=ORIENTED_EDGE ( 'NONE', *, *, #10390, .F. ) ;
#39800=ORIENTED_EDGE ( 'NONE', *, *, #43926, .T. ) ;
#39804=CARTESIAN_POINT ( 'NONE',  ( 8.250000000000005329, -8.249999999999998224, -26.00000000000001066 ) ) ;
#39811=LINE ( 'NONE', #61377, #30651 ) ;
#39818=DIRECTION ( 'NONE',  ( -0.000000000000000000, -0.000000000000000000, -1.000000000000000000 ) ) ;
#39829=FACE_OUTER_BOUND ( 'NONE', #9235, .T. ) ;
#39832=DIRECTION ( 'NONE',  ( -1.000000000000000000, 0.000000000000000000, 0.000000000000000000 ) ) ;
#39833=ORIENTED_EDGE ( 'NONE', *, *, #63724, .F. ) ;
#39837=DIRECTION ( 'NONE',  ( 0.000000000000000000, 0.000000000000000000, 1.000000000000000000 ) ) ;
#39838=AXIS2_PLACEMENT_3D ( 'NONE', #16339, #31917, #64105 ) ;
#39843=CIRCLE ( 'NONE', #10501, 0.9999999999999991118 ) ;
#39852=LINE ( 'NONE', #60740, #49959 ) ;
#39857=ADVANCED_FACE ( 'NONE', ( #9882 ), #42385, .F. ) ;
#39861=ORIENTED_EDGE ( 'NONE', *, *, #26288, .T. ) ;
#39863=CYLINDRICAL_SURFACE ( 'NONE', #16755, 1.500000000000001332 ) ;
#39866=FACE_OUTER_BOUND ( 'NONE', #29219, .T. ) ;
#39867=LINE ( 'NONE', #13362, #61601 ) ;
#39872=ORIENTED_EDGE ( 'NONE', *, *, #3537, .F. ) ;
#39875=DIRECTION ( 'NONE',  ( 0.000000000000000000, 0.000000000000000000, 1.000000000000000000 ) ) ;
#39876=LINE ( 'NONE', #55133, #43408 ) ;
#39877=VERTEX_POINT ( 'NONE', #32490 ) ;
#39879=FACE_OUTER_BOUND ( 'NONE', #24877, .T. ) ;
#39882=ORIENTED_EDGE ( 'NONE', *, *, #38098, .T. ) ;
#39891=VECTOR ( 'NONE', #35721, 1000.000000000000000 ) ;
#39892=DIRECTION ( 'NONE',  ( 0.000000000000000000, 0.000000000000000000, -1.000000000000000000 ) ) ;
#39904=EDGE_CURVE ( 'NONE', #18999, #4958, #53115, .T. ) ;
#39914=EDGE_LOOP ( 'NONE', ( #21181, #47686, #64204, #11891 ) ) ;
#39915=LINE ( 'NONE', #62190, #39650 ) ;
#39916=CARTESIAN_POINT ( 'NONE',  ( -7.450000000000001954, -7.249999999999998224, -8.500000000000000000 ) ) ;
#39917=DIRECTION ( 'NONE',  ( -1.000000000000000000, 0.000000000000000000, 0.000000000000000000 ) ) ;
#39933=DIRECTION ( 'NONE',  ( 0.000000000000000000, 1.000000000000000000, 0.000000000000000000 ) ) ;
#39943=EDGE_CURVE ( 'NONE', #11295, #7880, #38482, .T. ) ;
#39953=LINE ( 'NONE', #55884, #35149 ) ;
#39972=CARTESIAN_POINT ( 'NONE',  ( -7.250000000000000888, 7.250000000000001776, -20.50000000000000000 ) ) ;
#39973=ORIENTED_EDGE ( 'NONE', *, *, #32068, .F. ) ;
#39988=DIRECTION ( 'NONE',  ( 0.000000000000000000, 0.000000000000000000, -1.000000000000000000 ) ) ;
#39989=CARTESIAN_POINT ( 'NONE',  ( -7.450000000000001954, -7.249999999999998224, -17.50000000000000000 ) ) ;
#39996=CIRCLE ( 'NONE', #69358, 0.7499999999999997780 ) ;
#39999=CARTESIAN_POINT ( 'NONE',  ( -7.250000000000001776, -7.249999999999998224, -22.50000000000000000 ) ) ;
#40000=CARTESIAN_POINT ( 'NONE',  ( -7.250000000000000888, 8.250000000000001776, -22.00000000000000000 ) ) ;
#40004=EDGE_CURVE ( 'NONE', #66058, #36929, #12615, .T. ) ;
#40006=EDGE_LOOP ( 'NONE', ( #59576, #47827, #69189, #42897 ) ) ;
#40009=DIRECTION ( 'NONE',  ( 1.000000000000000000, 0.000000000000000000, 0.000000000000000000 ) ) ;
#40010=ORIENTED_EDGE ( 'NONE', *, *, #47280, .F. ) ;
#40013=FACE_OUTER_BOUND ( 'NONE', #12838, .T. ) ;
#40014=CIRCLE ( 'NONE', #14090, 1.000000000000000000 ) ;
#40019=DIRECTION ( 'NONE',  ( 1.000000000000000000, 0.000000000000000000, 0.000000000000000000 ) ) ;
#40028=CARTESIAN_POINT ( 'NONE',  ( -7.250000000000000888, 7.250000000000001776, -17.50000000000000000 ) ) ;
#40029=VERTEX_POINT ( 'NONE', #40546 ) ;
#40032=CARTESIAN_POINT ( 'NONE',  ( 7.450000000000004619, -1.336933437520057563E-15, -11.50000000000000000 ) ) ;
#40039=AXIS2_PLACEMENT_3D ( 'NONE', #54495, #64409, #26570 ) ;
#40040=AXIS2_PLACEMENT_3D ( 'NONE', #67832, #51922, #4193 ) ;
#40041=FACE_OUTER_BOUND ( 'NONE', #53259, .T. ) ;
#40049=ORIENTED_EDGE ( 'NONE', *, *, #59543, .T. ) ;
#40055=CARTESIAN_POINT ( 'NONE',  ( -9.690000000000001279, -9.750000000000001776, -5.000000000000000000 ) ) ;
#40057=CARTESIAN_POINT ( 'NONE',  ( 7.250000000000005329, -7.249999999999998224, -8.000000000000000000 ) ) ;
#40062=ADVANCED_FACE ( 'NONE', ( #7314 ), #18626, .T. ) ;
#40063=ORIENTED_EDGE ( 'NONE', *, *, #6976, .T. ) ;
#40067=VERTEX_POINT ( 'NONE', #29229 ) ;
#40068=ADVANCED_FACE ( 'NONE', ( #29940, #7669 ), #8363, .F. ) ;
#40073=ORIENTED_EDGE ( 'NONE', *, *, #1758, .T. ) ;
#40084=DIRECTION ( 'NONE',  ( -1.000000000000000000, 0.000000000000000000, 0.000000000000000000 ) ) ;
#40089=CYLINDRICAL_SURFACE ( 'NONE', #33698, 1.000000000000000000 ) ;
#40098=DIRECTION ( 'NONE',  ( 0.000000000000000000, 0.000000000000000000, -1.000000000000000000 ) ) ;
#40101=PLANE ( 'NONE',  #48902 ) ;
#40103=EDGE_CURVE ( 'NONE', #47005, #35485, #24994, .T. ) ;
#40114=AXIS2_PLACEMENT_3D ( 'NONE', #51699, #57340, #3602 ) ;
#40115=CARTESIAN_POINT ( 'NONE',  ( 7.250000000000005329, 7.250000000000000888, -18.50000000000000000 ) ) ;
#40124=VERTEX_POINT ( 'NONE', #18986 ) ;
#40125=LINE ( 'NONE', #30245, #22802 ) ;
#40127=ADVANCED_FACE ( 'NONE', ( #61401 ), #2375, .F. ) ;
#40136=EDGE_LOOP ( 'NONE', ( #67795, #68916, #42352, #30345 ) ) ;
#40140=EDGE_CURVE ( 'NONE', #64382, #40458, #64357, .T. ) ;
#40146=VECTOR ( 'NONE', #4719, 1000.000000000000000 ) ;
#40154=VECTOR ( 'NONE', #46455, 1000.000000000000000 ) ;
#40162=AXIS2_PLACEMENT_3D ( 'NONE', #27837, #624, #49418 ) ;
#40171=AXIS2_PLACEMENT_3D ( 'NONE', #51958, #19422, #46641 ) ;
#40179=DIRECTION ( 'NONE',  ( 0.000000000000000000, 0.000000000000000000, 1.000000000000000000 ) ) ;
#40181=DIRECTION ( 'NONE',  ( -1.794541526872559352E-16, -1.000000000000000000, 0.000000000000000000 ) ) ;
#40185=DIRECTION ( 'NONE',  ( 1.000000000000000000, 0.000000000000000000, 0.000000000000000000 ) ) ;
#40188=CARTESIAN_POINT ( 'NONE',  ( 7.250000000000005329, 7.250000000000000888, -13.50000000000000178 ) ) ;
#40191=ORIENTED_EDGE ( 'NONE', *, *, #60026, .T. ) ;
#40198=VECTOR ( 'NONE', #61119, 1000.000000000000000 ) ;
#40203=AXIS2_PLACEMENT_3D ( 'NONE', #36340, #63214, #69220 ) ;
#40205=EDGE_LOOP ( 'NONE', ( #1626, #15678, #41264, #36615 ) ) ;
#40207=LINE ( 'NONE', #56474, #18036 ) ;
#40209=CARTESIAN_POINT ( 'NONE',  ( 7.450000000000006395, 7.250000000000000888, -15.50000000000000000 ) ) ;
#40222=EDGE_CURVE ( 'NONE', #66435, #54499, #25712, .T. ) ;
#40236=DIRECTION ( 'NONE',  ( 1.000000000000000000, 0.000000000000000000, 0.000000000000000000 ) ) ;
#40257=LINE ( 'NONE', #14453, #47249 ) ;
#40258=CARTESIAN_POINT ( 'NONE',  ( 7.250000000000005329, 7.250000000000000888, -26.00000000000001066 ) ) ;
#40259=ORIENTED_EDGE ( 'NONE', *, *, #2247, .F. ) ;
#40262=CIRCLE ( 'NONE', #10904, 1.000000000000003553 ) ;
#40276=CARTESIAN_POINT ( 'NONE',  ( -7.250000000000001776, -7.249999999999998224, -14.50000000000000000 ) ) ;
#40281=DIRECTION ( 'NONE',  ( -0.000000000000000000, -0.000000000000000000, 1.000000000000000000 ) ) ;
#40283=CARTESIAN_POINT ( 'NONE',  ( 7.450000000000003730, -7.249999999999997335, -10.00000000000000000 ) ) ;
#40289=CARTESIAN_POINT ( 'NONE',  ( 7.250000000000005329, 8.250000000000001776, -12.00000000000000000 ) ) ;
#40291=ORIENTED_EDGE ( 'NONE', *, *, #19215, .T. ) ;
#40299=DIRECTION ( 'NONE',  ( 1.000000000000000000, 0.000000000000000000, 0.000000000000000000 ) ) ;
#40304=CARTESIAN_POINT ( 'NONE',  ( -7.250000000000000000, -7.449999999999998401, -18.00000000000000000 ) ) ;
#40313=VERTEX_POINT ( 'NONE', #21089 ) ;
#40334=DIRECTION ( 'NONE',  ( -1.000000000000000000, 1.794541526872559352E-16, 0.000000000000000000 ) ) ;
#40345=DIRECTION ( 'NONE',  ( 0.000000000000000000, -1.000000000000000000, 0.000000000000000000 ) ) ;
#40354=CARTESIAN_POINT ( 'NONE',  ( -7.450000000000001954, 7.250000000000000000, -8.500000000000000000 ) ) ;
#40357=VECTOR ( 'NONE', #43535, 1000.000000000000000 ) ;
#40359=CIRCLE ( 'NONE', #32509, 0.2000000000000005107 ) ;
#40363=CARTESIAN_POINT ( 'NONE',  ( 7.450000000000003730, -7.249999999999997335, -24.00000000000000000 ) ) ;
#40369=AXIS2_PLACEMENT_3D ( 'NONE', #64160, #52485, #20996 ) ;
#40380=CARTESIAN_POINT ( 'NONE',  ( -7.250000000000001776, -7.249999999999998224, -12.50000000000000000 ) ) ;
#40381=ORIENTED_EDGE ( 'NONE', *, *, #46488, .T. ) ;
#40390=VERTEX_POINT ( 'NONE', #43702 ) ;
#40393=CARTESIAN_POINT ( 'NONE',  ( 0.000000000000000000, 0.000000000000000000, -11.50000000000000000 ) ) ;
#40397=CIRCLE ( 'NONE', #16700, 1.500000000000000444 ) ;
#40398=ORIENTED_EDGE ( 'NONE', *, *, #53871, .T. ) ;
#40400=CARTESIAN_POINT ( 'NONE',  ( 8.250000000000005329, -7.249999999999998224, -16.00000000000000000 ) ) ;
#40403=DIRECTION ( 'NONE',  ( 1.000000000000000000, 0.000000000000000000, 0.000000000000000000 ) ) ;
#40408=LINE ( 'NONE', #55974, #32862 ) ;
#40417=CARTESIAN_POINT ( 'NONE',  ( 6.500000000000002665, 6.500000000000000888, -1.000000000000000000 ) ) ;
#40419=AXIS2_PLACEMENT_3D ( 'NONE', #7502, #8193, #18106 ) ;
#40430=CARTESIAN_POINT ( 'NONE',  ( -7.450000000000001954, -7.249999999999998224, -12.00000000000000000 ) ) ;
#40442=ORIENTED_EDGE ( 'NONE', *, *, #6846, .T. ) ;
#40444=LINE ( 'NONE', #1563, #44633 ) ;
#40446=VERTEX_POINT ( 'NONE', #34106 ) ;
#40447=DIRECTION ( 'NONE',  ( 0.000000000000000000, 0.000000000000000000, 1.000000000000000000 ) ) ;
#40450=VECTOR ( 'NONE', #16680, 1000.000000000000000 ) ;
#40453=ORIENTED_EDGE ( 'NONE', *, *, #47921, .T. ) ;
#40458=VERTEX_POINT ( 'NONE', #19512 ) ;
#40467=DIRECTION ( 'NONE',  ( 0.000000000000000000, 0.000000000000000000, 1.000000000000000000 ) ) ;
#40473=FACE_OUTER_BOUND ( 'NONE', #31979, .T. ) ;
#40475=LINE ( 'NONE', #57091, #60158 ) ;
#40477=FACE_OUTER_BOUND ( 'NONE', #50065, .T. ) ;
#40480=LINE ( 'NONE', #57097, #26039 ) ;
#40485=DIRECTION ( 'NONE',  ( 0.000000000000000000, 0.000000000000000000, 1.000000000000000000 ) ) ;
#40495=ORIENTED_EDGE ( 'NONE', *, *, #7554, .T. ) ;
#40496=AXIS2_PLACEMENT_3D ( 'NONE', #47910, #57119, #19632 ) ;
#40504=AXIS2_PLACEMENT_3D ( 'NONE', #35442, #24505, #2231 ) ;
#40506=DIRECTION ( 'NONE',  ( -0.000000000000000000, -0.000000000000000000, 1.000000000000000000 ) ) ;
#40508=VERTEX_POINT ( 'NONE', #14925 ) ;
#40509=DIRECTION ( 'NONE',  ( 0.000000000000000000, 0.000000000000000000, -1.000000000000000000 ) ) ;
#40514=ORIENTED_EDGE ( 'NONE', *, *, #68604, .F. ) ;
#40515=ORIENTED_EDGE ( 'NONE', *, *, #64056, .F. ) ;
#40518=CARTESIAN_POINT ( 'NONE',  ( 7.250000000000005329, -7.249999999999998224, -8.000000000000000000 ) ) ;
#40520=CARTESIAN_POINT ( 'NONE',  ( 8.250000000000005329, -7.249999999999998224, -26.00000000000001066 ) ) ;
#40528=CARTESIAN_POINT ( 'NONE',  ( -7.250000000000000888, -8.249999999999998224, -26.00000000000001066 ) ) ;
#40533=PLANE ( 'NONE',  #45726 ) ;
#40538=FACE_OUTER_BOUND ( 'NONE', #8502, .T. ) ;
#40540=DIRECTION ( 'NONE',  ( 1.000000000000000000, 0.000000000000000000, 0.000000000000000000 ) ) ;
#40546=CARTESIAN_POINT ( 'NONE',  ( -8.250000000000000000, 7.250000000000001776, -24.00000000000000000 ) ) ;
#40559=EDGE_LOOP ( 'NONE', ( #28155, #2653, #27918, #2135 ) ) ;
#40564=VECTOR ( 'NONE', #23419, 1000.000000000000000 ) ;
#40587=ORIENTED_EDGE ( 'NONE', *, *, #7463, .F. ) ;
#40588=EDGE_CURVE ( 'NONE', #30915, #52575, #58423, .T. ) ;
#40590=CARTESIAN_POINT ( 'NONE',  ( -7.250000000000000888, 8.250000000000001776, -26.00000000000001066 ) ) ;
#40600=ORIENTED_EDGE ( 'NONE', *, *, #2112, .T. ) ;
#40603=VECTOR ( 'NONE', #35174, 1000.000000000000000 ) ;
#40613=VERTEX_POINT ( 'NONE', #10658 ) ;
#40618=DIRECTION ( 'NONE',  ( -0.000000000000000000, -0.000000000000000000, 1.000000000000000000 ) ) ;
#40626=CARTESIAN_POINT ( 'NONE',  ( -8.250000000000001776, 0.000000000000000000, -12.00000000000000000 ) ) ;
#40635=EDGE_CURVE ( 'NONE', #66346, #34593, #5760, .T. ) ;
#40636=CARTESIAN_POINT ( 'NONE',  ( -9.690000000000001279, 9.750000000000001776, -4.250000000000000000 ) ) ;
#40638=LINE ( 'NONE', #13763, #32399 ) ;
#40657=CARTESIAN_POINT ( 'NONE',  ( 0.000000000000000000, -8.249999999999998224, -18.50000000000000000 ) ) ;
#40670=VECTOR ( 'NONE', #28098, 1000.000000000000000 ) ;
#40671=CARTESIAN_POINT ( 'NONE',  ( -8.250000000000001776, 7.250000000000000888, -26.00000000000001066 ) ) ;
#40677=CARTESIAN_POINT ( 'NONE',  ( 7.250000000000005329, -8.249999999999998224, -22.00000000000000000 ) ) ;
#40678=CARTESIAN_POINT ( 'NONE',  ( 7.250000000000005329, -7.449999999999998401, -22.00000000000000000 ) ) ;
#40681=ORIENTED_EDGE ( 'NONE', *, *, #33163, .F. ) ;
#40685=CARTESIAN_POINT ( 'NONE',  ( 7.450000000000006395, 7.250000000000000888, -21.50000000000000000 ) ) ;
#40698=DIRECTION ( 'NONE',  ( 1.000000000000000000, 2.312964634635741083E-15, 0.000000000000000000 ) ) ;
#40701=CARTESIAN_POINT ( 'NONE',  ( 0.000000000000000000, 8.250000000000001776, -15.50000000000000000 ) ) ;
#40706=EDGE_CURVE ( 'NONE', #49824, #3823, #36222, .T. ) ;
#40717=EDGE_CURVE ( 'NONE', #37156, #38565, #56560, .T. ) ;
#40719=EDGE_CURVE ( 'NONE', #25093, #31165, #55182, .T. ) ;
#40721=AXIS2_PLACEMENT_3D ( 'NONE', #69890, #47281, #9452 ) ;
#40725=CARTESIAN_POINT ( 'NONE',  ( 7.250000000000005329, 7.250000000000000888, -23.00000000000000000 ) ) ;
#40732=EDGE_CURVE ( 'NONE', #48512, #53541, #23347, .T. ) ;
#40734=DIRECTION ( 'NONE',  ( -0.000000000000000000, 0.000000000000000000, 1.000000000000000000 ) ) ;
#40752=CARTESIAN_POINT ( 'NONE',  ( -7.250000000000000888, 8.250000000000001776, -26.00000000000001066 ) ) ;
#40757=ORIENTED_EDGE ( 'NONE', *, *, #21740, .T. ) ;
#40760=AXIS2_PLACEMENT_3D ( 'NONE', #66015, #39155, #17577 ) ;
#40762=CARTESIAN_POINT ( 'NONE',  ( 8.250000000000005329, 0.000000000000000000, -17.00000000000000000 ) ) ;
#40765=LINE ( 'NONE', #62323, #26350 ) ;
#40774=ORIENTED_EDGE ( 'NONE', *, *, #65634, .F. ) ;
#40783=ORIENTED_EDGE ( 'NONE', *, *, #65005, .F. ) ;
#40792=ORIENTED_EDGE ( 'NONE', *, *, #33163, .T. ) ;
#40796=ORIENTED_EDGE ( 'NONE', *, *, #62648, .T. ) ;
#40801=CYLINDRICAL_SURFACE ( 'NONE', #1816, 1.000000000000000000 ) ;
#40804=DIRECTION ( 'NONE',  ( -1.000000000000000000, 0.000000000000000000, 0.000000000000000000 ) ) ;
#40805=CARTESIAN_POINT ( 'NONE',  ( -7.250000000000000888, 7.250000000000001776, -26.00000000000001066 ) ) ;
#40810=DIRECTION ( 'NONE',  ( -1.000000000000000000, 0.000000000000000000, 0.000000000000000000 ) ) ;
#40819=VECTOR ( 'NONE', #16691, 1000.000000000000000 ) ;
#40844=EDGE_CURVE ( 'NONE', #23324, #65486, #20137, .T. ) ;
#40845=CARTESIAN_POINT ( 'NONE',  ( -7.450000000000001954, 0.000000000000000000, -21.50000000000000000 ) ) ;
#40850=DIRECTION ( 'NONE',  ( 1.000000000000000000, 0.000000000000000000, 0.000000000000000000 ) ) ;
#40855=AXIS2_PLACEMENT_3D ( 'NONE', #28618, #33583, #45569 ) ;
#40866=DIRECTION ( 'NONE',  ( 1.000000000000000000, 0.000000000000000000, 0.000000000000000000 ) ) ;
#40870=CARTESIAN_POINT ( 'NONE',  ( 7.450000000000004619, -1.336933437520057563E-15, -12.50000000000000000 ) ) ;
#40873=ORIENTED_EDGE ( 'NONE', *, *, #37235, .F. ) ;
#40877=CARTESIAN_POINT ( 'NONE',  ( 0.000000000000000000, -7.449999999999998401, -11.50000000000000000 ) ) ;
#40891=VECTOR ( 'NONE', #21102, 1000.000000000000000 ) ;
#40903=DIRECTION ( 'NONE',  ( -0.000000000000000000, -0.000000000000000000, -1.000000000000000000 ) ) ;
#40904=VERTEX_POINT ( 'NONE', #14126 ) ;
#40905=CARTESIAN_POINT ( 'NONE',  ( -8.250000000000001776, -7.249999999999998224, -12.00000000000000000 ) ) ;
#40907=ORIENTED_EDGE ( 'NONE', *, *, #62101, .T. ) ;
#40908=DIRECTION ( 'NONE',  ( 0.000000000000000000, 0.000000000000000000, 1.000000000000000000 ) ) ;
#40911=CARTESIAN_POINT ( 'NONE',  ( -10.50000000000000178, -9.690000000000001279, 0.000000000000000000 ) ) ;
#40930=ORIENTED_EDGE ( 'NONE', *, *, #62735, .T. ) ;
#40932=CARTESIAN_POINT ( 'NONE',  ( -7.450000000000001954, -7.249999999999998224, -8.000000000000000000 ) ) ;
#40933=LINE ( 'NONE', #56167, #44848 ) ;
#40945=EDGE_LOOP ( 'NONE', ( #8836, #3306, #11959, #457 ) ) ;
#40947=EDGE_CURVE ( 'NONE', #60252, #32685, #24030, .T. ) ;
#40952=DIRECTION ( 'NONE',  ( -1.000000000000000000, 0.000000000000000000, 0.000000000000000000 ) ) ;
#40953=CARTESIAN_POINT ( 'NONE',  ( -7.250000000000001776, -7.249999999999998224, -22.50000000000000000 ) ) ;
#40955=ADVANCED_FACE ( 'NONE', ( #3881 ), #25445, .T. ) ;
#40959=ORIENTED_EDGE ( 'NONE', *, *, #64785, .T. ) ;
#40971=VERTEX_POINT ( 'NONE', #26152 ) ;
#40979=ORIENTED_EDGE ( 'NONE', *, *, #4007, .F. ) ;
#40987=VECTOR ( 'NONE', #22290, 1000.000000000000000 ) ;
#40999=DIRECTION ( 'NONE',  ( 0.000000000000000000, 0.000000000000000000, -1.000000000000000000 ) ) ;
#41007=EDGE_CURVE ( 'NONE', #10955, #48587, #42403, .T. ) ;
#41015=ORIENTED_EDGE ( 'NONE', *, *, #22810, .F. ) ;
#41016=LINE ( 'NONE', #68613, #14623 ) ;
#41022=ADVANCED_FACE ( 'NONE', ( #48059 ), #69639, .F. ) ;
#41031=CARTESIAN_POINT ( 'NONE',  ( -7.250000000000001776, -7.249999999999998224, -25.50000000000000355 ) ) ;
#41033=VERTEX_POINT ( 'NONE', #64328 ) ;
#41040=EDGE_LOOP ( 'NONE', ( #6079, #63881, #39195, #4099 ) ) ;
#41042=EDGE_CURVE ( 'NONE', #47075, #54499, #59014, .T. ) ;
#41053=ADVANCED_FACE ( 'NONE', ( #4241 ), #25806, .T. ) ;
#41058=VERTEX_POINT ( 'NONE', #27879 ) ;
#41059=FACE_OUTER_BOUND ( 'NONE', #41280, .T. ) ;
#41066=ORIENTED_EDGE ( 'NONE', *, *, #64158, .F. ) ;
#41072=CIRCLE ( 'NONE', #33143, 0.9999999999999991118 ) ;
#41073=AXIS2_PLACEMENT_3D ( 'NONE', #3382, #47566, #30602 ) ;
#41075=LINE ( 'NONE', #8195, #69054 ) ;
#41093=DIRECTION ( 'NONE',  ( 0.000000000000000000, -0.000000000000000000, 1.000000000000000000 ) ) ;
#41096=ORIENTED_EDGE ( 'NONE', *, *, #7980, .F. ) ;
#41129=ORIENTED_EDGE ( 'NONE', *, *, #21968, .T. ) ;
#41131=ORIENTED_EDGE ( 'NONE', *, *, #45672, .T. ) ;
#41133=ORIENTED_EDGE ( 'NONE', *, *, #7980, .T. ) ;
#41153=EDGE_CURVE ( 'NONE', #48512, #47820, #22236, .T. ) ;
#41157=CIRCLE ( 'NONE', #45689, 0.2000000000000005107 ) ;
#41158=EDGE_CURVE ( 'NONE', #32818, #53583, #1018, .T. ) ;
#41170=CARTESIAN_POINT ( 'NONE',  ( 4.456444791733522252E-16, 7.450000000000002842, -7.500000000000000000 ) ) ;
#41184=CARTESIAN_POINT ( 'NONE',  ( -7.450000000000001954, 7.250000000000000000, -19.50000000000000000 ) ) ;
#41187=CIRCLE ( 'NONE', #67176, 0.1999999999999996503 ) ;
#41191=VERTEX_POINT ( 'NONE', #23593 ) ;
#41194=VERTEX_POINT ( 'NONE', #59708 ) ;
#41198=DIRECTION ( 'NONE',  ( 0.000000000000000000, 0.000000000000000000, -1.000000000000000000 ) ) ;
#41203=DIRECTION ( 'NONE',  ( 0.000000000000000000, 0.000000000000000000, -1.000000000000000000 ) ) ;
#41205=VERTEX_POINT ( 'NONE', #62119 ) ;
#41206=ORIENTED_EDGE ( 'NONE', *, *, #8794, .F. ) ;
#41209=EDGE_LOOP ( 'NONE', ( #8352, #22749, #61024, #27568 ) ) ;
#41210=VECTOR ( 'NONE', #53907, 1000.000000000000000 ) ;
#41211=ORIENTED_EDGE ( 'NONE', *, *, #69417, .T. ) ;
#41226=CARTESIAN_POINT ( 'NONE',  ( -7.450000000000001954, 7.250000000000000000, -18.50000000000000000 ) ) ;
#41227=AXIS2_PLACEMENT_3D ( 'NONE', #32140, #9890, #9529 ) ;
#41231=DIRECTION ( 'NONE',  ( -0.000000000000000000, -0.000000000000000000, 1.000000000000000000 ) ) ;
#41234=EDGE_CURVE ( 'NONE', #54166, #42553, #40207, .T. ) ;
#41242=EDGE_CURVE ( 'NONE', #69246, #67025, #39482, .T. ) ;
#41245=CARTESIAN_POINT ( 'NONE',  ( 7.250000000000005329, 7.250000000000000888, -17.00000000000000000 ) ) ;
#41246=DIRECTION ( 'NONE',  ( -1.000000000000000000, 0.000000000000000000, 0.000000000000000000 ) ) ;
#41249=FACE_OUTER_BOUND ( 'NONE', #46937, .T. ) ;
#41258=DIRECTION ( 'NONE',  ( 0.000000000000000000, 1.000000000000000000, 0.000000000000000000 ) ) ;
#41263=PLANE ( 'NONE',  #16966 ) ;
#41264=ORIENTED_EDGE ( 'NONE', *, *, #2371, .T. ) ;
#41267=AXIS2_PLACEMENT_3D ( 'NONE', #42388, #37445, #63978 ) ;
#41269=ORIENTED_EDGE ( 'NONE', *, *, #23973, .F. ) ;
#41280=EDGE_LOOP ( 'NONE', ( #38717, #69565, #34871, #35632 ) ) ;
#41286=CARTESIAN_POINT ( 'NONE',  ( 7.450000000000004619, -1.336933437520057563E-15, -18.50000000000000000 ) ) ;
#41296=EDGE_LOOP ( 'NONE', ( #1551, #62682, #7617, #66205 ) ) ;
#41301=EDGE_CURVE ( 'NONE', #57771, #53541, #29240, .T. ) ;
#41303=EDGE_LOOP ( 'NONE', ( #14553, #65799, #66021, #8207 ) ) ;
#41304=CARTESIAN_POINT ( 'NONE',  ( -7.250000000000001776, -7.249999999999998224, -11.50000000000000000 ) ) ;
#41308=DIRECTION ( 'NONE',  ( -1.000000000000000000, 0.000000000000000000, -0.000000000000000000 ) ) ;
#41317=CIRCLE ( 'NONE', #9698, 0.2000000000000005107 ) ;
#41322=CARTESIAN_POINT ( 'NONE',  ( -7.250000000000000000, -7.449999999999998401, -18.50000000000000000 ) ) ;
#41326=CIRCLE ( 'NONE', #18766, 1.000000000000000000 ) ;
#41329=LINE ( 'NONE', #46631, #30192 ) ;
#41331=EDGE_CURVE ( 'NONE', #54026, #24533, #51880, .T. ) ;
#41339=VERTEX_POINT ( 'NONE', #35961 ) ;
#41352=DIRECTION ( 'NONE',  ( 0.000000000000000000, 0.000000000000000000, 1.000000000000000000 ) ) ;
#41356=ORIENTED_EDGE ( 'NONE', *, *, #4429, .F. ) ;
#41360=AXIS2_PLACEMENT_3D ( 'NONE', #68069, #30591, #4777 ) ;
#41361=ADVANCED_FACE ( 'NONE', ( #67785 ), #19339, .F. ) ;
#41374=CARTESIAN_POINT ( 'NONE',  ( 7.450000000000004619, -1.336933437520057563E-15, -18.00000000000000000 ) ) ;
#41378=PLANE ( 'NONE',  #28599 ) ;
#41386=ORIENTED_EDGE ( 'NONE', *, *, #67316, .T. ) ;
#41387=CARTESIAN_POINT ( 'NONE',  ( 0.000000000000000000, -7.449999999999998401, -13.50000000000000178 ) ) ;
#41398=DIRECTION ( 'NONE',  ( -0.000000000000000000, -0.000000000000000000, 1.000000000000000000 ) ) ;
#41402=LINE ( 'NONE', #40701, #55630 ) ;
#41404=EDGE_LOOP ( 'NONE', ( #26037, #69467, #27159, #41676, #8778, #29821, #13909, #1975 ) ) ;
#41412=FACE_BOUND ( 'NONE', #35289, .T. ) ;
#41419=VECTOR ( 'NONE', #53018, 1000.000000000000000 ) ;
#41422=ORIENTED_EDGE ( 'NONE', *, *, #36829, .F. ) ;
#41432=DIRECTION ( 'NONE',  ( -1.000000000000000000, 0.000000000000000000, 0.000000000000000000 ) ) ;
#41434=AXIS2_PLACEMENT_3D ( 'NONE', #12577, #34145, #40509 ) ;
#41439=ORIENTED_EDGE ( 'NONE', *, *, #8149, .T. ) ;
#41454=EDGE_CURVE ( 'NONE', #54119, #28003, #6782, .T. ) ;
#41455=EDGE_CURVE ( 'NONE', #55467, #17361, #10144, .T. ) ;
#41456=EDGE_CURVE ( 'NONE', #55374, #24148, #48326, .T. ) ;
#41457=CARTESIAN_POINT ( 'NONE',  ( -7.250000000000000888, 7.250000000000001776, -23.50000000000000000 ) ) ;
#41469=FACE_OUTER_BOUND ( 'NONE', #68607, .T. ) ;
#41470=CIRCLE ( 'NONE', #67462, 1.500000000000000444 ) ;
#41478=VERTEX_POINT ( 'NONE', #5538 ) ;
#41480=EDGE_CURVE ( 'NONE', #69235, #2477, #68499, .T. ) ;
#41484=AXIS2_PLACEMENT_3D ( 'NONE', #7212, #39395, #50358 ) ;
#41491=VECTOR ( 'NONE', #10814, 1000.000000000000000 ) ;
#41523=AXIS2_PLACEMENT_3D ( 'NONE', #39141, #17567, #32798 ) ;
#41525=ADVANCED_FACE ( 'NONE', ( #22148 ), #1271, .T. ) ;
#41529=DIRECTION ( 'NONE',  ( 1.000000000000000000, 0.000000000000000000, 0.000000000000000000 ) ) ;
#41531=FACE_OUTER_BOUND ( 'NONE', #60246, .T. ) ;
#41537=AXIS2_PLACEMENT_3D ( 'NONE', #47301, #21132, #69577 ) ;
#41538=CYLINDRICAL_SURFACE ( 'NONE', #59080, 1.000000000000000000 ) ;
#41543=EDGE_CURVE ( 'NONE', #30263, #54026, #66322, .T. ) ;
#41547=DIRECTION ( 'NONE',  ( -0.000000000000000000, -0.000000000000000000, -1.000000000000000000 ) ) ;
#41553=ORIENTED_EDGE ( 'NONE', *, *, #69883, .F. ) ;
#41562=DIRECTION ( 'NONE',  ( 0.000000000000000000, 0.000000000000000000, -1.000000000000000000 ) ) ;
#41565=AXIS2_PLACEMENT_3D ( 'NONE', #48852, #53816, #17343 ) ;
#41570=CARTESIAN_POINT ( 'NONE',  ( 0.000000000000000000, -7.449999999999998401, -17.50000000000000000 ) ) ;
#41579=VECTOR ( 'NONE', #45882, 1000.000000000000000 ) ;
#41580=CARTESIAN_POINT ( 'NONE',  ( -7.450000000000001954, 7.250000000000000000, -13.50000000000000178 ) ) ;
#41582=VERTEX_POINT ( 'NONE', #59965 ) ;
#41584=VECTOR ( 'NONE', #67129, 1000.000000000000000 ) ;
#41585=LINE ( 'NONE', #53263, #34543 ) ;
#41588=VECTOR ( 'NONE', #7928, 1000.000000000000000 ) ;
#41591=CARTESIAN_POINT ( 'NONE',  ( -7.250000000000001776, -7.249999999999998224, -13.00000000000000178 ) ) ;
#41607=CARTESIAN_POINT ( 'NONE',  ( -8.250000000000001776, -7.249999999999998224, -26.00000000000001066 ) ) ;
#41617=ORIENTED_EDGE ( 'NONE', *, *, #60813, .T. ) ;
#41618=DIRECTION ( 'NONE',  ( 1.000000000000000000, 0.000000000000000000, 0.000000000000000000 ) ) ;
#41622=FACE_OUTER_BOUND ( 'NONE', #33879, .T. ) ;
#41630=AXIS2_PLACEMENT_3D ( 'NONE', #68384, #3334, #46459 ) ;
#41634=ORIENTED_EDGE ( 'NONE', *, *, #25391, .T. ) ;
#41642=EDGE_CURVE ( 'NONE', #17131, #64382, #28469, .T. ) ;
#41649=CARTESIAN_POINT ( 'NONE',  ( -8.250000000000001776, 7.250000000000000888, -26.00000000000001066 ) ) ;
#41653=ORIENTED_EDGE ( 'NONE', *, *, #17579, .T. ) ;
#41657=LINE ( 'NONE', #63589, #20666 ) ;
#41659=LINE ( 'NONE', #36353, #54827 ) ;
#41665=CIRCLE ( 'NONE', #47325, 0.1999999999999996503 ) ;
#41668=CYLINDRICAL_SURFACE ( 'NONE', #9117, 0.2000000000000005107 ) ;
#41672=DIRECTION ( 'NONE',  ( -1.000000000000000000, 2.602085213965213008E-15, 0.000000000000000000 ) ) ;
#41673=CARTESIAN_POINT ( 'NONE',  ( -8.250000000000000000, 7.250000000000001776, -25.00000000000000000 ) ) ;
#41676=ORIENTED_EDGE ( 'NONE', *, *, #29379, .T. ) ;
#41680=CARTESIAN_POINT ( 'NONE',  ( 7.450000000000006395, 7.250000000000000888, -24.00000000000000000 ) ) ;
#41681=DIRECTION ( 'NONE',  ( 1.000000000000000000, 0.000000000000000000, 0.000000000000000000 ) ) ;
#41682=AXIS2_PLACEMENT_3D ( 'NONE', #46532, #30631, #24634 ) ;
#41684=ORIENTED_EDGE ( 'NONE', *, *, #33560, .T. ) ;
#41692=EDGE_LOOP ( 'NONE', ( #44923, #54285, #8121, #22512 ) ) ;
#41696=AXIS2_PLACEMENT_3D ( 'NONE', #43510, #48834, #27270 ) ;
#41701=EDGE_LOOP ( 'NONE', ( #49509, #54357, #21714, #24805 ) ) ;
#41705=CARTESIAN_POINT ( 'NONE',  ( 7.250000000000004441, 7.450000000000001954, -25.50000000000000355 ) ) ;
#41707=LINE ( 'NONE', #40657, #21710 ) ;
#41710=ORIENTED_EDGE ( 'NONE', *, *, #41242, .T. ) ;
#41711=FACE_OUTER_BOUND ( 'NONE', #36128, .T. ) ;
#41712=VECTOR ( 'NONE', #40345, 1000.000000000000000 ) ;
#41716=DIRECTION ( 'NONE',  ( 0.000000000000000000, 0.000000000000000000, 1.000000000000000000 ) ) ;
#41728=CIRCLE ( 'NONE', #11236, 0.9999999999999991118 ) ;
#41729=DIRECTION ( 'NONE',  ( 0.000000000000000000, 1.000000000000000000, 0.000000000000000000 ) ) ;
#41733=CARTESIAN_POINT ( 'NONE',  ( -7.250000000000000888, -8.249999999999998224, -26.00000000000001066 ) ) ;
#41737=AXIS2_PLACEMENT_3D ( 'NONE', #18738, #51258, #45251 ) ;
#41738=FACE_OUTER_BOUND ( 'NONE', #25736, .T. ) ;
#41751=PLANE ( 'NONE',  #13599 ) ;
#41755=CARTESIAN_POINT ( 'NONE',  ( -7.250000000000001776, -7.249999999999998224, -24.50000000000000000 ) ) ;
#41756=LINE ( 'NONE', #4308, #66740 ) ;
#41760=CARTESIAN_POINT ( 'NONE',  ( 0.000000000000000000, -7.449999999999998401, -7.000000000000000000 ) ) ;
#41772=VERTEX_POINT ( 'NONE', #34819 ) ;
#41775=EDGE_CURVE ( 'NONE', #66751, #10351, #40480, .T. ) ;
#41778=FACE_OUTER_BOUND ( 'NONE', #32794, .T. ) ;
#41780=EDGE_CURVE ( 'NONE', #11827, #1911, #42940, .T. ) ;
#41782=FACE_OUTER_BOUND ( 'NONE', #13907, .T. ) ;
#41784=EDGE_LOOP ( 'NONE', ( #20019, #64664, #69549, #68348, #33120, #18049, #7072, #6194 ) ) ;
#41788=VECTOR ( 'NONE', #14617, 1000.000000000000000 ) ;
#41800=CARTESIAN_POINT ( 'NONE',  ( 7.250000000000005329, -7.449999999999998401, -20.50000000000000000 ) ) ;
#41806=ORIENTED_EDGE ( 'NONE', *, *, #30209, .T. ) ;
#41816=ORIENTED_EDGE ( 'NONE', *, *, #55795, .F. ) ;
#41819=EDGE_CURVE ( 'NONE', #18073, #60008, #64176, .T. ) ;
#41831=ORIENTED_EDGE ( 'NONE', *, *, #14494, .F. ) ;
#41833=DIRECTION ( 'NONE',  ( -1.000000000000000000, 0.000000000000000000, 0.000000000000000000 ) ) ;
#41840=ORIENTED_EDGE ( 'NONE', *, *, #35885, .F. ) ;
#41842=DIRECTION ( 'NONE',  ( 0.000000000000000000, 0.000000000000000000, -1.000000000000000000 ) ) ;
#41854=ADVANCED_FACE ( 'NONE', ( #42230, #30579 ), #21015, .F. ) ;
#41860=LINE ( 'NONE', #8274, #9551 ) ;
#41866=CARTESIAN_POINT ( 'NONE',  ( 7.250000000000005329, -7.249999999999998224, -13.00000000000000178 ) ) ;
#41868=ORIENTED_EDGE ( 'NONE', *, *, #1939, .F. ) ;
#41874=VECTOR ( 'NONE', #7822, 1000.000000000000000 ) ;
#41877=LINE ( 'NONE', #63451, #11245 ) ;
#41890=CARTESIAN_POINT ( 'NONE',  ( 7.250000000000005329, 8.250000000000001776, -9.000000000000001776 ) ) ;
#41891=ORIENTED_EDGE ( 'NONE', *, *, #8705, .T. ) ;
#41900=CARTESIAN_POINT ( 'NONE',  ( 8.250000000000005329, -7.249999999999998224, -24.50000000000000000 ) ) ;
#41901=CYLINDRICAL_SURFACE ( 'NONE', #28487, 1.000000000000000000 ) ;
#41903=ORIENTED_EDGE ( 'NONE', *, *, #31379, .F. ) ;
#41904=EDGE_CURVE ( 'NONE', #64467, #23968, #46709, .T. ) ;
#41906=FACE_OUTER_BOUND ( 'NONE', #61872, .T. ) ;
#41916=ORIENTED_EDGE ( 'NONE', *, *, #53761, .T. ) ;
#41919=ORIENTED_EDGE ( 'NONE', *, *, #65946, .F. ) ;
#41929=DIRECTION ( 'NONE',  ( -1.000000000000000000, 0.000000000000000000, 0.000000000000000000 ) ) ;
#41933=EDGE_CURVE ( 'NONE', #6920, #38565, #9242, .T. ) ;
#41938=DIRECTION ( 'NONE',  ( 0.000000000000000000, 0.000000000000000000, -1.000000000000000000 ) ) ;
#41940=ORIENTED_EDGE ( 'NONE', *, *, #48818, .T. ) ;
#41943=DIRECTION ( 'NONE',  ( -1.794541526872559352E-16, -1.000000000000000000, 0.000000000000000000 ) ) ;
#41947=PLANE ( 'NONE',  #44425 ) ;
#41955=CARTESIAN_POINT ( 'NONE',  ( 8.250000000000005329, 0.000000000000000000, -12.50000000000000000 ) ) ;
#41963=DIRECTION ( 'NONE',  ( 0.000000000000000000, 0.000000000000000000, 1.000000000000000000 ) ) ;
#41968=CYLINDRICAL_SURFACE ( 'NONE', #44703, 0.2000000000000005107 ) ;
#41980=DIRECTION ( 'NONE',  ( 1.000000000000000000, 0.000000000000000000, 0.000000000000000000 ) ) ;
#41982=ORIENTED_EDGE ( 'NONE', *, *, #5594, .F. ) ;
#41987=ORIENTED_EDGE ( 'NONE', *, *, #58330, .T. ) ;
#41998=CIRCLE ( 'NONE', #20548, 0.9999999999999991118 ) ;
#42002=ORIENTED_EDGE ( 'NONE', *, *, #51636, .F. ) ;
#42015=ORIENTED_EDGE ( 'NONE', *, *, #23743, .T. ) ;
#42025=DIRECTION ( 'NONE',  ( -1.000000000000000000, 2.602085213965213008E-15, 0.000000000000000000 ) ) ;
#42030=VERTEX_POINT ( 'NONE', #21599 ) ;
#42032=CARTESIAN_POINT ( 'NONE',  ( -7.250000000000000888, 8.250000000000001776, -14.50000000000000000 ) ) ;
#42040=DIRECTION ( 'NONE',  ( 0.000000000000000000, -1.000000000000000000, 0.000000000000000000 ) ) ;
#42042=VERTEX_POINT ( 'NONE', #14898 ) ;
#42045=VECTOR ( 'NONE', #34560, 1000.000000000000000 ) ;
#42047=CARTESIAN_POINT ( 'NONE',  ( 7.250000000000005329, -7.449999999999998401, -13.50000000000000178 ) ) ;
#42058=CARTESIAN_POINT ( 'NONE',  ( 8.250000000000005329, 8.250000000000001776, -26.00000000000001066 ) ) ;
#42066=LINE ( 'NONE', #35700, #30278 ) ;
#42070=VERTEX_POINT ( 'NONE', #48467 ) ;
#42078=CARTESIAN_POINT ( 'NONE',  ( -7.250000000000001776, -7.249999999999998224, -26.00000000000001066 ) ) ;
#42084=FACE_OUTER_BOUND ( 'NONE', #32915, .T. ) ;
#42092=DIRECTION ( 'NONE',  ( 1.000000000000000000, -5.981805089575194965E-17, 0.000000000000000000 ) ) ;
#42101=ORIENTED_EDGE ( 'NONE', *, *, #49322, .F. ) ;
#42104=DIRECTION ( 'NONE',  ( 0.000000000000000000, 1.000000000000000000, 0.000000000000000000 ) ) ;
#42114=FACE_BOUND ( 'NONE', #58892, .T. ) ;
#42115=CARTESIAN_POINT ( 'NONE',  ( -7.250000000000000000, -7.449999999999998401, -19.50000000000000000 ) ) ;
#42124=DIRECTION ( 'NONE',  ( 0.000000000000000000, 0.000000000000000000, -1.000000000000000000 ) ) ;
#42133=ADVANCED_FACE ( 'NONE', ( #15609 ), #59427, .T. ) ;
#42137=FACE_OUTER_BOUND ( 'NONE', #41296, .T. ) ;
#42138=VECTOR ( 'NONE', #2150, 1000.000000000000000 ) ;
#42142=ORIENTED_EDGE ( 'NONE', *, *, #36968, .F. ) ;
#42148=VECTOR ( 'NONE', #32964, 1000.000000000000000 ) ;
#42161=LINE ( 'NONE', #31574, #6307 ) ;
#42162=LINE ( 'NONE', #31232, #34309 ) ;
#42163=CARTESIAN_POINT ( 'NONE',  ( -8.250000000000001776, 0.000000000000000000, -25.00000000000000000 ) ) ;
#42165=EDGE_LOOP ( 'NONE', ( #63064, #69622, #52059, #16695, #31853, #56915, #7584, #14727 ) ) ;
#42183=ORIENTED_EDGE ( 'NONE', *, *, #66985, .F. ) ;
#42187=DIRECTION ( 'NONE',  ( -0.000000000000000000, -0.000000000000000000, -1.000000000000000000 ) ) ;
#42195=FACE_OUTER_BOUND ( 'NONE', #2746, .T. ) ;
#42204=CARTESIAN_POINT ( 'NONE',  ( 8.250000000000005329, 7.250000000000000888, -17.50000000000000000 ) ) ;
#42220=ORIENTED_EDGE ( 'NONE', *, *, #448, .F. ) ;
#42221=DIRECTION ( 'NONE',  ( 0.000000000000000000, 0.000000000000000000, -1.000000000000000000 ) ) ;
#42230=FACE_BOUND ( 'NONE', #46103, .T. ) ;
#42235=CARTESIAN_POINT ( 'NONE',  ( -6.749999999999998224, -7.348062532927999158, 0.000000000000000000 ) ) ;
#42237=DIRECTION ( 'NONE',  ( 0.000000000000000000, 0.000000000000000000, 1.000000000000000000 ) ) ;
#42242=CARTESIAN_POINT ( 'NONE',  ( -8.689999999999999503, 9.750000000000001776, -7.000000000000000000 ) ) ;
#42249=ORIENTED_EDGE ( 'NONE', *, *, #35866, .T. ) ;
#42260=ORIENTED_EDGE ( 'NONE', *, *, #51890, .T. ) ;
#42262=DIRECTION ( 'NONE',  ( -1.000000000000000000, 0.000000000000000000, 0.000000000000000000 ) ) ;
#42263=ORIENTED_EDGE ( 'NONE', *, *, #46614, .F. ) ;
#42274=DIRECTION ( 'NONE',  ( 0.000000000000000000, 1.000000000000000000, 0.000000000000000000 ) ) ;
#42279=AXIS2_PLACEMENT_3D ( 'NONE', #42058, #63636, #14130 ) ;
#42281=CARTESIAN_POINT ( 'NONE',  ( -8.250000000000001776, 7.250000000000000888, -13.50000000000000178 ) ) ;
#42284=AXIS2_PLACEMENT_3D ( 'NONE', #32962, #26970, #5048 ) ;
#42290=CARTESIAN_POINT ( 'NONE',  ( -7.450000000000001954, 0.000000000000000000, -10.00000000000000000 ) ) ;
#42298=PLANE ( 'NONE',  #30167 ) ;
#42302=DIRECTION ( 'NONE',  ( 0.000000000000000000, 0.000000000000000000, 1.000000000000000000 ) ) ;
#42304=LINE ( 'NONE', #47269, #68805 ) ;
#42308=LINE ( 'NONE', #26756, #13150 ) ;
#42315=DIRECTION ( 'NONE',  ( -1.000000000000000000, 0.000000000000000000, 0.000000000000000000 ) ) ;
#42318=DIRECTION ( 'NONE',  ( 1.000000000000000000, 0.000000000000000000, 0.000000000000000000 ) ) ;
#42321=CARTESIAN_POINT ( 'NONE',  ( -7.450000000000001954, 0.000000000000000000, -8.000000000000000000 ) ) ;
#42330=AXIS2_PLACEMENT_3D ( 'NONE', #36670, #9813, #52230 ) ;
#42345=VERTEX_POINT ( 'NONE', #17064 ) ;
#42351=ORIENTED_EDGE ( 'NONE', *, *, #19085, .F. ) ;
#42352=ORIENTED_EDGE ( 'NONE', *, *, #63892, .F. ) ;
#42355=DIRECTION ( 'NONE',  ( 1.000000000000000000, 0.000000000000000000, 0.000000000000000000 ) ) ;
#42356=EDGE_CURVE ( 'NONE', #55865, #1911, #11409, .T. ) ;
#42358=ORIENTED_EDGE ( 'NONE', *, *, #25920, .T. ) ;
#42363=ORIENTED_EDGE ( 'NONE', *, *, #15466, .T. ) ;
#42371=VERTEX_POINT ( 'NONE', #10378 ) ;
#42375=CARTESIAN_POINT ( 'NONE',  ( 7.250000000000004441, 7.450000000000001954, -22.50000000000000000 ) ) ;
#42380=LINE ( 'NONE', #63970, #31774 ) ;
#42385=PLANE ( 'NONE',  #23698 ) ;
#42388=CARTESIAN_POINT ( 'NONE',  ( 7.250000000000005329, -7.249999999999998224, -24.50000000000000000 ) ) ;
#42399=DIRECTION ( 'NONE',  ( -1.000000000000000000, 0.000000000000000000, 0.000000000000000000 ) ) ;
#42400=ORIENTED_EDGE ( 'NONE', *, *, #57319, .T. ) ;
#42403=LINE ( 'NONE', #47356, #37401 ) ;
#42411=CARTESIAN_POINT ( 'NONE',  ( 8.250000000000005329, -8.249999999999998224, -26.00000000000001066 ) ) ;
#42422=PLANE ( 'NONE',  #7276 ) ;
#42426=ORIENTED_EDGE ( 'NONE', *, *, #67678, .T. ) ;
#42431=CIRCLE ( 'NONE', #13079, 1.000000000000000000 ) ;
#42433=CARTESIAN_POINT ( 'NONE',  ( -7.250000000000000888, 7.250000000000001776, -15.50000000000000000 ) ) ;
#42443=EDGE_CURVE ( 'NONE', #23322, #50347, #48696, .T. ) ;
#42445=VECTOR ( 'NONE', #19865, 1000.000000000000000 ) ;
#42449=EDGE_CURVE ( 'NONE', #33218, #67025, #54910, .T. ) ;
#42453=CARTESIAN_POINT ( 'NONE',  ( -7.250000000000000888, 7.450000000000003730, -9.500000000000001776 ) ) ;
#42458=CARTESIAN_POINT ( 'NONE',  ( -7.450000000000001954, 0.000000000000000000, -24.50000000000000000 ) ) ;
#42459=VERTEX_POINT ( 'NONE', #44265 ) ;
#42469=DIRECTION ( 'NONE',  ( 0.000000000000000000, 0.000000000000000000, 1.000000000000000000 ) ) ;
#42474=DIRECTION ( 'NONE',  ( 0.000000000000000000, 0.000000000000000000, 1.000000000000000000 ) ) ;
#42478=ORIENTED_EDGE ( 'NONE', *, *, #65106, .F. ) ;
#42482=CARTESIAN_POINT ( 'NONE',  ( -7.250000000000000888, 7.250000000000001776, -30.00000000000001066 ) ) ;
#42490=CARTESIAN_POINT ( 'NONE',  ( 7.250000000000005329, -7.449999999999998401, -23.50000000000000000 ) ) ;
#42491=CARTESIAN_POINT ( 'NONE',  ( -8.250000000000000000, 7.250000000000001776, -14.00000000000000000 ) ) ;
#42494=VECTOR ( 'NONE', #20106, 1000.000000000000000 ) ;
#42503=DIRECTION ( 'NONE',  ( 1.000000000000000000, 0.000000000000000000, 0.000000000000000000 ) ) ;
#42504=VECTOR ( 'NONE', #29183, 1000.000000000000000 ) ;
#42507=DIRECTION ( 'NONE',  ( -1.000000000000000000, 2.602085213965213008E-15, 0.000000000000000000 ) ) ;
#42512=ORIENTED_EDGE ( 'NONE', *, *, #60910, .F. ) ;
#42516=LINE ( 'NONE', #63742, #8317 ) ;
#42517=LINE ( 'NONE', #10683, #54576 ) ;
#42527=CARTESIAN_POINT ( 'NONE',  ( 8.250000000000005329, -7.249999999999998224, -11.50000000000000000 ) ) ;
#42537=FACE_OUTER_BOUND ( 'NONE', #28898, .T. ) ;
#42547=AXIS2_PLACEMENT_3D ( 'NONE', #59272, #11170, #230 ) ;
#42552=ORIENTED_EDGE ( 'NONE', *, *, #275, .T. ) ;
#42553=VERTEX_POINT ( 'NONE', #40363 ) ;
#42555=AXIS2_PLACEMENT_3D ( 'NONE', #53099, #31876, #14196 ) ;
#42569=CYLINDRICAL_SURFACE ( 'NONE', #47603, 0.1999999999999987899 ) ;
#42578=EDGE_CURVE ( 'NONE', #41772, #66919, #41756, .T. ) ;
#42581=LINE ( 'NONE', #26322, #65222 ) ;
#42583=ORIENTED_EDGE ( 'NONE', *, *, #39757, .T. ) ;
#42584=FACE_OUTER_BOUND ( 'NONE', #915, .T. ) ;
#42590=CARTESIAN_POINT ( 'NONE',  ( 8.250000000000005329, -7.249999999999998224, -26.00000000000001066 ) ) ;
#42592=DIRECTION ( 'NONE',  ( 0.000000000000000000, 0.000000000000000000, 1.000000000000000000 ) ) ;
#42606=EDGE_LOOP ( 'NONE', ( #67192, #62975, #48960, #64717 ) ) ;
#42611=CARTESIAN_POINT ( 'NONE',  ( 7.250000000000005329, 7.250000000000000888, -21.50000000000000000 ) ) ;
#42613=ORIENTED_EDGE ( 'NONE', *, *, #46148, .T. ) ;
#42615=DIRECTION ( 'NONE',  ( -1.000000000000000000, 0.000000000000000000, 0.000000000000000000 ) ) ;
#42617=ORIENTED_EDGE ( 'NONE', *, *, #50860, .T. ) ;
#42618=ADVANCED_FACE ( 'NONE', ( #14189 ), #19840, .F. ) ;
#42620=ORIENTED_EDGE ( 'NONE', *, *, #45199, .F. ) ;
#42628=ORIENTED_EDGE ( 'NONE', *, *, #69883, .T. ) ;
#42655=EDGE_CURVE ( 'NONE', #31236, #32512, #28338, .T. ) ;
#42661=LINE ( 'NONE', #4496, #57224 ) ;
#42671=FACE_OUTER_BOUND ( 'NONE', #46051, .T. ) ;
#42683=VERTEX_POINT ( 'NONE', #31522 ) ;
#42685=DIRECTION ( 'NONE',  ( 1.000000000000000000, -0.000000000000000000, 0.000000000000000000 ) ) ;
#42709=DIRECTION ( 'NONE',  ( 0.000000000000000000, -0.000000000000000000, 1.000000000000000000 ) ) ;
#42711=ORIENTED_EDGE ( 'NONE', *, *, #1847, .F. ) ;
#42718=LINE ( 'NONE', #49344, #64499 ) ;
#42742=DIRECTION ( 'NONE',  ( -0.000000000000000000, 0.000000000000000000, 1.000000000000000000 ) ) ;
#42745=DIRECTION ( 'NONE',  ( 0.000000000000000000, -0.000000000000000000, 1.000000000000000000 ) ) ;
#42751=DIRECTION ( 'NONE',  ( 0.000000000000000000, 0.000000000000000000, -1.000000000000000000 ) ) ;
#42756=ADVANCED_FACE ( 'NONE', ( #32205 ), #5351, .F. ) ;
#42760=DIRECTION ( 'NONE',  ( 1.000000000000000000, -5.981805089575196197E-17, 0.000000000000000000 ) ) ;
#42770=ORIENTED_EDGE ( 'NONE', *, *, #17394, .T. ) ;
#42771=ORIENTED_EDGE ( 'NONE', *, *, #11812, .T. ) ;
#42772=DIRECTION ( 'NONE',  ( 0.000000000000000000, 0.000000000000000000, -1.000000000000000000 ) ) ;
#42777=PLANE ( 'NONE',  #49025 ) ;
#42778=ORIENTED_EDGE ( 'NONE', *, *, #10331, .T. ) ;
#42779=DIRECTION ( 'NONE',  ( -0.000000000000000000, 0.000000000000000000, 1.000000000000000000 ) ) ;
#42792=EDGE_CURVE ( 'NONE', #14260, #55322, #60104, .T. ) ;
#42795=EDGE_CURVE ( 'NONE', #26651, #48173, #66453, .T. ) ;
#42800=CARTESIAN_POINT ( 'NONE',  ( 7.250000000000005329, 7.250000000000000888, -17.50000000000000000 ) ) ;
#42814=AXIS2_PLACEMENT_3D ( 'NONE', #54139, #44195, #22643 ) ;
#42815=CARTESIAN_POINT ( 'NONE',  ( -6.500000000000002665, 6.500000000000002665, -1.000000000000000000 ) ) ;
#42818=ADVANCED_FACE ( 'NONE', ( #24006 ), #38885, .T. ) ;
#42820=CARTESIAN_POINT ( 'NONE',  ( 7.250000000000005329, -8.249999999999998224, -17.50000000000000000 ) ) ;
#42830=CARTESIAN_POINT ( 'NONE',  ( 8.250000000000005329, 7.250000000000000888, -21.00000000000000000 ) ) ;
#42833=CIRCLE ( 'NONE', #21389, 0.8100000000000017186 ) ;
#42843=ORIENTED_EDGE ( 'NONE', *, *, #9011, .T. ) ;
#42858=DIRECTION ( 'NONE',  ( 1.000000000000000000, -0.000000000000000000, 0.000000000000000000 ) ) ;
#42878=ORIENTED_EDGE ( 'NONE', *, *, #40732, .T. ) ;
#42885=DIRECTION ( 'NONE',  ( 0.000000000000000000, 0.000000000000000000, 1.000000000000000000 ) ) ;
#42886=ADVANCED_FACE ( 'NONE', ( #67146 ), #56537, .T. ) ;
#42887=EDGE_CURVE ( 'NONE', #9824, #49229, #49506, .T. ) ;
#42889=VECTOR ( 'NONE', #16079, 1000.000000000000000 ) ;
#42897=ORIENTED_EDGE ( 'NONE', *, *, #27175, .F. ) ;
#42900=CARTESIAN_POINT ( 'NONE',  ( 7.250000000000005329, 7.250000000000000888, -22.50000000000000000 ) ) ;
#42901=CARTESIAN_POINT ( 'NONE',  ( -6.500000000000002665, -6.500000000000002665, -1.000000000000000000 ) ) ;
#42903=AXIS2_PLACEMENT_3D ( 'NONE', #3538, #29335, #13781 ) ;
#42907=AXIS2_PLACEMENT_3D ( 'NONE', #18464, #13169, #56309 ) ;
#42913=AXIS2_PLACEMENT_3D ( 'NONE', #46804, #35138, #62716 ) ;
#42917=CARTESIAN_POINT ( 'NONE',  ( -7.250000000000001776, -7.249999999999998224, -26.00000000000001066 ) ) ;
#42935=CIRCLE ( 'NONE', #12418, 0.1999999999999987899 ) ;
#42936=CARTESIAN_POINT ( 'NONE',  ( 9.690000000000001279, -9.690000000000001279, -5.000000000000000000 ) ) ;
#42937=ORIENTED_EDGE ( 'NONE', *, *, #18596, .T. ) ;
#42940=CIRCLE ( 'NONE', #27147, 0.1999999999999987899 ) ;
#42943=DIRECTION ( 'NONE',  ( 0.000000000000000000, -1.000000000000000000, -0.000000000000000000 ) ) ;
#42950=VECTOR ( 'NONE', #11945, 1000.000000000000000 ) ;
#42951=ORIENTED_EDGE ( 'NONE', *, *, #45741, .F. ) ;
#42954=CARTESIAN_POINT ( 'NONE',  ( 8.250000000000005329, 7.250000000000000888, -25.50000000000000355 ) ) ;
#42959=VECTOR ( 'NONE', #51325, 1000.000000000000000 ) ;
#42961=AXIS2_PLACEMENT_3D ( 'NONE', #5498, #11811, #33399 ) ;
#42964=ORIENTED_EDGE ( 'NONE', *, *, #6871, .T. ) ;
#42965=EDGE_LOOP ( 'NONE', ( #12163, #45414, #48433, #25300 ) ) ;
#42970=CARTESIAN_POINT ( 'NONE',  ( 8.250000000000005329, 7.250000000000000888, -26.00000000000001066 ) ) ;
#42973=CARTESIAN_POINT ( 'NONE',  ( 7.250000000000005329, -7.249999999999998224, -18.50000000000000000 ) ) ;
#42983=CARTESIAN_POINT ( 'NONE',  ( -7.450000000000001954, -7.249999999999998224, -17.00000000000000000 ) ) ;
#42985=DIRECTION ( 'NONE',  ( 0.000000000000000000, 0.000000000000000000, -1.000000000000000000 ) ) ;
#42990=FACE_OUTER_BOUND ( 'NONE', #21289, .T. ) ;
#42992=TOROIDAL_SURFACE ( 'NONE', #13614, 0.06000000000000080963, 0.7500000000000000000 ) ;
#42993=AXIS2_PLACEMENT_3D ( 'NONE', #43816, #10591, #5988 ) ;
#42998=CARTESIAN_POINT ( 'NONE',  ( 7.250000000000005329, -7.449999999999998401, -16.00000000000000000 ) ) ;
#43019=VERTEX_POINT ( 'NONE', #41673 ) ;
#43021=DIRECTION ( 'NONE',  ( 0.000000000000000000, 0.000000000000000000, 1.000000000000000000 ) ) ;
#43027=DIRECTION ( 'NONE',  ( 0.000000000000000000, 0.000000000000000000, 1.000000000000000000 ) ) ;
#43031=CARTESIAN_POINT ( 'NONE',  ( 7.250000000000005329, -7.249999999999998224, -30.00000000000001066 ) ) ;
#43042=ORIENTED_EDGE ( 'NONE', *, *, #6972, .T. ) ;
#43043=VERTEX_POINT ( 'NONE', #32480 ) ;
#43050=VERTEX_POINT ( 'NONE', #32805 ) ;
#43056=ADVANCED_FACE ( 'NONE', ( #292 ), #58990, .F. ) ;
#43062=EDGE_LOOP ( 'NONE', ( #12309, #6997, #5309, #24761, #69059, #23695, #29042, #65912 ) ) ;
#43065=CARTESIAN_POINT ( 'NONE',  ( 7.250000000000005329, -7.449999999999998401, -11.00000000000000000 ) ) ;
#43073=VERTEX_POINT ( 'NONE', #69943 ) ;
#43084=ORIENTED_EDGE ( 'NONE', *, *, #24209, .T. ) ;
#43093=VERTEX_POINT ( 'NONE', #21506 ) ;
#43099=CARTESIAN_POINT ( 'NONE',  ( 4.456444791733522252E-16, 7.450000000000002842, -25.50000000000000355 ) ) ;
#43100=DIRECTION ( 'NONE',  ( 1.000000000000000000, -5.981805089575194965E-17, 0.000000000000000000 ) ) ;
#43105=ORIENTED_EDGE ( 'NONE', *, *, #13399, .F. ) ;
#43114=CARTESIAN_POINT ( 'NONE',  ( 7.250000000000005329, 7.250000000000000888, -20.50000000000000000 ) ) ;
#43118=FACE_OUTER_BOUND ( 'NONE', #59838, .T. ) ;
#43122=ORIENTED_EDGE ( 'NONE', *, *, #55420, .F. ) ;
#43138=DIRECTION ( 'NONE',  ( -0.000000000000000000, -0.000000000000000000, -1.000000000000000000 ) ) ;
#43140=ORIENTED_EDGE ( 'NONE', *, *, #35033, .T. ) ;
#43147=VERTEX_POINT ( 'NONE', #12257 ) ;
#43154=EDGE_LOOP ( 'NONE', ( #21013, #53494, #40907, #5668 ) ) ;
#43155=CARTESIAN_POINT ( 'NONE',  ( -8.250000000000000000, 7.250000000000001776, -21.00000000000000000 ) ) ;
#43161=LINE ( 'NONE', #37868, #60670 ) ;
#43164=FACE_OUTER_BOUND ( 'NONE', #69787, .T. ) ;
#43165=ORIENTED_EDGE ( 'NONE', *, *, #64378, .F. ) ;
#43166=CARTESIAN_POINT ( 'NONE',  ( 8.250000000000005329, 7.250000000000000888, -7.500000000000000000 ) ) ;
#43172=DIRECTION ( 'NONE',  ( -0.000000000000000000, -0.000000000000000000, 1.000000000000000000 ) ) ;
#43173=ORIENTED_EDGE ( 'NONE', *, *, #4899, .T. ) ;
#43176=CIRCLE ( 'NONE', #10470, 0.2000000000000005107 ) ;
#43180=DIRECTION ( 'NONE',  ( 0.000000000000000000, 0.000000000000000000, 1.000000000000000000 ) ) ;
#43194=CARTESIAN_POINT ( 'NONE',  ( -7.250000000000000888, 7.250000000000001776, -26.00000000000001066 ) ) ;
#43197=VERTEX_POINT ( 'NONE', #61758 ) ;
#43218=EDGE_CURVE ( 'NONE', #29125, #26913, #51858, .T. ) ;
#43227=ORIENTED_EDGE ( 'NONE', *, *, #30443, .F. ) ;
#43228=ORIENTED_EDGE ( 'NONE', *, *, #9602, .F. ) ;
#43233=ORIENTED_EDGE ( 'NONE', *, *, #32605, .T. ) ;
#43235=LINE ( 'NONE', #4385, #3428 ) ;
#43243=ORIENTED_EDGE ( 'NONE', *, *, #68435, .F. ) ;
#43247=CARTESIAN_POINT ( 'NONE',  ( 0.000000000000000000, -7.449999999999998401, -18.50000000000000000 ) ) ;
#43252=ORIENTED_EDGE ( 'NONE', *, *, #28749, .T. ) ;
#43262=FACE_OUTER_BOUND ( 'NONE', #44929, .T. ) ;
#43263=AXIS2_PLACEMENT_3D ( 'NONE', #45491, #18983, #39494 ) ;
#43265=ADVANCED_FACE ( 'NONE', ( #3414 ), #40533, .F. ) ;
#43270=CARTESIAN_POINT ( 'NONE',  ( 7.250000000000005329, -7.249999999999998224, -14.00000000000000000 ) ) ;
#43274=CARTESIAN_POINT ( 'NONE',  ( 0.000000000000000000, -7.449999999999998401, -11.50000000000000000 ) ) ;
#43276=CARTESIAN_POINT ( 'NONE',  ( -9.189999999999999503, -9.750000000000001776, -5.000000000000000000 ) ) ;
#43290=FACE_OUTER_BOUND ( 'NONE', #10029, .T. ) ;
#43294=CARTESIAN_POINT ( 'NONE',  ( 7.250000000000005329, 7.250000000000000888, -14.50000000000000000 ) ) ;
#43296=ORIENTED_EDGE ( 'NONE', *, *, #52829, .F. ) ;
#43298=VERTEX_POINT ( 'NONE', #54573 ) ;
#43307=VECTOR ( 'NONE', #66739, 1000.000000000000000 ) ;
#43309=VERTEX_POINT ( 'NONE', #38984 ) ;
#43311=EDGE_LOOP ( 'NONE', ( #29608, #33404, #5645, #58344 ) ) ;
#43312=ORIENTED_EDGE ( 'NONE', *, *, #22793, .F. ) ;
#43316=CIRCLE ( 'NONE', #46692, 0.1999999999999996503 ) ;
#43317=CARTESIAN_POINT ( 'NONE',  ( 7.450000000000003730, -7.249999999999997335, -20.00000000000000000 ) ) ;
#43320=EDGE_CURVE ( 'NONE', #28252, #1208, #31062, .T. ) ;
#43324=ORIENTED_EDGE ( 'NONE', *, *, #8588, .T. ) ;
#43326=DIRECTION ( 'NONE',  ( 0.000000000000000000, 1.000000000000000000, 0.000000000000000000 ) ) ;
#43346=CARTESIAN_POINT ( 'NONE',  ( 6.500000000000002665, 6.500000000000000888, -1.000000000000000000 ) ) ;
#43347=CIRCLE ( 'NONE', #64825, 0.1999999999999987899 ) ;
#43350=DIRECTION ( 'NONE',  ( 0.000000000000000000, 0.000000000000000000, 1.000000000000000000 ) ) ;
#43360=DIRECTION ( 'NONE',  ( -1.000000000000000000, 0.000000000000000000, 0.000000000000000000 ) ) ;
#43361=EDGE_CURVE ( 'NONE', #68958, #69246, #4820, .T. ) ;
#43368=FACE_OUTER_BOUND ( 'NONE', #61433, .T. ) ;
#43375=CARTESIAN_POINT ( 'NONE',  ( 0.000000000000000000, 0.000000000000000000, -20.50000000000000000 ) ) ;
#43376=ORIENTED_EDGE ( 'NONE', *, *, #26365, .T. ) ;
#43381=ORIENTED_EDGE ( 'NONE', *, *, #37544, .F. ) ;
#43392=DIRECTION ( 'NONE',  ( -1.000000000000000000, 0.000000000000000000, 0.000000000000000000 ) ) ;
#43408=VECTOR ( 'NONE', #13007, 1000.000000000000000 ) ;
#43414=CIRCLE ( 'NONE', #54734, 1.000000000000000000 ) ;
#43416=LINE ( 'NONE', #43777, #31895 ) ;
#43437=DIRECTION ( 'NONE',  ( 0.000000000000000000, 0.000000000000000000, -1.000000000000000000 ) ) ;
#43451=EDGE_LOOP ( 'NONE', ( #53807, #19473, #53503, #62696 ) ) ;
#43456=VECTOR ( 'NONE', #62686, 1000.000000000000000 ) ;
#43481=DIRECTION ( 'NONE',  ( -0.000000000000000000, -0.000000000000000000, 1.000000000000000000 ) ) ;
#43486=DIRECTION ( 'NONE',  ( 0.000000000000000000, 0.000000000000000000, 1.000000000000000000 ) ) ;
#43493=VECTOR ( 'NONE', #21148, 1000.000000000000000 ) ;
#43504=CARTESIAN_POINT ( 'NONE',  ( 7.250000000000005329, 7.250000000000000888, -21.50000000000000000 ) ) ;
#43507=DIRECTION ( 'NONE',  ( 1.000000000000000000, 0.000000000000000000, 0.000000000000000000 ) ) ;
#43508=VECTOR ( 'NONE', #59833, 1000.000000000000000 ) ;
#43510=CARTESIAN_POINT ( 'NONE',  ( 7.250000000000005329, 7.250000000000000888, -19.50000000000000000 ) ) ;
#43513=DIRECTION ( 'NONE',  ( -0.000000000000000000, -0.000000000000000000, -1.000000000000000000 ) ) ;
#43530=ADVANCED_FACE ( 'NONE', ( #67606 ), #19157, .T. ) ;
#43531=CARTESIAN_POINT ( 'NONE',  ( 6.750000000000000000, 7.750000000000000000, -5.000000000000000000 ) ) ;
#43535=DIRECTION ( 'NONE',  ( 0.000000000000000000, 1.000000000000000000, 0.000000000000000000 ) ) ;
#43540=VECTOR ( 'NONE', #6229, 1000.000000000000000 ) ;
#43546=VERTEX_POINT ( 'NONE', #61937 ) ;
#43549=CIRCLE ( 'NONE', #8554, 1.000000000000003553 ) ;
#43553=DIRECTION ( 'NONE',  ( 0.000000000000000000, 0.000000000000000000, -1.000000000000000000 ) ) ;
#43556=VECTOR ( 'NONE', #7217, 1000.000000000000000 ) ;
#43562=VERTEX_POINT ( 'NONE', #35405 ) ;
#43564=VERTEX_POINT ( 'NONE', #14552 ) ;
#43566=VECTOR ( 'NONE', #69927, 1000.000000000000000 ) ;
#43572=ADVANCED_FACE ( 'NONE', ( #58750 ), #36119, .F. ) ;
#43576=CARTESIAN_POINT ( 'NONE',  ( -7.250000000000000888, 7.250000000000001776, -10.00000000000000000 ) ) ;
#43579=ORIENTED_EDGE ( 'NONE', *, *, #61991, .T. ) ;
#43588=EDGE_CURVE ( 'NONE', #33622, #16636, #52045, .T. ) ;
#43592=DIRECTION ( 'NONE',  ( 0.000000000000000000, 0.000000000000000000, 1.000000000000000000 ) ) ;
#43594=EDGE_CURVE ( 'NONE', #16332, #45036, #630, .T. ) ;
#43601=ORIENTED_EDGE ( 'NONE', *, *, #34592, .F. ) ;
#43613=CIRCLE ( 'NONE', #40203, 1.000000000000000000 ) ;
#43619=AXIS2_PLACEMENT_3D ( 'NONE', #34077, #23832, #62005 ) ;
#43621=SURFACE_SIDE_STYLE ('',( #43956 ) ) ;
#43628=CARTESIAN_POINT ( 'NONE',  ( 4.456444791733522252E-16, 7.450000000000002842, -8.000000000000000000 ) ) ;
#43631=PLANE ( 'NONE',  #49369 ) ;
#43636=CARTESIAN_POINT ( 'NONE',  ( 8.250000000000005329, -7.249999999999998224, -12.50000000000000000 ) ) ;
#43640=DIRECTION ( 'NONE',  ( 1.000000000000000000, -5.981805089575196197E-17, 0.000000000000000000 ) ) ;
#43641=ORIENTED_EDGE ( 'NONE', *, *, #65245, .F. ) ;
#43642=EDGE_CURVE ( 'NONE', #21330, #25093, #64743, .T. ) ;
#43644=LINE ( 'NONE', #10424, #9786 ) ;
#43654=CIRCLE ( 'NONE', #764, 1.000000000000000000 ) ;
#43656=CARTESIAN_POINT ( 'NONE',  ( 8.250000000000005329, 7.250000000000000888, -17.00000000000000000 ) ) ;
#43662=AXIS2_PLACEMENT_3D ( 'NONE', #15844, #4550, #32189 ) ;
#43668=ORIENTED_EDGE ( 'NONE', *, *, #8953, .F. ) ;
#43675=CARTESIAN_POINT ( 'NONE',  ( -7.250000000000000888, 7.250000000000001776, -12.50000000000000000 ) ) ;
#43681=CARTESIAN_POINT ( 'NONE',  ( 0.000000000000000000, 0.000000000000000000, -24.50000000000000000 ) ) ;
#43692=ORIENTED_EDGE ( 'NONE', *, *, #48066, .T. ) ;
#43699=AXIS2_PLACEMENT_3D ( 'NONE', #33145, #53351, #54045 ) ;
#43702=CARTESIAN_POINT ( 'NONE',  ( 8.250000000000005329, -7.249999999999998224, -15.00000000000000000 ) ) ;
#43704=DIRECTION ( 'NONE',  ( 0.000000000000000000, -0.000000000000000000, 1.000000000000000000 ) ) ;
#43707=DIRECTION ( 'NONE',  ( -1.000000000000000000, 0.000000000000000000, 0.000000000000000000 ) ) ;
#43717=VECTOR ( 'NONE', #39818, 1000.000000000000000 ) ;
#43721=EDGE_CURVE ( 'NONE', #34015, #47489, #54831, .T. ) ;
#43729=EDGE_CURVE ( 'NONE', #56308, #24826, #393, .T. ) ;
#43733=ORIENTED_EDGE ( 'NONE', *, *, #64533, .F. ) ;
#43743=DIRECTION ( 'NONE',  ( -0.000000000000000000, 0.000000000000000000, -1.000000000000000000 ) ) ;
#43747=AXIS2_PLACEMENT_3D ( 'NONE', #67614, #11845, #33435 ) ;
#43749=DIRECTION ( 'NONE',  ( 0.000000000000000000, 0.000000000000000000, -1.000000000000000000 ) ) ;
#43755=CARTESIAN_POINT ( 'NONE',  ( 0.000000000000000000, 8.250000000000001776, -16.00000000000000000 ) ) ;
#43756=LINE ( 'NONE', #55073, #2334 ) ;
#43761=VECTOR ( 'NONE', #1294, 1000.000000000000000 ) ;
#43763=EDGE_CURVE ( 'NONE', #9016, #65447, #24022, .T. ) ;
#43764=VERTEX_POINT ( 'NONE', #40289 ) ;
#43772=LINE ( 'NONE', #10545, #7543 ) ;
#43777=CARTESIAN_POINT ( 'NONE',  ( -8.250000000000001776, 7.250000000000000888, -26.00000000000001066 ) ) ;
#43780=DIRECTION ( 'NONE',  ( -0.000000000000000000, -0.000000000000000000, 1.000000000000000000 ) ) ;
#43789=CARTESIAN_POINT ( 'NONE',  ( -7.250000000000000888, 7.250000000000001776, -24.50000000000000000 ) ) ;
#43790=DIRECTION ( 'NONE',  ( 0.000000000000000000, 0.000000000000000000, 1.000000000000000000 ) ) ;
#43792=ORIENTED_EDGE ( 'NONE', *, *, #8159, .T. ) ;
#43796=CYLINDRICAL_SURFACE ( 'NONE', #46943, 0.1999999999999987899 ) ;
#43799=CARTESIAN_POINT ( 'NONE',  ( -7.250000000000001776, -7.249999999999998224, -14.50000000000000000 ) ) ;
#43801=CYLINDRICAL_SURFACE ( 'NONE', #3779, 1.000000000000000000 ) ;
#43803=ORIENTED_EDGE ( 'NONE', *, *, #48028, .F. ) ;
#43806=ORIENTED_EDGE ( 'NONE', *, *, #40717, .F. ) ;
#43812=DIRECTION ( 'NONE',  ( 0.000000000000000000, 0.000000000000000000, -1.000000000000000000 ) ) ;
#43816=CARTESIAN_POINT ( 'NONE',  ( 8.250000000000005329, -8.249999999999998224, -26.00000000000001066 ) ) ;
#43829=CARTESIAN_POINT ( 'NONE',  ( 8.250000000000005329, -7.249999999999998224, -26.00000000000001066 ) ) ;
#43832=FACE_OUTER_BOUND ( 'NONE', #50295, .T. ) ;
#43845=VECTOR ( 'NONE', #26868, 1000.000000000000000 ) ;
#43850=DIRECTION ( 'NONE',  ( -0.000000000000000000, -0.000000000000000000, -1.000000000000000000 ) ) ;
#43856=CARTESIAN_POINT ( 'NONE',  ( -8.750000000000001776, 7.250000000000000000, -30.00000000000001066 ) ) ;
#43860=CARTESIAN_POINT ( 'NONE',  ( 8.250000000000005329, -8.249999999999998224, -26.00000000000001066 ) ) ;
#43866=ORIENTED_EDGE ( 'NONE', *, *, #51363, .F. ) ;
#43871=CARTESIAN_POINT ( 'NONE',  ( -7.250000000000000888, 7.250000000000001776, -15.50000000000000000 ) ) ;
#43875=FACE_BOUND ( 'NONE', #10688, .T. ) ;
#43893=ORIENTED_EDGE ( 'NONE', *, *, #46386, .T. ) ;
#43896=LINE ( 'NONE', #27639, #50698 ) ;
#43897=PLANE ( 'NONE',  #6073 ) ;
#43903=EDGE_LOOP ( 'NONE', ( #53481, #14560, #39110, #68610, #46463, #33552, #40873, #2083 ) ) ;
#43905=ORIENTED_EDGE ( 'NONE', *, *, #1939, .T. ) ;
#43906=ORIENTED_EDGE ( 'NONE', *, *, #56272, .F. ) ;
#43907=ORIENTED_EDGE ( 'NONE', *, *, #18513, .T. ) ;
#43908=VECTOR ( 'NONE', #51265, 1000.000000000000000 ) ;
#43911=DIRECTION ( 'NONE',  ( 1.000000000000000000, 0.000000000000000000, -0.000000000000000000 ) ) ;
#43913=CARTESIAN_POINT ( 'NONE',  ( 0.000000000000000000, -7.449999999999998401, -24.00000000000000000 ) ) ;
#43916=ORIENTED_EDGE ( 'NONE', *, *, #62649, .F. ) ;
#43923=CARTESIAN_POINT ( 'NONE',  ( -7.250000000000001776, -7.249999999999998224, -18.00000000000000000 ) ) ;
#43926=EDGE_CURVE ( 'NONE', #32685, #57125, #32327, .T. ) ;
#43929=CARTESIAN_POINT ( 'NONE',  ( 7.250000000000005329, -7.449999999999998401, -13.50000000000000178 ) ) ;
#43932=CARTESIAN_POINT ( 'NONE',  ( -7.250000000000001776, -7.249999999999998224, -8.500000000000000000 ) ) ;
#43940=ORIENTED_EDGE ( 'NONE', *, *, #63563, .F. ) ;
#43946=CARTESIAN_POINT ( 'NONE',  ( 8.250000000000005329, 0.000000000000000000, -9.500000000000001776 ) ) ;
#43951=PLANE ( 'NONE',  #46127 ) ;
#43954=VECTOR ( 'NONE', #52920, 1000.000000000000000 ) ;
#43956=SURFACE_STYLE_FILL_AREA ( #18117 ) ;
#43966=LINE ( 'NONE', #38331, #21780 ) ;
#43973=LINE ( 'NONE', #65884, #10307 ) ;
#43981=DIRECTION ( 'NONE',  ( -1.000000000000000000, 0.000000000000000000, 0.000000000000000000 ) ) ;
#43984=ORIENTED_EDGE ( 'NONE', *, *, #41331, .F. ) ;
#43989=VECTOR ( 'NONE', #19796, 1000.000000000000000 ) ;
#43996=FACE_OUTER_BOUND ( 'NONE', #49872, .T. ) ;
#43998=EDGE_CURVE ( 'NONE', #11705, #43019, #5275, .T. ) ;
#44005=DIRECTION ( 'NONE',  ( 0.000000000000000000, 0.000000000000000000, 1.000000000000000000 ) ) ;
#44010=CARTESIAN_POINT ( 'NONE',  ( 9.750000000000001776, 9.690000000000001279, -4.250000000000000000 ) ) ;
#44013=CARTESIAN_POINT ( 'NONE',  ( 8.250000000000005329, -7.249999999999998224, -25.50000000000000355 ) ) ;
#44021=DIRECTION ( 'NONE',  ( -1.000000000000000000, 0.000000000000000000, 0.000000000000000000 ) ) ;
#44038=DIRECTION ( 'NONE',  ( -0.000000000000000000, 0.000000000000000000, -1.000000000000000000 ) ) ;
#44055=LINE ( 'NONE', #16849, #45086 ) ;
#44062=ADVANCED_FACE ( 'NONE', ( #5952 ), #27870, .F. ) ;
#44071=CARTESIAN_POINT ( 'NONE',  ( 0.000000000000000000, 0.000000000000000000, -26.00000000000001066 ) ) ;
#44076=EDGE_CURVE ( 'NONE', #32954, #62786, #21010, .T. ) ;
#44091=CARTESIAN_POINT ( 'NONE',  ( -9.750000000000000000, -9.690000000000001279, -4.250000000000000000 ) ) ;
#44099=CARTESIAN_POINT ( 'NONE',  ( 0.000000000000000000, 8.250000000000001776, -7.500000000000000000 ) ) ;
#44102=EDGE_CURVE ( 'NONE', #9064, #34571, #11927, .T. ) ;
#44108=CARTESIAN_POINT ( 'NONE',  ( 4.456444791733522252E-16, 7.450000000000002842, -19.50000000000000000 ) ) ;
#44112=CARTESIAN_POINT ( 'NONE',  ( 7.450000000000006395, 7.250000000000000888, -17.50000000000000000 ) ) ;
#44114=ORIENTED_EDGE ( 'NONE', *, *, #8445, .F. ) ;
#44118=VECTOR ( 'NONE', #35641, 1000.000000000000000 ) ;
#44127=CARTESIAN_POINT ( 'NONE',  ( 0.000000000000000000, 0.000000000000000000, -12.00000000000000000 ) ) ;
#44131=AXIS2_PLACEMENT_3D ( 'NONE', #67676, #29840, #40804 ) ;
#44140=EDGE_CURVE ( 'NONE', #60691, #31600, #61060, .T. ) ;
#44142=AXIS2_PLACEMENT_3D ( 'NONE', #30937, #10419, #52507 ) ;
#44148=EDGE_LOOP ( 'NONE', ( #32074, #64578, #29562, #6243 ) ) ;
#44151=ORIENTED_EDGE ( 'NONE', *, *, #1696, .F. ) ;
#44154=CARTESIAN_POINT ( 'NONE',  ( 8.250000000000005329, -8.249999999999998224, -26.00000000000001066 ) ) ;
#44168=VECTOR ( 'NONE', #48988, 1000.000000000000000 ) ;
#44173=ORIENTED_EDGE ( 'NONE', *, *, #59856, .T. ) ;
#44191=LINE ( 'NONE', #12009, #57230 ) ;
#44192=VECTOR ( 'NONE', #53140, 1000.000000000000000 ) ;
#44195=DIRECTION ( 'NONE',  ( -1.000000000000000000, 0.000000000000000000, 0.000000000000000000 ) ) ;
#44199=CARTESIAN_POINT ( 'NONE',  ( -8.250000000000001776, 0.000000000000000000, -22.00000000000000000 ) ) ;
#44204=LINE ( 'NONE', #65779, #31871 ) ;
#44208=CARTESIAN_POINT ( 'NONE',  ( -7.250000000000001776, -7.249999999999998224, -17.00000000000000000 ) ) ;
#44213=DIRECTION ( 'NONE',  ( -0.000000000000000000, 0.000000000000000000, 1.000000000000000000 ) ) ;
#44214=EDGE_CURVE ( 'NONE', #15601, #46187, #35585, .T. ) ;
#44215=CARTESIAN_POINT ( 'NONE',  ( -8.250000000000000000, 7.250000000000001776, -19.00000000000000000 ) ) ;
#44223=FACE_OUTER_BOUND ( 'NONE', #51050, .T. ) ;
#44224=CARTESIAN_POINT ( 'NONE',  ( 8.250000000000005329, -8.249999999999998224, -26.00000000000001066 ) ) ;
#44226=EDGE_CURVE ( 'NONE', #65577, #10775, #41187, .T. ) ;
#44251=CIRCLE ( 'NONE', #30582, 1.000000000000000000 ) ;
#44255=ORIENTED_EDGE ( 'NONE', *, *, #40635, .T. ) ;
#44265=CARTESIAN_POINT ( 'NONE',  ( 8.250000000000005329, 7.250000000000000888, -10.00000000000000000 ) ) ;
#44266=EDGE_CURVE ( 'NONE', #28651, #43043, #3429, .T. ) ;
#44267=ORIENTED_EDGE ( 'NONE', *, *, #62382, .F. ) ;
#44268=ORIENTED_EDGE ( 'NONE', *, *, #32836, .T. ) ;
#44293=FILL_AREA_STYLE_COLOUR ( '', #23161 ) ;
#44295=VERTEX_POINT ( 'NONE', #9430 ) ;
#44298=ORIENTED_EDGE ( 'NONE', *, *, #34476, .F. ) ;
#44299=VERTEX_POINT ( 'NONE', #4833 ) ;
#44309=CARTESIAN_POINT ( 'NONE',  ( 7.250000000000005329, -7.249999999999998224, -26.00000000000001066 ) ) ;
#44312=LINE ( 'NONE', #21377, #31650 ) ;
#44321=CIRCLE ( 'NONE', #68060, 1.000000000000000000 ) ;
#44322=ORIENTED_EDGE ( 'NONE', *, *, #29253, .T. ) ;
#44332=ORIENTED_EDGE ( 'NONE', *, *, #49581, .T. ) ;
#44346=ORIENTED_EDGE ( 'NONE', *, *, #11174, .F. ) ;
#44348=VECTOR ( 'NONE', #18291, 1000.000000000000000 ) ;
#44353=ORIENTED_EDGE ( 'NONE', *, *, #45452, .T. ) ;
#44362=DIRECTION ( 'NONE',  ( -1.000000000000000000, 0.000000000000000000, 0.000000000000000000 ) ) ;
#44363=AXIS2_PLACEMENT_3D ( 'NONE', #18468, #61600, #23087 ) ;
#44364=EDGE_CURVE ( 'NONE', #37823, #52634, #65283, .T. ) ;
#44365=CARTESIAN_POINT ( 'NONE',  ( 9.690000000000001279, 9.750000000000000000, -5.000000000000000000 ) ) ;
#44368=AXIS2_PLACEMENT_3D ( 'NONE', #18542, #42124, #58044 ) ;
#44381=CARTESIAN_POINT ( 'NONE',  ( 0.000000000000000000, -8.249999999999998224, -12.00000000000000000 ) ) ;
#44384=EDGE_LOOP ( 'NONE', ( #3347, #31910, #21135, #56018, #51878, #51995, #43984, #45334 ) ) ;
#44386=CYLINDRICAL_SURFACE ( 'NONE', #4487, 1.000000000000002665 ) ;
#44404=CYLINDRICAL_SURFACE ( 'NONE', #29337, 1.500000000000000444 ) ;
#44405=CARTESIAN_POINT ( 'NONE',  ( -8.250000000000001776, 0.000000000000000000, -25.50000000000000355 ) ) ;
#44412=EDGE_CURVE ( 'NONE', #55597, #66058, #58162, .T. ) ;
#44425=AXIS2_PLACEMENT_3D ( 'NONE', #68821, #21077, #20379 ) ;
#44437=ORIENTED_EDGE ( 'NONE', *, *, #63349, .T. ) ;
#44438=ORIENTED_EDGE ( 'NONE', *, *, #18939, .T. ) ;
#44439=ADVANCED_FACE ( 'NONE', ( #22820 ), #28459, .F. ) ;
#44440=DIRECTION ( 'NONE',  ( -1.000000000000000000, 0.000000000000000000, 0.000000000000000000 ) ) ;
#44454=LINE ( 'NONE', #54403, #5154 ) ;
#44465=CARTESIAN_POINT ( 'NONE',  ( 8.250000000000005329, -8.249999999999998224, -26.00000000000001066 ) ) ;
#44508=ORIENTED_EDGE ( 'NONE', *, *, #68938, .F. ) ;
#44527=LINE ( 'NONE', #61854, #35184 ) ;
#44529=AXIS2_PLACEMENT_3D ( 'NONE', #35965, #57530, #30316 ) ;
#44530=FACE_OUTER_BOUND ( 'NONE', #31537, .T. ) ;
#44542=VECTOR ( 'NONE', #51298, 1000.000000000000000 ) ;
#44552=DIRECTION ( 'NONE',  ( -1.000000000000000000, 1.794541526872559352E-16, 0.000000000000000000 ) ) ;
#44555=CARTESIAN_POINT ( 'NONE',  ( 0.000000000000000000, -7.449999999999998401, -14.50000000000000000 ) ) ;
#44563=LINE ( 'NONE', #54854, #40357 ) ;
#44566=DIRECTION ( 'NONE',  ( 0.000000000000000000, 0.000000000000000000, 1.000000000000000000 ) ) ;
#44570=ADVANCED_FACE ( 'NONE', ( #24570 ), #25627, .F. ) ;
#44572=EDGE_CURVE ( 'NONE', #35627, #34716, #61682, .T. ) ;
#44580=ORIENTED_EDGE ( 'NONE', *, *, #59715, .T. ) ;
#44583=VECTOR ( 'NONE', #4766, 1000.000000000000000 ) ;
#44585=ORIENTED_EDGE ( 'NONE', *, *, #5442, .F. ) ;
#44592=ORIENTED_EDGE ( 'NONE', *, *, #448, .T. ) ;
#44608=DIRECTION ( 'NONE',  ( -0.000000000000000000, -0.000000000000000000, 1.000000000000000000 ) ) ;
#44624=EDGE_CURVE ( 'NONE', #56702, #49332, #51437, .T. ) ;
#44632=CARTESIAN_POINT ( 'NONE',  ( 7.250000000000005329, -7.249999999999998224, -21.50000000000000000 ) ) ;
#44633=VECTOR ( 'NONE', #1921, 1000.000000000000000 ) ;
#44635=AXIS2_PLACEMENT_3D ( 'NONE', #68011, #47156, #63058 ) ;
#44642=DIRECTION ( 'NONE',  ( 0.000000000000000000, -0.000000000000000000, 1.000000000000000000 ) ) ;
#44646=ORIENTED_EDGE ( 'NONE', *, *, #54013, .F. ) ;
#44651=CARTESIAN_POINT ( 'NONE',  ( 0.000000000000000000, 8.250000000000001776, -11.50000000000000000 ) ) ;
#44658=VERTEX_POINT ( 'NONE', #32321 ) ;
#44665=ORIENTED_EDGE ( 'NONE', *, *, #35860, .T. ) ;
#44670=DIRECTION ( 'NONE',  ( 1.000000000000000000, 0.000000000000000000, 0.000000000000000000 ) ) ;
#44672=ORIENTED_EDGE ( 'NONE', *, *, #58050, .T. ) ;
#44678=CIRCLE ( 'NONE', #1786, 1.000000000000000000 ) ;
#44679=ORIENTED_EDGE ( 'NONE', *, *, #29063, .T. ) ;
#44682=VECTOR ( 'NONE', #33448, 1000.000000000000000 ) ;
#44683=DIRECTION ( 'NONE',  ( 0.000000000000000000, 0.000000000000000000, 1.000000000000000000 ) ) ;
#44687=CIRCLE ( 'NONE', #14220, 0.1999999999999996503 ) ;
#44688=AXIS2_PLACEMENT_3D ( 'NONE', #68487, #21437, #46901 ) ;
#44690=CARTESIAN_POINT ( 'NONE',  ( 8.250000000000005329, -8.249999999999998224, -26.00000000000001066 ) ) ;
#44691=DIRECTION ( 'NONE',  ( -1.000000000000000000, 0.000000000000000000, 0.000000000000000000 ) ) ;
#44693=AXIS2_PLACEMENT_3D ( 'NONE', #53954, #30979, #9772 ) ;
#44694=VECTOR ( 'NONE', #53490, 1000.000000000000000 ) ;
#44702=FACE_OUTER_BOUND ( 'NONE', #10884, .T. ) ;
#44703=AXIS2_PLACEMENT_3D ( 'NONE', #20053, #40908, #41618 ) ;
#44717=EDGE_CURVE ( 'NONE', #43043, #4784, #50271, .T. ) ;
#44718=FACE_OUTER_BOUND ( 'NONE', #52165, .T. ) ;
#44723=DIRECTION ( 'NONE',  ( 1.000000000000000000, 0.000000000000000000, 0.000000000000000000 ) ) ;
#44726=ORIENTED_EDGE ( 'NONE', *, *, #48254, .T. ) ;
#44727=FACE_OUTER_BOUND ( 'NONE', #1195, .T. ) ;
#44728=CARTESIAN_POINT ( 'NONE',  ( -8.250000000000001776, -7.249999999999998224, -26.00000000000001066 ) ) ;
#44733=CARTESIAN_POINT ( 'NONE',  ( 7.250000000000005329, -7.449999999999998401, -8.500000000000000000 ) ) ;
#44749=LINE ( 'NONE', #28492, #33992 ) ;
#44751=DIRECTION ( 'NONE',  ( 0.000000000000000000, 0.000000000000000000, -1.000000000000000000 ) ) ;
#44754=MANIFOLD_SOLID_BREP ( 'Cut-Extrude8', #60051 ) ;
#44763=ADVANCED_FACE ( 'NONE', ( #17089 ), #23436, .F. ) ;
#44770=ORIENTED_EDGE ( 'NONE', *, *, #47280, .T. ) ;
#44774=CARTESIAN_POINT ( 'NONE',  ( 7.450000000000006395, 7.250000000000000888, -13.50000000000000178 ) ) ;
#44775=AXIS2_PLACEMENT_3D ( 'NONE', #7405, #50556, #61859 ) ;
#44776=AXIS2_PLACEMENT_3D ( 'NONE', #26203, #4640, #64049 ) ;
#44784=EDGE_CURVE ( 'NONE', #35155, #36053, #33009, .T. ) ;
#44789=DIRECTION ( 'NONE',  ( 1.000000000000000000, -5.981805089575196197E-17, 0.000000000000000000 ) ) ;
#44792=CARTESIAN_POINT ( 'NONE',  ( 0.000000000000000000, -8.249999999999998224, -17.50000000000000000 ) ) ;
#44794=CARTESIAN_POINT ( 'NONE',  ( 7.250000000000005329, 7.250000000000000888, -8.000000000000000000 ) ) ;
#44798=DIRECTION ( 'NONE',  ( -1.000000000000000000, 0.000000000000000000, 0.000000000000000000 ) ) ;
#44808=LINE ( 'NONE', #35588, #24733 ) ;
#44810=DIRECTION ( 'NONE',  ( -1.000000000000000000, 0.000000000000000000, 0.000000000000000000 ) ) ;
#44821=CARTESIAN_POINT ( 'NONE',  ( -8.250000000000001776, -7.249999999999998224, -7.500000000000000000 ) ) ;
#44824=EDGE_CURVE ( 'NONE', #18463, #62655, #30034, .T. ) ;
#44828=EDGE_CURVE ( 'NONE', #59074, #40124, #7156, .T. ) ;
#44837=ADVANCED_FACE ( 'NONE', ( #14842 ), #31810, .T. ) ;
#44839=VECTOR ( 'NONE', #21716, 1000.000000000000000 ) ;
#44847=AXIS2_PLACEMENT_3D ( 'NONE', #39411, #1253, #22812 ) ;
#44848=VECTOR ( 'NONE', #23975, 1000.000000000000000 ) ;
#44853=ORIENTED_EDGE ( 'NONE', *, *, #47931, .F. ) ;
#44854=VERTEX_POINT ( 'NONE', #4587 ) ;
#44861=CARTESIAN_POINT ( 'NONE',  ( 7.450000000000006395, 7.250000000000000888, -7.500000000000000000 ) ) ;
#44864=VERTEX_POINT ( 'NONE', #66901 ) ;
#44866=CARTESIAN_POINT ( 'NONE',  ( -8.250000000000000000, 7.250000000000001776, -10.00000000000000000 ) ) ;
#44874=CARTESIAN_POINT ( 'NONE',  ( 8.250000000000005329, -7.249999999999998224, -22.50000000000000000 ) ) ;
#44876=EDGE_CURVE ( 'NONE', #53195, #60406, #25447, .T. ) ;
#44882=DIRECTION ( 'NONE',  ( 1.000000000000000000, -0.000000000000000000, 0.000000000000000000 ) ) ;
#44885=ORIENTED_EDGE ( 'NONE', *, *, #60518, .T. ) ;
#44896=CARTESIAN_POINT ( 'NONE',  ( -7.450000000000001954, 7.250000000000000000, -25.50000000000000355 ) ) ;
#44901=AXIS2_PLACEMENT_3D ( 'NONE', #35389, #44965, #2522 ) ;
#44903=ORIENTED_EDGE ( 'NONE', *, *, #50536, .T. ) ;
#44908=VECTOR ( 'NONE', #39875, 1000.000000000000000 ) ;
#44910=CARTESIAN_POINT ( 'NONE',  ( 7.749999999999998224, -7.348062532928000934, 0.000000000000000000 ) ) ;
#44914=LINE ( 'NONE', #11683, #14284 ) ;
#44915=DIRECTION ( 'NONE',  ( -0.000000000000000000, -0.000000000000000000, 1.000000000000000000 ) ) ;
#44919=CARTESIAN_POINT ( 'NONE',  ( 7.450000000000004619, -1.336933437520057563E-15, -23.50000000000000000 ) ) ;
#44923=ORIENTED_EDGE ( 'NONE', *, *, #57610, .T. ) ;
#44929=EDGE_LOOP ( 'NONE', ( #47829, #21323, #68328, #11550 ) ) ;
#44935=CARTESIAN_POINT ( 'NONE',  ( 0.000000000000000000, 0.000000000000000000, -25.50000000000000355 ) ) ;
#44939=LINE ( 'NONE', #40685, #65969 ) ;
#44940=CARTESIAN_POINT ( 'NONE',  ( -7.250000000000000888, -8.249999999999998224, -26.00000000000001066 ) ) ;
#44941=ORIENTED_EDGE ( 'NONE', *, *, #64488, .T. ) ;
#44943=FACE_OUTER_BOUND ( 'NONE', #61434, .T. ) ;
#44944=EDGE_LOOP ( 'NONE', ( #45169, #32237, #20866, #8922 ) ) ;
#44949=CIRCLE ( 'NONE', #29148, 1.000000000000000000 ) ;
#44951=DIRECTION ( 'NONE',  ( 0.000000000000000000, 0.000000000000000000, -1.000000000000000000 ) ) ;
#44955=AXIS2_PLACEMENT_3D ( 'NONE', #41304, #66772, #68179 ) ;
#44960=VERTEX_POINT ( 'NONE', #54754 ) ;
#44964=VECTOR ( 'NONE', #40467, 1000.000000000000000 ) ;
#44965=DIRECTION ( 'NONE',  ( 0.000000000000000000, 0.000000000000000000, 1.000000000000000000 ) ) ;
#44981=ORIENTED_EDGE ( 'NONE', *, *, #8953, .T. ) ;
#44990=PRESENTATION_STYLE_ASSIGNMENT (( #28728 ) ) ;
#44992=CARTESIAN_POINT ( 'NONE',  ( 8.250000000000005329, 8.250000000000001776, -26.00000000000001066 ) ) ;
#44996=ORIENTED_EDGE ( 'NONE', *, *, #59182, .T. ) ;
#44997=AXIS2_PLACEMENT_3D ( 'NONE', #69859, #33068, #41672 ) ;
#45000=ORIENTED_EDGE ( 'NONE', *, *, #63892, .T. ) ;
#45002=CARTESIAN_POINT ( 'NONE',  ( -7.250000000000000888, 7.450000000000003730, -23.50000000000000000 ) ) ;
#45013=EDGE_CURVE ( 'NONE', #50, #35620, #4931, .T. ) ;
#45015=FACE_OUTER_BOUND ( 'NONE', #39578, .T. ) ;
#45016=EDGE_CURVE ( 'NONE', #29071, #25480, #10927, .T. ) ;
#45023=ADVANCED_FACE ( 'NONE', ( #38160 ), #43796, .T. ) ;
#45036=VERTEX_POINT ( 'NONE', #2729 ) ;
#45047=VECTOR ( 'NONE', #12785, 1000.000000000000000 ) ;
#45049=CARTESIAN_POINT ( 'NONE',  ( 0.000000000000000000, -7.449999999999998401, -18.00000000000000000 ) ) ;
#45052=EDGE_LOOP ( 'NONE', ( #17799, #35575, #24692, #28980 ) ) ;
#45056=ADVANCED_FACE ( 'NONE', ( #45159 ), #23949, .F. ) ;
#45059=ORIENTED_EDGE ( 'NONE', *, *, #15841, .F. ) ;
#45063=AXIS2_PLACEMENT_3D ( 'NONE', #43860, #53794, #65436 ) ;
#45064=DIRECTION ( 'NONE',  ( -1.000000000000000000, 0.000000000000000000, 0.000000000000000000 ) ) ;
#45067=ORIENTED_EDGE ( 'NONE', *, *, #39307, .F. ) ;
#45070=DIRECTION ( 'NONE',  ( -0.000000000000000000, -0.000000000000000000, -1.000000000000000000 ) ) ;
#45072=VECTOR ( 'NONE', #30442, 1000.000000000000000 ) ;
#45074=CARTESIAN_POINT ( 'NONE',  ( -7.250000000000000000, -7.449999999999998401, -13.50000000000000178 ) ) ;
#45076=DIRECTION ( 'NONE',  ( -0.000000000000000000, -0.000000000000000000, 1.000000000000000000 ) ) ;
#45078=ORIENTED_EDGE ( 'NONE', *, *, #20985, .F. ) ;
#45082=CIRCLE ( 'NONE', #28140, 0.2000000000000005107 ) ;
#45086=VECTOR ( 'NONE', #17528, 1000.000000000000000 ) ;
#45088=ORIENTED_EDGE ( 'NONE', *, *, #54796, .T. ) ;
#45090=ADVANCED_FACE ( 'NONE', ( #6650 ), #50480, .T. ) ;
#45092=DIRECTION ( 'NONE',  ( -0.000000000000000000, -0.000000000000000000, 1.000000000000000000 ) ) ;
#45097=CIRCLE ( 'NONE', #20288, 0.2000000000000005107 ) ;
#45108=EDGE_CURVE ( 'NONE', #50347, #68595, #55783, .T. ) ;
#45114=EDGE_LOOP ( 'NONE', ( #1437, #60231, #31739, #34940, #65531, #29184, #46499, #66362 ) ) ;
#45117=CARTESIAN_POINT ( 'NONE',  ( 7.450000000000003730, -7.249999999999997335, -10.50000000000000000 ) ) ;
#45147=CARTESIAN_POINT ( 'NONE',  ( 0.000000000000000000, 0.000000000000000000, -15.50000000000000000 ) ) ;
#45149=AXIS2_PLACEMENT_3D ( 'NONE', #13869, #15284, #62652 ) ;
#45150=CARTESIAN_POINT ( 'NONE',  ( -9.690000000000001279, 8.750000000000000000, -7.000000000000000000 ) ) ;
#45153=VECTOR ( 'NONE', #8975, 1000.000000000000000 ) ;
#45154=FACE_OUTER_BOUND ( 'NONE', #32282, .T. ) ;
#45159=FACE_OUTER_BOUND ( 'NONE', #29550, .T. ) ;
#45162=CARTESIAN_POINT ( 'NONE',  ( 8.689999999999999503, -8.750000000000000000, -5.000000000000000000 ) ) ;
#45163=LINE ( 'NONE', #2390, #10195 ) ;
#45169=ORIENTED_EDGE ( 'NONE', *, *, #38830, .T. ) ;
#45185=EDGE_CURVE ( 'NONE', #28299, #54080, #8023, .T. ) ;
#45199=EDGE_CURVE ( 'NONE', #10277, #7833, #19683, .T. ) ;
#45207=ORIENTED_EDGE ( 'NONE', *, *, #32605, .F. ) ;
#45208=VECTOR ( 'NONE', #25873, 1000.000000000000000 ) ;
#45209=VECTOR ( 'NONE', #65905, 1000.000000000000000 ) ;
#45212=ORIENTED_EDGE ( 'NONE', *, *, #50221, .F. ) ;
#45223=ORIENTED_EDGE ( 'NONE', *, *, #48818, .F. ) ;
#45228=DIRECTION ( 'NONE',  ( 0.000000000000000000, 0.000000000000000000, -1.000000000000000000 ) ) ;
#45229=ORIENTED_EDGE ( 'NONE', *, *, #11274, .T. ) ;
#45233=CARTESIAN_POINT ( 'NONE',  ( -7.250000000000000000, -7.449999999999998401, -16.50000000000000000 ) ) ;
#45248=DIRECTION ( 'NONE',  ( 0.000000000000000000, 0.000000000000000000, 1.000000000000000000 ) ) ;
#45251=DIRECTION ( 'NONE',  ( -1.000000000000000000, 0.000000000000000000, 0.000000000000000000 ) ) ;
#45257=EDGE_CURVE ( 'NONE', #65777, #67217, #4154, .T. ) ;
#45263=DIRECTION ( 'NONE',  ( 1.000000000000000000, -5.981805089575194965E-17, 0.000000000000000000 ) ) ;
#45265=ORIENTED_EDGE ( 'NONE', *, *, #2596, .T. ) ;
#45266=ORIENTED_EDGE ( 'NONE', *, *, #30598, .F. ) ;
#45268=ORIENTED_EDGE ( 'NONE', *, *, #12454, .T. ) ;
#45270=LINE ( 'NONE', #2841, #7204 ) ;
#45271=EDGE_CURVE ( 'NONE', #25515, #48269, #9093, .T. ) ;
#45272=LINE ( 'NONE', #50595, #42138 ) ;
#45274=CARTESIAN_POINT ( 'NONE',  ( -7.250000000000001776, -7.249999999999998224, -24.00000000000000000 ) ) ;
#45277=CARTESIAN_POINT ( 'NONE',  ( -7.250000000000000888, -8.249999999999998224, -26.00000000000001066 ) ) ;
#45280=ORIENTED_EDGE ( 'NONE', *, *, #49480, .T. ) ;
#45285=CYLINDRICAL_SURFACE ( 'NONE', #56387, 0.2000000000000005107 ) ;
#45287=ORIENTED_EDGE ( 'NONE', *, *, #54110, .F. ) ;
#45291=CARTESIAN_POINT ( 'NONE',  ( 7.250000000000005329, -7.249999999999998224, -12.50000000000000000 ) ) ;
#45292=ADVANCED_FACE ( 'NONE', ( #35238 ), #41968, .T. ) ;
#45293=ORIENTED_EDGE ( 'NONE', *, *, #33032, .F. ) ;
#45294=AXIS2_PLACEMENT_3D ( 'NONE', #6150, #59556, #65882 ) ;
#45298=DIRECTION ( 'NONE',  ( 0.000000000000000000, 0.000000000000000000, -1.000000000000000000 ) ) ;
#45305=CIRCLE ( 'NONE', #14857, 0.9999999999999991118 ) ;
#45306=CARTESIAN_POINT ( 'NONE',  ( -7.450000000000001954, -7.249999999999998224, -19.50000000000000000 ) ) ;
#45311=EDGE_CURVE ( 'NONE', #51641, #16435, #63547, .T. ) ;
#45312=CARTESIAN_POINT ( 'NONE',  ( -7.250000000000000888, -8.249999999999998224, -24.00000000000000000 ) ) ;
#45313=DIRECTION ( 'NONE',  ( 1.000000000000000000, 0.000000000000000000, 0.000000000000000000 ) ) ;
#45315=LINE ( 'NONE', #6797, #45047 ) ;
#45319=DIRECTION ( 'NONE',  ( -0.000000000000000000, -0.000000000000000000, 1.000000000000000000 ) ) ;
#45331=AXIS2_PLACEMENT_3D ( 'NONE', #54135, #5695, #48830 ) ;
#45334=ORIENTED_EDGE ( 'NONE', *, *, #46099, .F. ) ;
#45346=ADVANCED_FACE ( 'NONE', ( #60957 ), #40801, .T. ) ;
#45348=DIRECTION ( 'NONE',  ( -1.794541526872559352E-16, -1.000000000000000000, 0.000000000000000000 ) ) ;
#45359=LINE ( 'NONE', #23101, #63554 ) ;
#45367=APPLICATION_CONTEXT ( 'automotive_design' ) ;
#45368=EDGE_CURVE ( 'NONE', #24527, #27762, #31227, .T. ) ;
#45371=( NAMED_UNIT ( * ) PLANE_ANGLE_UNIT ( ) SI_UNIT ( $, .RADIAN. ) );
#45398=DIRECTION ( 'NONE',  ( 0.000000000000000000, 0.000000000000000000, 1.000000000000000000 ) ) ;
#45414=ORIENTED_EDGE ( 'NONE', *, *, #35205, .F. ) ;
#45431=DIRECTION ( 'NONE',  ( 1.000000000000000000, 0.000000000000000000, 0.000000000000000000 ) ) ;
#45432=DIRECTION ( 'NONE',  ( -1.000000000000000000, 0.000000000000000000, 0.000000000000000000 ) ) ;
#45435=ORIENTED_EDGE ( 'NONE', *, *, #64390, .F. ) ;
#45436=DIRECTION ( 'NONE',  ( 0.000000000000000000, 0.000000000000000000, 1.000000000000000000 ) ) ;
#45437=ORIENTED_EDGE ( 'NONE', *, *, #62194, .T. ) ;
#45439=DIRECTION ( 'NONE',  ( 0.000000000000000000, -0.000000000000000000, 1.000000000000000000 ) ) ;
#45441=AXIS2_PLACEMENT_3D ( 'NONE', #20872, #25482, #47393 ) ;
#45442=FACE_OUTER_BOUND ( 'NONE', #49473, .T. ) ;
#45443=ORIENTED_EDGE ( 'NONE', *, *, #67727, .F. ) ;
#45447=DIRECTION ( 'NONE',  ( 0.000000000000000000, -0.000000000000000000, 1.000000000000000000 ) ) ;
#45451=FACE_BOUND ( 'NONE', #65524, .T. ) ;
#45452=EDGE_CURVE ( 'NONE', #58124, #6525, #69630, .T. ) ;
#45453=CIRCLE ( 'NONE', #29654, 0.1999999999999987899 ) ;
#45456=EDGE_CURVE ( 'NONE', #66058, #27819, #9685, .T. ) ;
#45458=AXIS2_PLACEMENT_3D ( 'NONE', #61688, #13255, #19603 ) ;
#45460=ORIENTED_EDGE ( 'NONE', *, *, #38878, .F. ) ;
#45469=CIRCLE ( 'NONE', #54543, 0.9999999999999991118 ) ;
#45471=EDGE_LOOP ( 'NONE', ( #43866, #31658, #48012, #39727, #2226, #52917, #11343, #67815 ) ) ;
#45472=EDGE_LOOP ( 'NONE', ( #62151, #30000, #48225, #68264 ) ) ;
#45473=AXIS2_PLACEMENT_3D ( 'NONE', #7862, #51006, #2565 ) ;
#45475=LINE ( 'NONE', #40528, #43717 ) ;
#45485=DIRECTION ( 'NONE',  ( -1.794541526872559352E-16, -1.000000000000000000, 0.000000000000000000 ) ) ;
#45486=EDGE_CURVE ( 'NONE', #68065, #32954, #9328, .T. ) ;
#45491=CARTESIAN_POINT ( 'NONE',  ( -7.250000000000001776, -7.249999999999998224, -16.00000000000000000 ) ) ;
#45504=DIRECTION ( 'NONE',  ( -0.000000000000000000, 0.000000000000000000, 1.000000000000000000 ) ) ;
#45505=VECTOR ( 'NONE', #5199, 1000.000000000000000 ) ;
#45508=DIRECTION ( 'NONE',  ( 1.000000000000000000, -0.000000000000000000, 0.000000000000000000 ) ) ;
#45509=ORIENTED_EDGE ( 'NONE', *, *, #40588, .F. ) ;
#45532=CARTESIAN_POINT ( 'NONE',  ( -7.250000000000000888, 7.450000000000003730, -20.50000000000000000 ) ) ;
#45533=FACE_OUTER_BOUND ( 'NONE', #11719, .T. ) ;
#45541=CARTESIAN_POINT ( 'NONE',  ( 7.250000000000005329, -7.249999999999998224, -9.500000000000001776 ) ) ;
#45550=CARTESIAN_POINT ( 'NONE',  ( -6.500000000000002665, 6.500000000000002665, -1.000000000000000000 ) ) ;
#45552=VECTOR ( 'NONE', #33801, 1000.000000000000000 ) ;
#45553=FACE_OUTER_BOUND ( 'NONE', #36708, .T. ) ;
#45558=VECTOR ( 'NONE', #8438, 1000.000000000000000 ) ;
#45566=EDGE_LOOP ( 'NONE', ( #60631, #58961, #29879, #1784 ) ) ;
#45569=DIRECTION ( 'NONE',  ( 1.000000000000000000, 0.000000000000000000, 0.000000000000000000 ) ) ;
#45573=CARTESIAN_POINT ( 'NONE',  ( 8.250000000000005329, 7.250000000000000888, -26.00000000000001066 ) ) ;
#45574=DIRECTION ( 'NONE',  ( 0.000000000000000000, 1.000000000000000000, 0.000000000000000000 ) ) ;
#45579=DIRECTION ( 'NONE',  ( 0.000000000000000000, 0.000000000000000000, 1.000000000000000000 ) ) ;
#45586=CARTESIAN_POINT ( 'NONE',  ( -2.500000000000000000, 0.000000000000000000, -29.90000000000000924 ) ) ;
#45593=DIRECTION ( 'NONE',  ( 0.000000000000000000, 0.000000000000000000, 1.000000000000000000 ) ) ;
#45596=CARTESIAN_POINT ( 'NONE',  ( 7.250000000000005329, -7.249999999999998224, -14.50000000000000000 ) ) ;
#45599=ADVANCED_FACE ( 'NONE', ( #42195 ), #34345, .T. ) ;
#45606=ORIENTED_EDGE ( 'NONE', *, *, #15984, .T. ) ;
#45607=DIRECTION ( 'NONE',  ( 0.000000000000000000, 0.000000000000000000, 1.000000000000000000 ) ) ;
#45612=CARTESIAN_POINT ( 'NONE',  ( 0.000000000000000000, 0.000000000000000000, -29.90000000000000924 ) ) ;
#45616=EDGE_LOOP ( 'NONE', ( #6669, #49309, #24740, #29261, #69816, #41868, #39058, #22778 ) ) ;
#45623=CARTESIAN_POINT ( 'NONE',  ( 7.749999999999998224, -7.348062532928000934, 0.000000000000000000 ) ) ;
#45625=CARTESIAN_POINT ( 'NONE',  ( 8.250000000000005329, 7.250000000000000888, -8.500000000000000000 ) ) ;
#45626=ORIENTED_EDGE ( 'NONE', *, *, #44572, .F. ) ;
#45627=CARTESIAN_POINT ( 'NONE',  ( 8.250000000000005329, 7.250000000000000888, -19.00000000000000000 ) ) ;
#45637=EDGE_CURVE ( 'NONE', #53899, #59557, #35758, .T. ) ;
#45649=LINE ( 'NONE', #60872, #53815 ) ;
#45658=VECTOR ( 'NONE', #58499, 1000.000000000000000 ) ;
#45660=DIRECTION ( 'NONE',  ( -0.000000000000000000, -0.000000000000000000, 1.000000000000000000 ) ) ;
#45662=DIRECTION ( 'NONE',  ( 0.000000000000000000, 0.000000000000000000, -1.000000000000000000 ) ) ;
#45664=VECTOR ( 'NONE', #24334, 1000.000000000000000 ) ;
#45665=DIRECTION ( 'NONE',  ( 0.000000000000000000, 0.000000000000000000, -1.000000000000000000 ) ) ;
#45672=EDGE_CURVE ( 'NONE', #1043, #29792, #34709, .T. ) ;
#45673=EDGE_CURVE ( 'NONE', #5244, #65035, #68294, .T. ) ;
#45674=CARTESIAN_POINT ( 'NONE',  ( 7.450000000000004619, -1.336933437520057563E-15, -16.00000000000000000 ) ) ;
#45685=DIRECTION ( 'NONE',  ( 0.000000000000000000, 0.000000000000000000, -1.000000000000000000 ) ) ;
#45687=FACE_OUTER_BOUND ( 'NONE', #6598, .T. ) ;
#45689=AXIS2_PLACEMENT_3D ( 'NONE', #62574, #57285, #34662 ) ;
#45690=ORIENTED_EDGE ( 'NONE', *, *, #35423, .F. ) ;
#45696=DIRECTION ( 'NONE',  ( 0.000000000000000000, -0.000000000000000000, 1.000000000000000000 ) ) ;
#45708=DIRECTION ( 'NONE',  ( 0.000000000000000000, 0.000000000000000000, -1.000000000000000000 ) ) ;
#45711=DIRECTION ( 'NONE',  ( 1.000000000000000000, 0.000000000000000000, 0.000000000000000000 ) ) ;
#45712=ORIENTED_EDGE ( 'NONE', *, *, #61052, .T. ) ;
#45714=ORIENTED_EDGE ( 'NONE', *, *, #6160, .T. ) ;
#45715=EDGE_CURVE ( 'NONE', #29937, #25227, #5336, .T. ) ;
#45726=AXIS2_PLACEMENT_3D ( 'NONE', #3074, #9419, #24982 ) ;
#45727=DIRECTION ( 'NONE',  ( -1.000000000000000000, 0.000000000000000000, 0.000000000000000000 ) ) ;
#45730=CARTESIAN_POINT ( 'NONE',  ( -7.250000000000000888, -8.249999999999998224, -20.00000000000000000 ) ) ;
#45733=DIRECTION ( 'NONE',  ( 0.000000000000000000, 0.000000000000000000, -1.000000000000000000 ) ) ;
#45737=ORIENTED_EDGE ( 'NONE', *, *, #52798, .F. ) ;
#45740=DIRECTION ( 'NONE',  ( 0.000000000000000000, 1.000000000000000000, 0.000000000000000000 ) ) ;
#45741=EDGE_CURVE ( 'NONE', #59830, #59223, #56969, .T. ) ;
#45745=ORIENTED_EDGE ( 'NONE', *, *, #69769, .F. ) ;
#45747=AXIS2_PLACEMENT_3D ( 'NONE', #6146, #27375, #49297 ) ;
#45748=DIRECTION ( 'NONE',  ( 0.000000000000000000, 0.000000000000000000, 1.000000000000000000 ) ) ;
#45754=ORIENTED_EDGE ( 'NONE', *, *, #29026, .F. ) ;
#45756=EDGE_CURVE ( 'NONE', #10719, #41033, #9251, .T. ) ;
#45758=VECTOR ( 'NONE', #28210, 1000.000000000000000 ) ;
#45760=CARTESIAN_POINT ( 'NONE',  ( 7.250000000000005329, -8.249999999999998224, -26.00000000000001066 ) ) ;
#45762=ADVANCED_FACE ( 'NONE', ( #42114, #19847, #4649, #14906, #63343, #68654 ), #52754, .T. ) ;
#45776=AXIS2_PLACEMENT_3D ( 'NONE', #37980, #59540, #9712 ) ;
#45790=LINE ( 'NONE', #55705, #27214 ) ;
#45793=ORIENTED_EDGE ( 'NONE', *, *, #40844, .F. ) ;
#45795=FACE_OUTER_BOUND ( 'NONE', #64011, .T. ) ;
#45797=VECTOR ( 'NONE', #41943, 1000.000000000000000 ) ;
#45798=DIRECTION ( 'NONE',  ( 1.000000000000000000, 0.000000000000000000, 0.000000000000000000 ) ) ;
#45801=AXIS2_PLACEMENT_3D ( 'NONE', #29874, #2309, #57449 ) ;
#45821=EDGE_CURVE ( 'NONE', #24533, #6680, #64398, .T. ) ;
#45824=CIRCLE ( 'NONE', #54888, 0.1999999999999987899 ) ;
#45825=CARTESIAN_POINT ( 'NONE',  ( 7.250000000000004441, 7.450000000000001954, -13.50000000000000178 ) ) ;
#45828=ORIENTED_EDGE ( 'NONE', *, *, #30931, .T. ) ;
#45829=CARTESIAN_POINT ( 'NONE',  ( -8.750000000000003553, -7.348062532927999158, -5.000000000000000000 ) ) ;
#45834=ORIENTED_EDGE ( 'NONE', *, *, #25342, .T. ) ;
#45844=EDGE_LOOP ( 'NONE', ( #50435, #64336, #63924, #56725 ) ) ;
#45845=CARTESIAN_POINT ( 'NONE',  ( 7.250000000000005329, 8.250000000000001776, -8.500000000000000000 ) ) ;
#45848=DIRECTION ( 'NONE',  ( 1.000000000000000000, 0.000000000000000000, 0.000000000000000000 ) ) ;
#45850=ORIENTED_EDGE ( 'NONE', *, *, #41819, .F. ) ;
#45879=CARTESIAN_POINT ( 'NONE',  ( -7.250000000000000888, 7.450000000000003730, -14.00000000000000000 ) ) ;
#45882=DIRECTION ( 'NONE',  ( 0.000000000000000000, 0.000000000000000000, 1.000000000000000000 ) ) ;
#45906=ADVANCED_FACE ( 'NONE', ( #38559 ), #741, .T. ) ;
#45918=AXIS2_PLACEMENT_3D ( 'NONE', #22775, #53934, #32355 ) ;
#45924=LINE ( 'NONE', #31064, #53819 ) ;
#45926=CARTESIAN_POINT ( 'NONE',  ( 8.250000000000005329, -8.249999999999998224, -26.00000000000001066 ) ) ;
#45938=DIRECTION ( 'NONE',  ( -1.000000000000000000, 0.000000000000000000, 0.000000000000000000 ) ) ;
#45944=FACE_OUTER_BOUND ( 'NONE', #9475, .T. ) ;
#45952=ADVANCED_FACE ( 'NONE', ( #44530 ), #28625, .F. ) ;
#45988=EDGE_LOOP ( 'NONE', ( #43376, #64583, #20274, #2126 ) ) ;
#45992=ORIENTED_EDGE ( 'NONE', *, *, #20540, .F. ) ;
#45993=CARTESIAN_POINT ( 'NONE',  ( 7.250000000000005329, 7.250000000000000888, -26.00000000000001066 ) ) ;
#46000=EDGE_CURVE ( 'NONE', #35196, #21984, #43161, .T. ) ;
#46004=CARTESIAN_POINT ( 'NONE',  ( 0.000000000000000000, 0.000000000000000000, -10.50000000000000000 ) ) ;
#46018=DIRECTION ( 'NONE',  ( 0.000000000000000000, 0.000000000000000000, 1.000000000000000000 ) ) ;
#46027=DIRECTION ( 'NONE',  ( 1.000000000000000000, -0.000000000000000000, 0.000000000000000000 ) ) ;
#46031=ORIENTED_EDGE ( 'NONE', *, *, #25034, .T. ) ;
#46046=ORIENTED_EDGE ( 'NONE', *, *, #62759, .T. ) ;
#46051=EDGE_LOOP ( 'NONE', ( #57012, #63583, #49232, #41919 ) ) ;
#46053=EDGE_LOOP ( 'NONE', ( #34468, #16683, #30005, #50650 ) ) ;
#46075=VERTEX_POINT ( 'NONE', #40283 ) ;
#46082=AXIS2_PLACEMENT_3D ( 'NONE', #36938, #8987, #57432 ) ;
#46088=ORIENTED_EDGE ( 'NONE', *, *, #69008, .F. ) ;
#46098=EDGE_CURVE ( 'NONE', #6078, #39010, #17773, .T. ) ;
#46099=EDGE_CURVE ( 'NONE', #44854, #54026, #4218, .T. ) ;
#46103=EDGE_LOOP ( 'NONE', ( #16330, #60742, #36503, #23230, #39800, #44981, #40073, #53471 ) ) ;
#46104=DIRECTION ( 'NONE',  ( 0.000000000000000000, -1.000000000000000000, 0.000000000000000000 ) ) ;
#46116=CARTESIAN_POINT ( 'NONE',  ( 7.250000000000004441, 7.450000000000001954, -18.00000000000000000 ) ) ;
#46124=VERTEX_POINT ( 'NONE', #28976 ) ;
#46126=DIRECTION ( 'NONE',  ( -0.000000000000000000, -0.000000000000000000, -1.000000000000000000 ) ) ;
#46127=AXIS2_PLACEMENT_3D ( 'NONE', #65530, #38656, #20999 ) ;
#46131=DIRECTION ( 'NONE',  ( 8.951101527228106186E-17, -1.000000000000000000, 0.000000000000000000 ) ) ;
#46148=EDGE_CURVE ( 'NONE', #37385, #13530, #56886, .T. ) ;
#46155=EDGE_LOOP ( 'NONE', ( #7816, #56158, #13439, #64777 ) ) ;
#46157=LINE ( 'NONE', #56416, #14845 ) ;
#46171=CARTESIAN_POINT ( 'NONE',  ( -7.250000000000001776, -7.249999999999998224, -30.00000000000001066 ) ) ;
#46185=CARTESIAN_POINT ( 'NONE',  ( 7.250000000000005329, 7.250000000000000888, -26.00000000000001066 ) ) ;
#46187=VERTEX_POINT ( 'NONE', #41680 ) ;
#46206=AXIS2_PLACEMENT_3D ( 'NONE', #1762, #32912, #6045 ) ;
#46211=DIRECTION ( 'NONE',  ( 0.000000000000000000, 0.000000000000000000, -1.000000000000000000 ) ) ;
#46215=CIRCLE ( 'NONE', #55270, 1.000000000000000000 ) ;
#46217=DIRECTION ( 'NONE',  ( -1.000000000000000000, 0.000000000000000000, 0.000000000000000000 ) ) ;
#46220=ORIENTED_EDGE ( 'NONE', *, *, #15762, .T. ) ;
#46221=AXIS2_PLACEMENT_3D ( 'NONE', #41170, #9355, #4759 ) ;
#46224=DIRECTION ( 'NONE',  ( -0.000000000000000000, -0.000000000000000000, -1.000000000000000000 ) ) ;
#46232=EDGE_CURVE ( 'NONE', #62306, #27562, #41329, .T. ) ;
#46234=LINE ( 'NONE', #12646, #69506 ) ;
#46246=DIRECTION ( 'NONE',  ( 0.000000000000000000, 1.000000000000000000, 0.000000000000000000 ) ) ;
#46252=ORIENTED_EDGE ( 'NONE', *, *, #40844, .T. ) ;
#46253=SHAPE_DEFINITION_REPRESENTATION ( #33517, #25847 ) ;
#46292=ORIENTED_EDGE ( 'NONE', *, *, #40732, .F. ) ;
#46303=EDGE_LOOP ( 'NONE', ( #51566, #24491, #25454, #52024 ) ) ;
#46318=AXIS2_PLACEMENT_3D ( 'NONE', #64589, #35967, #31016 ) ;
#46331=ORIENTED_EDGE ( 'NONE', *, *, #45637, .F. ) ;
#46337=ORIENTED_EDGE ( 'NONE', *, *, #57339, .F. ) ;
#46353=DIRECTION ( 'NONE',  ( 0.000000000000000000, 0.000000000000000000, 1.000000000000000000 ) ) ;
#46355=CARTESIAN_POINT ( 'NONE',  ( 7.450000000000006395, 7.250000000000000888, -25.00000000000000000 ) ) ;
#46356=CIRCLE ( 'NONE', #27143, 0.2000000000000005107 ) ;
#46366=CARTESIAN_POINT ( 'NONE',  ( -9.690000000000001279, -8.750000000000000000, -7.000000000000000000 ) ) ;
#46386=EDGE_CURVE ( 'NONE', #40313, #34713, #68559, .T. ) ;
#46393=ORIENTED_EDGE ( 'NONE', *, *, #54332, .T. ) ;
#46401=LINE ( 'NONE', #45002, #1555 ) ;
#46408=ORIENTED_EDGE ( 'NONE', *, *, #29063, .F. ) ;
#46411=CARTESIAN_POINT ( 'NONE',  ( 8.250000000000005329, -8.249999999999998224, -26.00000000000001066 ) ) ;
#46417=ORIENTED_EDGE ( 'NONE', *, *, #42449, .T. ) ;
#46421=CIRCLE ( 'NONE', #29591, 0.1999999999999987899 ) ;
#46427=VECTOR ( 'NONE', #67150, 1000.000000000000000 ) ;
#46438=CARTESIAN_POINT ( 'NONE',  ( -7.250000000000000888, 8.250000000000001776, -26.00000000000001066 ) ) ;
#46439=ADVANCED_FACE ( 'NONE', ( #6289 ), #27863, .T. ) ;
#46444=ORIENTED_EDGE ( 'NONE', *, *, #37147, .F. ) ;
#46449=CARTESIAN_POINT ( 'NONE',  ( -8.750000000000003553, 7.750000000000001776, 5.000000000000000000 ) ) ;
#46452=ORIENTED_EDGE ( 'NONE', *, *, #21922, .F. ) ;
#46455=DIRECTION ( 'NONE',  ( -0.000000000000000000, -0.000000000000000000, -1.000000000000000000 ) ) ;
#46459=DIRECTION ( 'NONE',  ( 1.000000000000000000, 0.000000000000000000, 0.000000000000000000 ) ) ;
#46463=ORIENTED_EDGE ( 'NONE', *, *, #11730, .F. ) ;
#46467=AXIS2_PLACEMENT_3D ( 'NONE', #28663, #23704, #18749 ) ;
#46472=ADVANCED_FACE ( 'NONE', ( #1662 ), #2024, .T. ) ;
#46473=ADVANCED_FACE ( 'NONE', ( #61766 ), #61050, .F. ) ;
#46478=ADVANCED_FACE ( 'NONE', ( #67435 ), #18981, .T. ) ;
#46488=EDGE_CURVE ( 'NONE', #10769, #31506, #34717, .T. ) ;
#46491=DIRECTION ( 'NONE',  ( 0.000000000000000000, 0.000000000000000000, 1.000000000000000000 ) ) ;
#46497=VERTEX_POINT ( 'NONE', #28536 ) ;
#46499=ORIENTED_EDGE ( 'NONE', *, *, #45673, .F. ) ;
#46502=CARTESIAN_POINT ( 'NONE',  ( 7.250000000000005329, -7.249999999999998224, -14.50000000000000000 ) ) ;
#46506=LINE ( 'NONE', #18584, #61870 ) ;
#46508=VERTEX_POINT ( 'NONE', #35221 ) ;
#46517=EDGE_LOOP ( 'NONE', ( #23348, #40930, #33466, #11483, #44726, #26911, #42613, #28358 ) ) ;
#46522=CIRCLE ( 'NONE', #50904, 0.2000000000000005107 ) ;
#46529=DIRECTION ( 'NONE',  ( 0.000000000000000000, 0.000000000000000000, 1.000000000000000000 ) ) ;
#46532=CARTESIAN_POINT ( 'NONE',  ( 8.250000000000005329, 8.250000000000001776, -26.00000000000001066 ) ) ;
#46547=DIRECTION ( 'NONE',  ( -8.951101527228104953E-17, 1.000000000000000000, 0.000000000000000000 ) ) ;
#46551=EDGE_CURVE ( 'NONE', #37385, #6182, #19326, .T. ) ;
#46562=CARTESIAN_POINT ( 'NONE',  ( 7.250000000000005329, 8.250000000000001776, -26.00000000000001066 ) ) ;
#46569=AXIS2_PLACEMENT_3D ( 'NONE', #4440, #63472, #19621 ) ;
#46570=ORIENTED_EDGE ( 'NONE', *, *, #57864, .F. ) ;
#46588=AXIS2_PLACEMENT_3D ( 'NONE', #67930, #30095, #46704 ) ;
#46589=ORIENTED_EDGE ( 'NONE', *, *, #67049, .F. ) ;
#46614=EDGE_CURVE ( 'NONE', #41478, #65577, #57158, .T. ) ;
#46616=ORIENTED_EDGE ( 'NONE', *, *, #2810, .F. ) ;
#46622=EDGE_LOOP ( 'NONE', ( #40398, #36783, #34588, #26082 ) ) ;
#46624=VERTEX_POINT ( 'NONE', #3766 ) ;
#46626=AXIS2_PLACEMENT_3D ( 'NONE', #64580, #37710, #27094 ) ;
#46627=CARTESIAN_POINT ( 'NONE',  ( 8.689999999999999503, 9.750000000000001776, -7.000000000000000000 ) ) ;
#46631=CARTESIAN_POINT ( 'NONE',  ( 7.450000000000006395, 7.250000000000000888, -25.50000000000000355 ) ) ;
#46634=FACE_OUTER_BOUND ( 'NONE', #18229, .T. ) ;
#46637=ORIENTED_EDGE ( 'NONE', *, *, #36591, .T. ) ;
#46641=DIRECTION ( 'NONE',  ( -1.000000000000000000, 0.000000000000000000, 0.000000000000000000 ) ) ;
#46644=CARTESIAN_POINT ( 'NONE',  ( -7.450000000000001954, 7.250000000000000000, -25.50000000000000355 ) ) ;
#46654=FACE_OUTER_BOUND ( 'NONE', #36006, .T. ) ;
#46657=DIRECTION ( 'NONE',  ( -1.000000000000000000, 0.000000000000000000, 0.000000000000000000 ) ) ;
#46658=ADVANCED_FACE ( 'NONE', ( #31369 ), #63873, .T. ) ;
#46661=LINE ( 'NONE', #68233, #43908 ) ;
#46664=ORIENTED_EDGE ( 'NONE', *, *, #7987, .T. ) ;
#46671=CYLINDRICAL_SURFACE ( 'NONE', #61142, 1.000000000000000000 ) ;
#46678=CARTESIAN_POINT ( 'NONE',  ( -9.690000000000001279, 9.750000000000000000, -4.250000000000000000 ) ) ;
#46685=CIRCLE ( 'NONE', #34245, 0.2000000000000005107 ) ;
#46692=AXIS2_PLACEMENT_3D ( 'NONE', #6450, #31934, #455 ) ;
#46704=DIRECTION ( 'NONE',  ( 1.000000000000000000, 0.000000000000000000, 0.000000000000000000 ) ) ;
#46709=LINE ( 'NONE', #30805, #41874 ) ;
#46713=DIRECTION ( 'NONE',  ( 0.000000000000000000, 0.000000000000000000, -1.000000000000000000 ) ) ;
#46718=CARTESIAN_POINT ( 'NONE',  ( 8.250000000000005329, 0.000000000000000000, -21.00000000000000000 ) ) ;
#46729=DIRECTION ( 'NONE',  ( -0.000000000000000000, -0.000000000000000000, 1.000000000000000000 ) ) ;
#46732=FACE_OUTER_BOUND ( 'NONE', #33480, .T. ) ;
#46735=CARTESIAN_POINT ( 'NONE',  ( -7.250000000000000888, -8.249999999999998224, -26.00000000000001066 ) ) ;
#46746=AXIS2_PLACEMENT_3D ( 'NONE', #22356, #17038, #38608 ) ;
#46748=CARTESIAN_POINT ( 'NONE',  ( 7.250000000000004441, 7.450000000000001954, -16.00000000000000000 ) ) ;
#46759=CARTESIAN_POINT ( 'NONE',  ( 7.250000000000005329, -7.249999999999998224, -19.50000000000000000 ) ) ;
#46763=LINE ( 'NONE', #17372, #5022 ) ;
#46773=PLANE ( 'NONE',  #7149 ) ;
#46774=ORIENTED_EDGE ( 'NONE', *, *, #68093, .F. ) ;
#46791=EDGE_LOOP ( 'NONE', ( #19348, #22184, #25326, #34201 ) ) ;
#46794=FACE_BOUND ( 'NONE', #3719, .T. ) ;
#46797=CARTESIAN_POINT ( 'NONE',  ( 4.456444791733522252E-16, 7.450000000000002842, -10.00000000000000000 ) ) ;
#46802=CARTESIAN_POINT ( 'NONE',  ( 8.250000000000005329, -8.249999999999998224, -26.00000000000001066 ) ) ;
#46804=CARTESIAN_POINT ( 'NONE',  ( -7.250000000000001776, -7.249999999999998224, -15.00000000000000000 ) ) ;
#46813=LINE ( 'NONE', #35864, #56229 ) ;
#46825=PLANE ( 'NONE',  #19580 ) ;
#46831=EDGE_LOOP ( 'NONE', ( #6309, #43122, #63324, #6166 ) ) ;
#46833=CARTESIAN_POINT ( 'NONE',  ( 7.250000000000005329, -7.449999999999998401, -21.50000000000000000 ) ) ;
#46839=EDGE_LOOP ( 'NONE', ( #39030, #10102, #1108, #18833 ) ) ;
#46843=CYLINDRICAL_SURFACE ( 'NONE', #41360, 1.000000000000000000 ) ;
#46844=VECTOR ( 'NONE', #46529, 1000.000000000000000 ) ;
#46852=ORIENTED_EDGE ( 'NONE', *, *, #11138, .F. ) ;
#46859=ORIENTED_EDGE ( 'NONE', *, *, #26053, .T. ) ;
#46862=ORIENTED_EDGE ( 'NONE', *, *, #4386, .T. ) ;
#46867=EDGE_CURVE ( 'NONE', #41582, #13987, #2290, .T. ) ;
#46870=DIRECTION ( 'NONE',  ( 0.000000000000000000, -1.000000000000000000, 0.000000000000000000 ) ) ;
#46871=AXIS2_PLACEMENT_3D ( 'NONE', #54992, #5149, #26719 ) ;
#46877=ORIENTED_EDGE ( 'NONE', *, *, #41480, .T. ) ;
#46881=DIRECTION ( 'NONE',  ( 1.000000000000000000, -0.000000000000000000, 0.000000000000000000 ) ) ;
#46882=AXIS2_PLACEMENT_3D ( 'NONE', #54538, #6093, #59139 ) ;
#46897=VERTEX_POINT ( 'NONE', #1255 ) ;
#46898=CARTESIAN_POINT ( 'NONE',  ( -7.450000000000001954, 0.000000000000000000, -15.50000000000000000 ) ) ;
#46901=DIRECTION ( 'NONE',  ( -1.000000000000000000, 0.000000000000000000, 0.000000000000000000 ) ) ;
#46925=ORIENTED_EDGE ( 'NONE', *, *, #25254, .T. ) ;
#46929=VECTOR ( 'NONE', #29027, 1000.000000000000000 ) ;
#46930=EDGE_CURVE ( 'NONE', #18594, #36419, #39319, .T. ) ;
#46931=CARTESIAN_POINT ( 'NONE',  ( 4.456444791733522252E-16, 7.450000000000002842, -22.50000000000000000 ) ) ;
#46933=AXIS2_PLACEMENT_3D ( 'NONE', #52635, #42709, #4199 ) ;
#46937=EDGE_LOOP ( 'NONE', ( #66508, #23799, #68517, #13813 ) ) ;
#46942=CARTESIAN_POINT ( 'NONE',  ( 7.450000000000006395, 7.250000000000000888, -16.00000000000000000 ) ) ;
#46943=AXIS2_PLACEMENT_3D ( 'NONE', #668, #22238, #11260 ) ;
#46946=VECTOR ( 'NONE', #28208, 1000.000000000000000 ) ;
#46956=DIRECTION ( 'NONE',  ( 0.000000000000000000, 1.000000000000000000, 0.000000000000000000 ) ) ;
#46960=DIRECTION ( 'NONE',  ( 0.000000000000000000, 1.000000000000000000, -0.000000000000000000 ) ) ;
#46961=EDGE_CURVE ( 'NONE', #67142, #64098, #61320, .T. ) ;
#46964=VERTEX_POINT ( 'NONE', #18543 ) ;
#46987=AXIS2_PLACEMENT_3D ( 'NONE', #68465, #41938, #4472 ) ;
#46989=CIRCLE ( 'NONE', #30075, 0.1999999999999987899 ) ;
#47001=CARTESIAN_POINT ( 'NONE',  ( 0.000000000000000000, 0.000000000000000000, -22.50000000000000000 ) ) ;
#47005=VERTEX_POINT ( 'NONE', #4409 ) ;
#47007=CARTESIAN_POINT ( 'NONE',  ( 8.750000000000000000, -7.348062532928000934, 5.000000000000000000 ) ) ;
#47009=DIRECTION ( 'NONE',  ( 0.000000000000000000, 0.000000000000000000, 1.000000000000000000 ) ) ;
#47010=ADVANCED_FACE ( 'NONE', ( #25972 ), #63090, .F. ) ;
#47028=DIRECTION ( 'NONE',  ( 0.000000000000000000, 0.000000000000000000, -1.000000000000000000 ) ) ;
#47040=EDGE_CURVE ( 'NONE', #47719, #8412, #61882, .T. ) ;
#47052=EDGE_CURVE ( 'NONE', #41205, #62492, #62730, .T. ) ;
#47063=DIRECTION ( 'NONE',  ( -1.000000000000000000, 0.000000000000000000, 0.000000000000000000 ) ) ;
#47064=ORIENTED_EDGE ( 'NONE', *, *, #40719, .F. ) ;
#47070=EDGE_CURVE ( 'NONE', #190, #23182, #46813, .T. ) ;
#47075=VERTEX_POINT ( 'NONE', #10054 ) ;
#47081=CARTESIAN_POINT ( 'NONE',  ( 9.690000000000001279, -9.690000000000001279, 0.000000000000000000 ) ) ;
#47083=CARTESIAN_POINT ( 'NONE',  ( -7.450000000000001954, 7.250000000000000000, -21.50000000000000000 ) ) ;
#47085=VECTOR ( 'NONE', #29303, 1000.000000000000000 ) ;
#47094=FACE_OUTER_BOUND ( 'NONE', #29134, .T. ) ;
#47096=CIRCLE ( 'NONE', #23364, 0.8100000000000017186 ) ;
#47104=CARTESIAN_POINT ( 'NONE',  ( 7.250000000000005329, -8.249999999999998224, -17.00000000000000000 ) ) ;
#47110=CARTESIAN_POINT ( 'NONE',  ( -7.250000000000000000, -7.449999999999998401, -7.000000000000000000 ) ) ;
#47112=EDGE_CURVE ( 'NONE', #40446, #997, #64183, .T. ) ;
#47128=CARTESIAN_POINT ( 'NONE',  ( -7.250000000000000888, 7.250000000000001776, -16.50000000000000000 ) ) ;
#47131=LINE ( 'NONE', #59130, #37866 ) ;
#47142=CARTESIAN_POINT ( 'NONE',  ( -8.689999999999999503, -9.750000000000001776, -7.000000000000000000 ) ) ;
#47145=VECTOR ( 'NONE', #59547, 1000.000000000000000 ) ;
#47149=ORIENTED_EDGE ( 'NONE', *, *, #63819, .F. ) ;
#47151=CARTESIAN_POINT ( 'NONE',  ( 0.000000000000000000, -8.249999999999998224, -10.00000000000000000 ) ) ;
#47154=ORIENTED_EDGE ( 'NONE', *, *, #37659, .F. ) ;
#47156=DIRECTION ( 'NONE',  ( -1.000000000000000000, 0.000000000000000000, 0.000000000000000000 ) ) ;
#47162=VERTEX_POINT ( 'NONE', #65198 ) ;
#47165=VECTOR ( 'NONE', #7664, 1000.000000000000000 ) ;
#47172=DIRECTION ( 'NONE',  ( -1.000000000000000000, 1.794541526872559352E-16, 0.000000000000000000 ) ) ;
#47184=VERTEX_POINT ( 'NONE', #22403 ) ;
#47190=CIRCLE ( 'NONE', #62982, 1.000000000000000000 ) ;
#47191=CYLINDRICAL_SURFACE ( 'NONE', #8974, 1.000000000000000000 ) ;
#47194=VECTOR ( 'NONE', #32901, 1000.000000000000000 ) ;
#47208=ADVANCED_FACE ( 'NONE', ( #27696 ), #43951, .F. ) ;
#47217=DIRECTION ( 'NONE',  ( -0.000000000000000000, -0.000000000000000000, 1.000000000000000000 ) ) ;
#47220=DIRECTION ( 'NONE',  ( 0.000000000000000000, 0.000000000000000000, -1.000000000000000000 ) ) ;
#47228=CYLINDRICAL_SURFACE ( 'NONE', #69814, 1.000000000000000000 ) ;
#47229=EDGE_LOOP ( 'NONE', ( #1064, #13711, #42101, #19792, #6764, #49489, #64174, #39106 ) ) ;
#47231=DIRECTION ( 'NONE',  ( 0.000000000000000000, 0.000000000000000000, 1.000000000000000000 ) ) ;
#47240=ORIENTED_EDGE ( 'NONE', *, *, #60072, .T. ) ;
#47244=CARTESIAN_POINT ( 'NONE',  ( 9.189999999999999503, 9.750000000000000000, -5.000000000000000000 ) ) ;
#47249=VECTOR ( 'NONE', #13386, 1000.000000000000000 ) ;
#47255=CARTESIAN_POINT ( 'NONE',  ( 7.450000000000004619, -1.336933437520057563E-15, -14.50000000000000000 ) ) ;
#47259=CARTESIAN_POINT ( 'NONE',  ( 7.250000000000005329, 7.250000000000000888, -24.50000000000000000 ) ) ;
#47261=CARTESIAN_POINT ( 'NONE',  ( 0.000000000000000000, 0.000000000000000000, -29.90000000000000924 ) ) ;
#47269=CARTESIAN_POINT ( 'NONE',  ( -7.450000000000001954, 0.000000000000000000, -7.500000000000000000 ) ) ;
#47272=CYLINDRICAL_SURFACE ( 'NONE', #52205, 1.000000000000000000 ) ;
#47280=EDGE_CURVE ( 'NONE', #16692, #9544, #65333, .T. ) ;
#47281=DIRECTION ( 'NONE',  ( 0.000000000000000000, 0.000000000000000000, 1.000000000000000000 ) ) ;
#47288=DIRECTION ( 'NONE',  ( 0.000000000000000000, 1.000000000000000000, 0.000000000000000000 ) ) ;
#47293=ORIENTED_EDGE ( 'NONE', *, *, #69567, .T. ) ;
#47294=DIRECTION ( 'NONE',  ( 0.000000000000000000, 1.000000000000000000, 0.000000000000000000 ) ) ;
#47295=VERTEX_POINT ( 'NONE', #34359 ) ;
#47297=PLANE ( 'NONE',  #62216 ) ;
#47298=ORIENTED_EDGE ( 'NONE', *, *, #2810, .T. ) ;
#47301=CARTESIAN_POINT ( 'NONE',  ( 7.250000000000005329, 7.250000000000000888, -22.00000000000000000 ) ) ;
#47317=EDGE_LOOP ( 'NONE', ( #11112, #31880, #30970, #44332 ) ) ;
#47318=VERTEX_POINT ( 'NONE', #18817 ) ;
#47322=DIRECTION ( 'NONE',  ( 0.000000000000000000, 0.000000000000000000, -1.000000000000000000 ) ) ;
#47325=AXIS2_PLACEMENT_3D ( 'NONE', #67731, #44751, #56765 ) ;
#47341=CIRCLE ( 'NONE', #56367, 0.1999999999999987899 ) ;
#47348=CARTESIAN_POINT ( 'NONE',  ( 8.250000000000005329, -7.249999999999998224, -7.500000000000000000 ) ) ;
#47350=DIRECTION ( 'NONE',  ( 0.000000000000000000, 0.000000000000000000, -1.000000000000000000 ) ) ;
#47356=CARTESIAN_POINT ( 'NONE',  ( -7.450000000000001954, -7.249999999999998224, -25.50000000000000355 ) ) ;
#47363=LINE ( 'NONE', #29690, #29713 ) ;
#47371=CARTESIAN_POINT ( 'NONE',  ( 7.250000000000005329, 7.250000000000000888, -8.000000000000000000 ) ) ;
#47373=DIRECTION ( 'NONE',  ( -0.000000000000000000, 0.000000000000000000, -1.000000000000000000 ) ) ;
#47380=EDGE_CURVE ( 'NONE', #7833, #57470, #30335, .T. ) ;
#47384=CARTESIAN_POINT ( 'NONE',  ( 9.690000000000001279, 8.750000000000000000, -5.000000000000000000 ) ) ;
#47393=DIRECTION ( 'NONE',  ( -1.000000000000000000, 2.602085213965213008E-15, 0.000000000000000000 ) ) ;
#47394=ORIENTED_EDGE ( 'NONE', *, *, #11574, .T. ) ;
#47395=ORIENTED_EDGE ( 'NONE', *, *, #15123, .T. ) ;
#47396=VECTOR ( 'NONE', #55532, 1000.000000000000000 ) ;
#47397=DIRECTION ( 'NONE',  ( -5.981805089575196197E-17, -1.000000000000000000, 0.000000000000000000 ) ) ;
#47404=DIRECTION ( 'NONE',  ( -2.312964634635740689E-15, 1.000000000000000000, 0.000000000000000000 ) ) ;
#47405=ORIENTED_EDGE ( 'NONE', *, *, #31290, .F. ) ;
#47409=ORIENTED_EDGE ( 'NONE', *, *, #66618, .T. ) ;
#47413=ORIENTED_EDGE ( 'NONE', *, *, #47975, .F. ) ;
#47422=EDGE_CURVE ( 'NONE', #2415, #13815, #12244, .T. ) ;
#47424=ORIENTED_EDGE ( 'NONE', *, *, #41007, .T. ) ;
#47437=ORIENTED_EDGE ( 'NONE', *, *, #24940, .F. ) ;
#47438=DIRECTION ( 'NONE',  ( 1.000000000000000000, -0.000000000000000000, 0.000000000000000000 ) ) ;
#47440=EDGE_CURVE ( 'NONE', #59557, #7845, #15547, .T. ) ;
#47441=ORIENTED_EDGE ( 'NONE', *, *, #57738, .T. ) ;
#47443=DIRECTION ( 'NONE',  ( 0.000000000000000000, 0.000000000000000000, 1.000000000000000000 ) ) ;
#47445=CIRCLE ( 'NONE', #42907, 1.000000000000000000 ) ;
#47450=ORIENTED_EDGE ( 'NONE', *, *, #44784, .T. ) ;
#47463=EDGE_LOOP ( 'NONE', ( #2420, #34794, #43803, #706 ) ) ;
#47470=FACE_OUTER_BOUND ( 'NONE', #44148, .T. ) ;
#47471=CARTESIAN_POINT ( 'NONE',  ( -8.250000000000001776, -7.249999999999998224, -15.50000000000000000 ) ) ;
#47473=ORIENTED_EDGE ( 'NONE', *, *, #51436, .T. ) ;
#47489=VERTEX_POINT ( 'NONE', #26147 ) ;
#47493=CIRCLE ( 'NONE', #3483, 0.1999999999999987899 ) ;
#47500=ORIENTED_EDGE ( 'NONE', *, *, #45016, .F. ) ;
#47506=ORIENTED_EDGE ( 'NONE', *, *, #633, .F. ) ;
#47514=DIRECTION ( 'NONE',  ( 0.000000000000000000, 1.000000000000000000, 0.000000000000000000 ) ) ;
#47539=DIRECTION ( 'NONE',  ( 1.000000000000000000, 0.000000000000000000, -0.000000000000000000 ) ) ;
#47541=DIRECTION ( 'NONE',  ( -1.000000000000000000, 0.000000000000000000, 0.000000000000000000 ) ) ;
#47547=CIRCLE ( 'NONE', #31759, 0.1999999999999996503 ) ;
#47552=ORIENTED_EDGE ( 'NONE', *, *, #26139, .F. ) ;
#47556=ADVANCED_FACE ( 'NONE', ( #22231 ), #33171, .T. ) ;
#47564=VERTEX_POINT ( 'NONE', #65016 ) ;
#47566=DIRECTION ( 'NONE',  ( 1.000000000000000000, 0.000000000000000000, 0.000000000000000000 ) ) ;
#47567=CARTESIAN_POINT ( 'NONE',  ( -8.250000000000001776, 7.250000000000000888, -20.50000000000000000 ) ) ;
#47570=ORIENTED_EDGE ( 'NONE', *, *, #63074, .F. ) ;
#47597=DIRECTION ( 'NONE',  ( 1.000000000000000000, 0.000000000000000000, 0.000000000000000000 ) ) ;
#47603=AXIS2_PLACEMENT_3D ( 'NONE', #5093, #27007, #16050 ) ;
#47608=ORIENTED_EDGE ( 'NONE', *, *, #69417, .F. ) ;
#47617=CARTESIAN_POINT ( 'NONE',  ( 0.000000000000000000, -7.449999999999998401, -12.00000000000000000 ) ) ;
#47643=ORIENTED_EDGE ( 'NONE', *, *, #13240, .F. ) ;
#47644=DIRECTION ( 'NONE',  ( -1.000000000000000000, 0.000000000000000000, 0.000000000000000000 ) ) ;
#47654=ORIENTED_EDGE ( 'NONE', *, *, #11575, .T. ) ;
#47663=ADVANCED_FACE ( 'NONE', ( #54407 ), #54062, .T. ) ;
#47667=ORIENTED_EDGE ( 'NONE', *, *, #30029, .T. ) ;
#47674=DIRECTION ( 'NONE',  ( 0.000000000000000000, 0.000000000000000000, 1.000000000000000000 ) ) ;
#47679=ORIENTED_EDGE ( 'NONE', *, *, #56385, .T. ) ;
#47686=ORIENTED_EDGE ( 'NONE', *, *, #64880, .F. ) ;
#47691=CIRCLE ( 'NONE', #64644, 0.9999999999999991118 ) ;
#47715=ORIENTED_EDGE ( 'NONE', *, *, #26365, .F. ) ;
#47719=VERTEX_POINT ( 'NONE', #39502 ) ;
#47725=CARTESIAN_POINT ( 'NONE',  ( -7.750000000000001776, 7.750000000000001776, -5.000000000000000000 ) ) ;
#47727=ORIENTED_EDGE ( 'NONE', *, *, #41543, .T. ) ;
#47728=VERTEX_POINT ( 'NONE', #19334 ) ;
#47729=DIRECTION ( 'NONE',  ( 1.000000000000000000, 0.000000000000000000, 0.000000000000000000 ) ) ;
#47740=ORIENTED_EDGE ( 'NONE', *, *, #45016, .T. ) ;
#47741=CARTESIAN_POINT ( 'NONE',  ( 8.250000000000005329, 7.250000000000000888, -14.50000000000000000 ) ) ;
#47743=EDGE_LOOP ( 'NONE', ( #60873, #19095, #43227, #64887 ) ) ;
#47753=EDGE_LOOP ( 'NONE', ( #3834, #31287, #50123, #42770 ) ) ;
#47754=LINE ( 'NONE', #15603, #18361 ) ;
#47756=CARTESIAN_POINT ( 'NONE',  ( 0.000000000000000000, 0.000000000000000000, -29.90000000000000924 ) ) ;
#47771=CARTESIAN_POINT ( 'NONE',  ( 7.250000000000005329, -8.249999999999998224, -26.00000000000001066 ) ) ;
#47772=DIRECTION ( 'NONE',  ( 0.000000000000000000, 0.000000000000000000, 1.000000000000000000 ) ) ;
#47773=FACE_OUTER_BOUND ( 'NONE', #52501, .T. ) ;
#47775=CIRCLE ( 'NONE', #44368, 0.1999999999999996503 ) ;
#47778=EDGE_CURVE ( 'NONE', #51438, #68065, #44808, .T. ) ;
#47789=DIRECTION ( 'NONE',  ( -0.000000000000000000, -0.000000000000000000, 1.000000000000000000 ) ) ;
#47791=DIRECTION ( 'NONE',  ( 0.000000000000000000, -1.000000000000000000, 0.000000000000000000 ) ) ;
#47794=FACE_OUTER_BOUND ( 'NONE', #5130, .T. ) ;
#47797=AXIS2_PLACEMENT_3D ( 'NONE', #23691, #18739, #65795 ) ;
#47805=CARTESIAN_POINT ( 'NONE',  ( 7.450000000000004619, -1.336933437520057563E-15, -25.50000000000000355 ) ) ;
#47806=VERTEX_POINT ( 'NONE', #7318 ) ;
#47812=CARTESIAN_POINT ( 'NONE',  ( -7.250000000000000888, 8.250000000000001776, -19.00000000000000000 ) ) ;
#47820=VERTEX_POINT ( 'NONE', #32053 ) ;
#47824=LINE ( 'NONE', #37234, #43508 ) ;
#47827=ORIENTED_EDGE ( 'NONE', *, *, #45311, .F. ) ;
#47829=ORIENTED_EDGE ( 'NONE', *, *, #31079, .F. ) ;
#47833=DIRECTION ( 'NONE',  ( 1.000000000000000000, -5.981805089575196197E-17, 0.000000000000000000 ) ) ;
#47838=ORIENTED_EDGE ( 'NONE', *, *, #47944, .F. ) ;
#47841=AXIS2_PLACEMENT_3D ( 'NONE', #44910, #2816, #50211 ) ;
#47843=FACE_OUTER_BOUND ( 'NONE', #58245, .T. ) ;
#47847=DIRECTION ( 'NONE',  ( 1.000000000000000000, -5.981805089575194965E-17, 0.000000000000000000 ) ) ;
#47855=DIRECTION ( 'NONE',  ( 1.000000000000000000, 0.000000000000000000, 0.000000000000000000 ) ) ;
#47860=AXIS2_PLACEMENT_3D ( 'NONE', #46004, #1822, #17386 ) ;
#47870=ORIENTED_EDGE ( 'NONE', *, *, #65703, .F. ) ;
#47888=CARTESIAN_POINT ( 'NONE',  ( 9.689999999999999503, -9.750000000000001776, -5.000000000000000000 ) ) ;
#47889=DIRECTION ( 'NONE',  ( 0.000000000000000000, 0.000000000000000000, -1.000000000000000000 ) ) ;
#47890=ORIENTED_EDGE ( 'NONE', *, *, #18363, .T. ) ;
#47891=CARTESIAN_POINT ( 'NONE',  ( 8.250000000000005329, 7.250000000000000888, -26.00000000000001066 ) ) ;
#47895=CARTESIAN_POINT ( 'NONE',  ( -7.450000000000001954, 7.250000000000000000, -11.50000000000000000 ) ) ;
#47897=DIRECTION ( 'NONE',  ( 0.000000000000000000, 0.000000000000000000, -1.000000000000000000 ) ) ;
#47901=CIRCLE ( 'NONE', #26459, 1.000000000000000000 ) ;
#47903=AXIS2_PLACEMENT_3D ( 'NONE', #53890, #10048, #59177 ) ;
#47908=ADVANCED_FACE ( 'NONE', ( #41249 ), #68491, .T. ) ;
#47910=CARTESIAN_POINT ( 'NONE',  ( 7.250000000000005329, -7.249999999999998224, -8.500000000000000000 ) ) ;
#47920=VERTEX_POINT ( 'NONE', #31002 ) ;
#47921=EDGE_CURVE ( 'NONE', #10775, #32155, #42304, .T. ) ;
#47931=EDGE_CURVE ( 'NONE', #50433, #26084, #11203, .T. ) ;
#47938=ORIENTED_EDGE ( 'NONE', *, *, #26047, .T. ) ;
#47944=EDGE_CURVE ( 'NONE', #23638, #24719, #60296, .T. ) ;
#47949=EDGE_LOOP ( 'NONE', ( #22626, #4532, #46774, #53656, #49488, #4551, #51930, #30453 ) ) ;
#47970=DIRECTION ( 'NONE',  ( 0.000000000000000000, 1.000000000000000000, 0.000000000000000000 ) ) ;
#47975=EDGE_CURVE ( 'NONE', #16799, #27858, #18001, .T. ) ;
#47981=ORIENTED_EDGE ( 'NONE', *, *, #8343, .T. ) ;
#47995=DIRECTION ( 'NONE',  ( -1.000000000000000000, 0.000000000000000000, -0.000000000000000000 ) ) ;
#47999=LINE ( 'NONE', #9473, #33607 ) ;
#48008=AXIS2_PLACEMENT_3D ( 'NONE', #26004, #25658, #47220 ) ;
#48009=ORIENTED_EDGE ( 'NONE', *, *, #38828, .T. ) ;
#48012=ORIENTED_EDGE ( 'NONE', *, *, #25920, .F. ) ;
#48014=CARTESIAN_POINT ( 'NONE',  ( 7.250000000000005329, -7.449999999999998401, -21.00000000000000000 ) ) ;
#48015=CARTESIAN_POINT ( 'NONE',  ( -7.250000000000001776, -7.249999999999998224, -10.00000000000000000 ) ) ;
#48016=EDGE_LOOP ( 'NONE', ( #37511, #55557, #33612, #48060 ) ) ;
#48023=FACE_OUTER_BOUND ( 'NONE', #59274, .T. ) ;
#48028=EDGE_CURVE ( 'NONE', #29479, #6534, #30441, .T. ) ;
#48033=ORIENTED_EDGE ( 'NONE', *, *, #54318, .T. ) ;
#48036=DIRECTION ( 'NONE',  ( -1.000000000000000000, 0.000000000000000000, 0.000000000000000000 ) ) ;
#48047=ORIENTED_EDGE ( 'NONE', *, *, #63553, .T. ) ;
#48048=AXIS2_PLACEMENT_3D ( 'NONE', #59928, #48629, #5845 ) ;
#48059=FACE_OUTER_BOUND ( 'NONE', #50443, .T. ) ;
#48060=ORIENTED_EDGE ( 'NONE', *, *, #4273, .T. ) ;
#48063=CIRCLE ( 'NONE', #40162, 0.06000000000000102474 ) ;
#48066=EDGE_CURVE ( 'NONE', #7845, #26371, #54181, .T. ) ;
#48068=( GEOMETRIC_REPRESENTATION_CONTEXT ( 3 ) GLOBAL_UNCERTAINTY_ASSIGNED_CONTEXT ( ( #59235 ) ) GLOBAL_UNIT_ASSIGNED_CONTEXT ( ( #1868, #1512, #12458 ) ) REPRESENTATION_CONTEXT ( 'NONE', 'WORKASPACE' ) );
#48069=ORIENTED_EDGE ( 'NONE', *, *, #15062, .F. ) ;
#48074=AXIS2_PLACEMENT_3D ( 'NONE', #36843, #57689, #9259 ) ;
#48094=CARTESIAN_POINT ( 'NONE',  ( 7.450000000000003730, -7.249999999999997335, -9.000000000000001776 ) ) ;
#48097=EDGE_LOOP ( 'NONE', ( #19430, #12403, #29897, #62247, #19047, #3649, #47441, #60327 ) ) ;
#48111=DIRECTION ( 'NONE',  ( 0.000000000000000000, 0.000000000000000000, 1.000000000000000000 ) ) ;
#48126=VERTEX_POINT ( 'NONE', #60986 ) ;
#48129=VERTEX_POINT ( 'NONE', #33775 ) ;
#48141=ORIENTED_EDGE ( 'NONE', *, *, #4058, .F. ) ;
#48143=CARTESIAN_POINT ( 'NONE',  ( -8.250000000000001776, -7.249999999999998224, -26.00000000000001066 ) ) ;
#48145=LINE ( 'NONE', #53455, #57790 ) ;
#48168=DIRECTION ( 'NONE',  ( -0.000000000000000000, -0.000000000000000000, 1.000000000000000000 ) ) ;
#48169=ORIENTED_EDGE ( 'NONE', *, *, #24672, .T. ) ;
#48173=VERTEX_POINT ( 'NONE', #23863 ) ;
#48175=VECTOR ( 'NONE', #47847, 1000.000000000000000 ) ;
#48182=CYLINDRICAL_SURFACE ( 'NONE', #5213, 1.000000000000000000 ) ;
#48198=CARTESIAN_POINT ( 'NONE',  ( -7.250000000000000888, 8.250000000000001776, -26.00000000000001066 ) ) ;
#48205=CARTESIAN_POINT ( 'NONE',  ( -7.250000000000000888, 8.250000000000001776, -26.00000000000001066 ) ) ;
#48208=AXIS2_PLACEMENT_3D ( 'NONE', #12549, #22495, #1267 ) ;
#48209=VECTOR ( 'NONE', #6016, 1000.000000000000000 ) ;
#48210=( GEOMETRIC_REPRESENTATION_CONTEXT ( 3 ) GLOBAL_UNCERTAINTY_ASSIGNED_CONTEXT ( ( #21755 ) ) GLOBAL_UNIT_ASSIGNED_CONTEXT ( ( #23818, #45371, #12499 ) ) REPRESENTATION_CONTEXT ( 'NONE', 'WORKASPACE' ) );
#48213=ADVANCED_FACE ( 'NONE', ( #40473 ), #6901, .F. ) ;
#48218=CARTESIAN_POINT ( 'NONE',  ( 0.000000000000000000, 8.250000000000001776, -14.00000000000000000 ) ) ;
#48224=VECTOR ( 'NONE', #11229, 1000.000000000000000 ) ;
#48225=ORIENTED_EDGE ( 'NONE', *, *, #11548, .F. ) ;
#48226=DIRECTION ( 'NONE',  ( -1.000000000000000000, 0.000000000000000000, 0.000000000000000000 ) ) ;
#48242=DIRECTION ( 'NONE',  ( 0.000000000000000000, 0.000000000000000000, -1.000000000000000000 ) ) ;
#48243=LINE ( 'NONE', #48589, #26327 ) ;
#48244=ORIENTED_EDGE ( 'NONE', *, *, #16553, .F. ) ;
#48253=ORIENTED_EDGE ( 'NONE', *, *, #61950, .T. ) ;
#48254=EDGE_CURVE ( 'NONE', #17912, #43298, #41877, .T. ) ;
#48261=DIRECTION ( 'NONE',  ( 0.000000000000000000, 0.000000000000000000, -1.000000000000000000 ) ) ;
#48266=PLANE ( 'NONE',  #48008 ) ;
#48269=VERTEX_POINT ( 'NONE', #57089 ) ;
#48271=ADVANCED_FACE ( 'NONE', ( #41531 ), #52862, .F. ) ;
#48274=CARTESIAN_POINT ( 'NONE',  ( 7.250000000000005329, -7.249999999999998224, -26.00000000000001066 ) ) ;
#48289=CARTESIAN_POINT ( 'NONE',  ( 7.250000000000005329, 7.250000000000000888, -20.50000000000000000 ) ) ;
#48302=DIRECTION ( 'NONE',  ( 1.000000000000000000, 0.000000000000000000, 0.000000000000000000 ) ) ;
#48303=CARTESIAN_POINT ( 'NONE',  ( -7.250000000000001776, -7.249999999999998224, -26.00000000000001066 ) ) ;
#48304=VERTEX_POINT ( 'NONE', #68760 ) ;
#48305=CARTESIAN_POINT ( 'NONE',  ( 7.250000000000005329, -8.249999999999998224, -26.00000000000001066 ) ) ;
#48312=CARTESIAN_POINT ( 'NONE',  ( 7.250000000000005329, -7.249999999999998224, -18.50000000000000000 ) ) ;
#48316=CARTESIAN_POINT ( 'NONE',  ( 0.000000000000000000, 8.250000000000001776, -11.00000000000000000 ) ) ;
#48326=LINE ( 'NONE', #14751, #53111 ) ;
#48336=DIRECTION ( 'NONE',  ( 0.000000000000000000, 0.000000000000000000, -1.000000000000000000 ) ) ;
#48342=DIRECTION ( 'NONE',  ( -1.000000000000000000, 0.000000000000000000, 0.000000000000000000 ) ) ;
#48343=ORIENTED_EDGE ( 'NONE', *, *, #45271, .T. ) ;
#48346=EDGE_CURVE ( 'NONE', #67047, #60224, #53547, .T. ) ;
#48347=ORIENTED_EDGE ( 'NONE', *, *, #15452, .T. ) ;
#48351=CARTESIAN_POINT ( 'NONE',  ( 7.250000000000005329, -7.449999999999998401, -11.50000000000000000 ) ) ;
#48363=VERTEX_POINT ( 'NONE', #64504 ) ;
#48384=ORIENTED_EDGE ( 'NONE', *, *, #3178, .T. ) ;
#48402=CARTESIAN_POINT ( 'NONE',  ( 0.000000000000000000, -7.449999999999998401, -9.000000000000001776 ) ) ;
#48408=ORIENTED_EDGE ( 'NONE', *, *, #63559, .F. ) ;
#48413=ADVANCED_FACE ( 'NONE', ( #27019 ), #38666, .T. ) ;
#48422=ORIENTED_EDGE ( 'NONE', *, *, #11138, .T. ) ;
#48425=ORIENTED_EDGE ( 'NONE', *, *, #34410, .F. ) ;
#48433=ORIENTED_EDGE ( 'NONE', *, *, #60813, .F. ) ;
#48436=CARTESIAN_POINT ( 'NONE',  ( -7.250000000000001776, -7.249999999999998224, -8.000000000000000000 ) ) ;
#48446=ORIENTED_EDGE ( 'NONE', *, *, #8588, .F. ) ;
#48448=AXIS2_PLACEMENT_3D ( 'NONE', #37319, #32699, #10774 ) ;
#48449=CARTESIAN_POINT ( 'NONE',  ( 0.000000000000000000, -8.249999999999998224, -21.00000000000000000 ) ) ;
#48455=FACE_OUTER_BOUND ( 'NONE', #56975, .T. ) ;
#48461=DIRECTION ( 'NONE',  ( 0.000000000000000000, 0.000000000000000000, -1.000000000000000000 ) ) ;
#48467=CARTESIAN_POINT ( 'NONE',  ( -7.250000000000000888, 7.450000000000003730, -9.500000000000001776 ) ) ;
#48468=CARTESIAN_POINT ( 'NONE',  ( 0.000000000000000000, 0.000000000000000000, -29.90000000000000924 ) ) ;
#48470=DIRECTION ( 'NONE',  ( 0.000000000000000000, 0.000000000000000000, -1.000000000000000000 ) ) ;
#48471=EDGE_LOOP ( 'NONE', ( #33558, #41840, #41096, #9159 ) ) ;
#48480=LINE ( 'NONE', #37526, #52003 ) ;
#48483=FACE_OUTER_BOUND ( 'NONE', #6135, .T. ) ;
#48486=CARTESIAN_POINT ( 'NONE',  ( -8.250000000000001776, 0.000000000000000000, -14.00000000000000000 ) ) ;
#48495=ORIENTED_EDGE ( 'NONE', *, *, #60380, .T. ) ;
#48499=LINE ( 'NONE', #11019, #13332 ) ;
#48503=DIRECTION ( 'NONE',  ( 0.000000000000000000, 0.000000000000000000, 1.000000000000000000 ) ) ;
#48506=VECTOR ( 'NONE', #37874, 1000.000000000000000 ) ;
#48509=AXIS2_PLACEMENT_3D ( 'NONE', #36216, #63098, #53209 ) ;
#48512=VERTEX_POINT ( 'NONE', #2915 ) ;
#48528=ORIENTED_EDGE ( 'NONE', *, *, #28420, .T. ) ;
#48531=LINE ( 'NONE', #32961, #12996 ) ;
#48535=VECTOR ( 'NONE', #68629, 1000.000000000000000 ) ;
#48536=ORIENTED_EDGE ( 'NONE', *, *, #32836, .F. ) ;
#48537=ORIENTED_EDGE ( 'NONE', *, *, #50020, .T. ) ;
#48543=VERTEX_POINT ( 'NONE', #61957 ) ;
#48544=DIRECTION ( 'NONE',  ( 0.000000000000000000, 0.000000000000000000, -1.000000000000000000 ) ) ;
#48545=DIRECTION ( 'NONE',  ( -1.000000000000000000, 0.000000000000000000, 0.000000000000000000 ) ) ;
#48549=EDGE_CURVE ( 'NONE', #7124, #18304, #28386, .T. ) ;
#48553=EDGE_LOOP ( 'NONE', ( #42843, #49600, #59722, #57050 ) ) ;
#48555=VECTOR ( 'NONE', #42040, 1000.000000000000000 ) ;
#48556=LINE ( 'NONE', #51851, #28117 ) ;
#48559=DIRECTION ( 'NONE',  ( 0.000000000000000000, 1.000000000000000000, -0.000000000000000000 ) ) ;
#48561=EDGE_CURVE ( 'NONE', #20561, #29125, #50307, .T. ) ;
#48565=EDGE_CURVE ( 'NONE', #9839, #15117, #55327, .T. ) ;
#48566=ADVANCED_FACE ( 'NONE', ( #45687 ), #66907, .T. ) ;
#48572=CARTESIAN_POINT ( 'NONE',  ( 8.250000000000005329, 7.250000000000000888, -24.00000000000000000 ) ) ;
#48575=CARTESIAN_POINT ( 'NONE',  ( -8.250000000000001776, 7.250000000000000888, -17.50000000000000000 ) ) ;
#48587=VERTEX_POINT ( 'NONE', #61595 ) ;
#48588=FACE_OUTER_BOUND ( 'NONE', #16224, .T. ) ;
#48589=CARTESIAN_POINT ( 'NONE',  ( -7.250000000000000888, 7.450000000000003730, -14.50000000000000000 ) ) ;
#48597=PLANE ( 'NONE',  #5771 ) ;
#48604=EDGE_CURVE ( 'NONE', #9143, #67986, #47445, .T. ) ;
#48610=ORIENTED_EDGE ( 'NONE', *, *, #8979, .F. ) ;
#48611=EDGE_LOOP ( 'NONE', ( #50833, #38181, #16942, #26172, #21678, #20821, #51080, #58539 ) ) ;
#48613=VECTOR ( 'NONE', #11264, 1000.000000000000000 ) ;
#48617=DIRECTION ( 'NONE',  ( 0.000000000000000000, 0.000000000000000000, -1.000000000000000000 ) ) ;
#48627=DIRECTION ( 'NONE',  ( 0.000000000000000000, 0.000000000000000000, -1.000000000000000000 ) ) ;
#48629=DIRECTION ( 'NONE',  ( 0.000000000000000000, 0.000000000000000000, -1.000000000000000000 ) ) ;
#48636=CARTESIAN_POINT ( 'NONE',  ( 4.456444791733522252E-16, 7.450000000000002842, -11.50000000000000000 ) ) ;
#48638=LINE ( 'NONE', #209, #58659 ) ;
#48640=VERTEX_POINT ( 'NONE', #47110 ) ;
#48648=ORIENTED_EDGE ( 'NONE', *, *, #51593, .F. ) ;
#48649=VECTOR ( 'NONE', #60816, 1000.000000000000000 ) ;
#48650=FACE_OUTER_BOUND ( 'NONE', #33544, .T. ) ;
#48652=ADVANCED_FACE ( 'NONE', ( #8911 ), #52058, .T. ) ;
#48661=DIRECTION ( 'NONE',  ( -0.000000000000000000, 0.000000000000000000, 1.000000000000000000 ) ) ;
#48664=DIRECTION ( 'NONE',  ( 0.000000000000000000, 1.000000000000000000, 0.000000000000000000 ) ) ;
#48667=DIRECTION ( 'NONE',  ( 0.000000000000000000, 0.000000000000000000, -1.000000000000000000 ) ) ;
#48669=DIRECTION ( 'NONE',  ( -1.000000000000000000, 0.000000000000000000, 0.000000000000000000 ) ) ;
#48674=DIRECTION ( 'NONE',  ( 0.000000000000000000, 0.000000000000000000, 1.000000000000000000 ) ) ;
#48675=FACE_BOUND ( 'NONE', #21062, .T. ) ;
#48696=CIRCLE ( 'NONE', #39633, 0.2000000000000005107 ) ;
#48697=ORIENTED_EDGE ( 'NONE', *, *, #9660, .F. ) ;
#48701=CARTESIAN_POINT ( 'NONE',  ( 8.250000000000005329, -7.249999999999998224, -26.00000000000001066 ) ) ;
#48706=CIRCLE ( 'NONE', #45294, 1.000000000000000000 ) ;
#48709=EDGE_CURVE ( 'NONE', #5314, #51178, #5671, .T. ) ;
#48719=FACE_BOUND ( 'NONE', #12871, .T. ) ;
#48734=EDGE_CURVE ( 'NONE', #68045, #59557, #62064, .T. ) ;
#48744=EDGE_CURVE ( 'NONE', #56308, #68972, #60139, .T. ) ;
#48751=CARTESIAN_POINT ( 'NONE',  ( 7.450000000000004619, -1.336933437520057563E-15, -19.50000000000000000 ) ) ;
#48763=CARTESIAN_POINT ( 'NONE',  ( 4.456444791733522252E-16, 7.450000000000002842, -19.00000000000000000 ) ) ;
#48765=VERTEX_POINT ( 'NONE', #26944 ) ;
#48766=LINE ( 'NONE', #327, #19360 ) ;
#48769=ADVANCED_FACE ( 'NONE', ( #16684 ), #411, .T. ) ;
#48777=ORIENTED_EDGE ( 'NONE', *, *, #8127, .T. ) ;
#48778=PLANE ( 'NONE',  #42993 ) ;
#48784=CARTESIAN_POINT ( 'NONE',  ( 7.250000000000005329, -7.449999999999998401, -10.00000000000000000 ) ) ;
#48792=ORIENTED_EDGE ( 'NONE', *, *, #23397, .F. ) ;
#48793=ORIENTED_EDGE ( 'NONE', *, *, #49726, .F. ) ;
#48805=ADVANCED_FACE ( 'NONE', ( #47794 ), #11359, .T. ) ;
#48807=PLANE ( 'NONE',  #61657 ) ;
#48818=EDGE_CURVE ( 'NONE', #68319, #18594, #22339, .T. ) ;
#48830=DIRECTION ( 'NONE',  ( -1.000000000000000000, 0.000000000000000000, 0.000000000000000000 ) ) ;
#48834=DIRECTION ( 'NONE',  ( 0.000000000000000000, 0.000000000000000000, -1.000000000000000000 ) ) ;
#48836=VERTEX_POINT ( 'NONE', #43531 ) ;
#48837=LINE ( 'NONE', #64404, #48506 ) ;
#48845=ORIENTED_EDGE ( 'NONE', *, *, #52524, .F. ) ;
#48846=CYLINDRICAL_SURFACE ( 'NONE', #7141, 1.000000000000000000 ) ;
#48852=CARTESIAN_POINT ( 'NONE',  ( 7.250000000000005329, -7.249999999999998224, -14.50000000000000000 ) ) ;
#48856=ORIENTED_EDGE ( 'NONE', *, *, #58515, .F. ) ;
#48858=CIRCLE ( 'NONE', #9327, 1.000000000000000000 ) ;
#48862=CARTESIAN_POINT ( 'NONE',  ( -8.250000000000001776, 0.000000000000000000, -11.50000000000000000 ) ) ;
#48867=ORIENTED_EDGE ( 'NONE', *, *, #22660, .T. ) ;
#48871=CARTESIAN_POINT ( 'NONE',  ( 0.000000000000000000, -8.249999999999998224, -19.50000000000000000 ) ) ;
#48874=CIRCLE ( 'NONE', #46626, 0.2000000000000005107 ) ;
#48879=EDGE_LOOP ( 'NONE', ( #5920, #42512, #50985, #33125 ) ) ;
#48884=ORIENTED_EDGE ( 'NONE', *, *, #23743, .F. ) ;
#48886=CIRCLE ( 'NONE', #20648, 0.2000000000000005107 ) ;
#48888=DIRECTION ( 'NONE',  ( 0.000000000000000000, 0.000000000000000000, 1.000000000000000000 ) ) ;
#48891=ORIENTED_EDGE ( 'NONE', *, *, #65946, .T. ) ;
#48901=CARTESIAN_POINT ( 'NONE',  ( 7.450000000000006395, 7.250000000000000888, -19.50000000000000000 ) ) ;
#48902=AXIS2_PLACEMENT_3D ( 'NONE', #7927, #7586, #20211 ) ;
#48913=DIRECTION ( 'NONE',  ( 0.000000000000000000, 0.000000000000000000, 1.000000000000000000 ) ) ;
#48932=AXIS2_PLACEMENT_3D ( 'NONE', #66717, #61769, #39832 ) ;
#48939=LINE ( 'NONE', #6144, #28570 ) ;
#48953=DIRECTION ( 'NONE',  ( -1.000000000000000000, 0.000000000000000000, 0.000000000000000000 ) ) ;
#48959=EDGE_CURVE ( 'NONE', #6054, #2145, #60853, .T. ) ;
#48960=ORIENTED_EDGE ( 'NONE', *, *, #27131, .T. ) ;
#48973=ORIENTED_EDGE ( 'NONE', *, *, #35801, .F. ) ;
#48974=AXIS2_PLACEMENT_3D ( 'NONE', #34202, #17266, #22921 ) ;
#48988=DIRECTION ( 'NONE',  ( -0.000000000000000000, 0.000000000000000000, 1.000000000000000000 ) ) ;
#48995=DIRECTION ( 'NONE',  ( -1.000000000000000000, 0.000000000000000000, 0.000000000000000000 ) ) ;
#48997=LINE ( 'NONE', #69862, #23402 ) ;
#48998=ORIENTED_EDGE ( 'NONE', *, *, #64840, .T. ) ;
#49001=EDGE_CURVE ( 'NONE', #62786, #46075, #62224, .T. ) ;
#49002=CARTESIAN_POINT ( 'NONE',  ( 9.690000000000001279, -8.750000000000000000, -7.000000000000000000 ) ) ;
#49004=EDGE_CURVE ( 'NONE', #6993, #44864, #56911, .T. ) ;
#49013=ORIENTED_EDGE ( 'NONE', *, *, #23485, .T. ) ;
#49021=FACE_OUTER_BOUND ( 'NONE', #28163, .T. ) ;
#49024=LINE ( 'NONE', #31725, #1631 ) ;
#49025=AXIS2_PLACEMENT_3D ( 'NONE', #64691, #37828, #32867 ) ;
#49028=ORIENTED_EDGE ( 'NONE', *, *, #13665, .T. ) ;
#49031=CARTESIAN_POINT ( 'NONE',  ( 7.450000000000004619, -1.336933437520057563E-15, -14.50000000000000000 ) ) ;
#49038=ORIENTED_EDGE ( 'NONE', *, *, #22491, .F. ) ;
#49044=CARTESIAN_POINT ( 'NONE',  ( 7.250000000000005329, -8.249999999999998224, -10.00000000000000000 ) ) ;
#49046=ORIENTED_EDGE ( 'NONE', *, *, #20624, .F. ) ;
#49072=EDGE_LOOP ( 'NONE', ( #68149, #6770, #61070, #45828 ) ) ;
#49080=CARTESIAN_POINT ( 'NONE',  ( -8.250000000000001776, -7.249999999999998224, -11.50000000000000000 ) ) ;
#49088=AXIS2_PLACEMENT_3D ( 'NONE', #45612, #13792, #2833 ) ;
#49093=CARTESIAN_POINT ( 'NONE',  ( 7.250000000000005329, -8.249999999999998224, -22.50000000000000000 ) ) ;
#49096=ORIENTED_EDGE ( 'NONE', *, *, #8801, .T. ) ;
#49099=CARTESIAN_POINT ( 'NONE',  ( -7.450000000000001954, -7.249999999999998224, -7.000000000000000000 ) ) ;
#49100=EDGE_CURVE ( 'NONE', #17018, #18984, #46661, .T. ) ;
#49102=LINE ( 'NONE', #60741, #29346 ) ;
#49109=CARTESIAN_POINT ( 'NONE',  ( 7.250000000000005329, -7.449999999999998401, -21.50000000000000000 ) ) ;
#49125=CARTESIAN_POINT ( 'NONE',  ( 9.690000000000001279, -9.750000000000001776, -7.000000000000000000 ) ) ;
#49147=ORIENTED_EDGE ( 'NONE', *, *, #26980, .F. ) ;
#49148=CARTESIAN_POINT ( 'NONE',  ( 0.000000000000000000, 0.000000000000000000, -15.00000000000000000 ) ) ;
#49153=DIRECTION ( 'NONE',  ( 0.000000000000000000, 1.000000000000000000, 0.000000000000000000 ) ) ;
#49157=VECTOR ( 'NONE', #32459, 1000.000000000000000 ) ;
#49158=CIRCLE ( 'NONE', #8455, 0.2000000000000005107 ) ;
#49165=ORIENTED_EDGE ( 'NONE', *, *, #64880, .T. ) ;
#49167=CIRCLE ( 'NONE', #19767, 0.2000000000000005107 ) ;
#49174=CARTESIAN_POINT ( 'NONE',  ( 0.000000000000000000, 0.000000000000000000, -30.00000000000001066 ) ) ;
#49176=FACE_OUTER_BOUND ( 'NONE', #38345, .T. ) ;
#49184=CARTESIAN_POINT ( 'NONE',  ( -7.250000000000000888, 7.250000000000001776, -10.00000000000000000 ) ) ;
#49186=LINE ( 'NONE', #6726, #9432 ) ;
#49190=CARTESIAN_POINT ( 'NONE',  ( -8.250000000000000000, 7.250000000000001776, -7.500000000000000000 ) ) ;
#49204=EDGE_CURVE ( 'NONE', #34259, #41478, #25908, .T. ) ;
#49226=AXIS2_PLACEMENT_3D ( 'NONE', #64358, #63668, #42779 ) ;
#49229=VERTEX_POINT ( 'NONE', #56440 ) ;
#49232=ORIENTED_EDGE ( 'NONE', *, *, #61435, .T. ) ;
#49234=VECTOR ( 'NONE', #33485, 1000.000000000000000 ) ;
#49235=DIRECTION ( 'NONE',  ( 0.000000000000000000, -1.000000000000000000, 0.000000000000000000 ) ) ;
#49247=ORIENTED_EDGE ( 'NONE', *, *, #34594, .T. ) ;
#49249=FACE_OUTER_BOUND ( 'NONE', #57440, .T. ) ;
#49256=DIRECTION ( 'NONE',  ( -0.000000000000000000, -0.000000000000000000, -1.000000000000000000 ) ) ;
#49258=AXIS2_PLACEMENT_3D ( 'NONE', #5550, #1280, #64946 ) ;
#49260=FACE_OUTER_BOUND ( 'NONE', #21246, .T. ) ;
#49266=EDGE_CURVE ( 'NONE', #25825, #6078, #8346, .T. ) ;
#49268=ORIENTED_EDGE ( 'NONE', *, *, #60072, .F. ) ;
#49271=AXIS2_PLACEMENT_3D ( 'NONE', #57232, #47322, #41308 ) ;
#49275=EDGE_CURVE ( 'NONE', #11123, #9064, #14005, .T. ) ;
#49283=AXIS2_PLACEMENT_3D ( 'NONE', #18886, #55661, #13574 ) ;
#49286=DIRECTION ( 'NONE',  ( 0.000000000000000000, 0.000000000000000000, 1.000000000000000000 ) ) ;
#49291=ADVANCED_FACE ( 'NONE', ( #57496 ), #9062, .F. ) ;
#49293=EDGE_CURVE ( 'NONE', #36081, #14970, #23598, .T. ) ;
#49295=CYLINDRICAL_SURFACE ( 'NONE', #30811, 1.000000000000001776 ) ;
#49297=DIRECTION ( 'NONE',  ( 1.000000000000000000, 0.000000000000000000, 0.000000000000000000 ) ) ;
#49309=ORIENTED_EDGE ( 'NONE', *, *, #36371, .F. ) ;
#49317=ORIENTED_EDGE ( 'NONE', *, *, #7941, .T. ) ;
#49321=CYLINDRICAL_SURFACE ( 'NONE', #20219, 1.000000000000000000 ) ;
#49322=EDGE_CURVE ( 'NONE', #26913, #60006, #47341, .T. ) ;
#49323=CIRCLE ( 'NONE', #66258, 1.000000000000000000 ) ;
#49332=VERTEX_POINT ( 'NONE', #42281 ) ;
#49333=VERTEX_POINT ( 'NONE', #68466 ) ;
#49336=FACE_OUTER_BOUND ( 'NONE', #29128, .T. ) ;
#49338=ORIENTED_EDGE ( 'NONE', *, *, #44266, .F. ) ;
#49339=CARTESIAN_POINT ( 'NONE',  ( 7.250000000000005329, -7.249999999999998224, -7.000000000000000000 ) ) ;
#49344=CARTESIAN_POINT ( 'NONE',  ( -7.450000000000001954, -7.249999999999998224, -10.50000000000000000 ) ) ;
#49368=CARTESIAN_POINT ( 'NONE',  ( -7.450000000000001954, 0.000000000000000000, -16.00000000000000000 ) ) ;
#49369=AXIS2_PLACEMENT_3D ( 'NONE', #27710, #65876, #17433 ) ;
#49370=VECTOR ( 'NONE', #23835, 1000.000000000000000 ) ;
#49374=DIRECTION ( 'NONE',  ( -1.000000000000000000, 0.000000000000000000, 0.000000000000000000 ) ) ;
#49380=DIRECTION ( 'NONE',  ( 0.000000000000000000, 0.000000000000000000, 1.000000000000000000 ) ) ;
#49384=CARTESIAN_POINT ( 'NONE',  ( 7.250000000000005329, 7.250000000000000888, -22.50000000000000000 ) ) ;
#49385=DIRECTION ( 'NONE',  ( -1.000000000000000000, 0.000000000000000000, 0.000000000000000000 ) ) ;
#49386=ORIENTED_EDGE ( 'NONE', *, *, #55993, .T. ) ;
#49391=LINE ( 'NONE', #39109, #20582 ) ;
#49392=ORIENTED_EDGE ( 'NONE', *, *, #35205, .T. ) ;
#49394=VERTEX_POINT ( 'NONE', #32038 ) ;
#49396=CARTESIAN_POINT ( 'NONE',  ( 4.456444791733522252E-16, 7.450000000000002842, -18.00000000000000000 ) ) ;
#49397=ORIENTED_EDGE ( 'NONE', *, *, #50259, .T. ) ;
#49399=CARTESIAN_POINT ( 'NONE',  ( 4.456444791733522252E-16, 7.450000000000002842, -15.00000000000000000 ) ) ;
#49407=DIRECTION ( 'NONE',  ( 0.000000000000000000, -0.000000000000000000, 1.000000000000000000 ) ) ;
#49412=AXIS2_PLACEMENT_3D ( 'NONE', #21073, #21773, #64222 ) ;
#49413=DIRECTION ( 'NONE',  ( 1.000000000000000000, 0.000000000000000000, 0.000000000000000000 ) ) ;
#49418=DIRECTION ( 'NONE',  ( 1.000000000000000000, 0.000000000000000000, 0.000000000000000000 ) ) ;
#49426=CARTESIAN_POINT ( 'NONE',  ( 7.250000000000004441, 7.450000000000001954, -17.50000000000000000 ) ) ;
#49431=CARTESIAN_POINT ( 'NONE',  ( 7.250000000000004441, 7.450000000000001954, -15.50000000000000000 ) ) ;
#49442=CARTESIAN_POINT ( 'NONE',  ( 8.250000000000005329, -7.249999999999998224, -14.00000000000000000 ) ) ;
#49458=CARTESIAN_POINT ( 'NONE',  ( -7.250000000000001776, -7.249999999999998224, -26.00000000000001066 ) ) ;
#49459=DIRECTION ( 'NONE',  ( -1.000000000000000000, 0.000000000000000000, 0.000000000000000000 ) ) ;
#49470=ORIENTED_EDGE ( 'NONE', *, *, #32945, .T. ) ;
#49473=EDGE_LOOP ( 'NONE', ( #15285, #45287, #10177, #34523 ) ) ;
#49476=DIRECTION ( 'NONE',  ( 0.000000000000000000, -0.000000000000000000, 1.000000000000000000 ) ) ;
#49480=EDGE_CURVE ( 'NONE', #31236, #32954, #59249, .T. ) ;
#49488=ORIENTED_EDGE ( 'NONE', *, *, #56278, .F. ) ;
#49489=ORIENTED_EDGE ( 'NONE', *, *, #45185, .F. ) ;
#49506=LINE ( 'NONE', #1075, #11480 ) ;
#49507=ORIENTED_EDGE ( 'NONE', *, *, #28035, .F. ) ;
#49508=DIRECTION ( 'NONE',  ( 1.000000000000000000, -5.981805089575194965E-17, 0.000000000000000000 ) ) ;
#49509=ORIENTED_EDGE ( 'NONE', *, *, #45486, .T. ) ;
#49512=DIRECTION ( 'NONE',  ( -0.000000000000000000, -0.000000000000000000, 1.000000000000000000 ) ) ;
#49514=CARTESIAN_POINT ( 'NONE',  ( -7.250000000000000000, -7.449999999999998401, -17.00000000000000000 ) ) ;
#49515=DIRECTION ( 'NONE',  ( 0.000000000000000000, 0.000000000000000000, 1.000000000000000000 ) ) ;
#49521=ORIENTED_EDGE ( 'NONE', *, *, #17405, .F. ) ;
#49524=LINE ( 'NONE', #32918, #25633 ) ;
#49525=EDGE_CURVE ( 'NONE', #55726, #5045, #48638, .T. ) ;
#49526=EDGE_CURVE ( 'NONE', #12501, #66919, #64905, .T. ) ;
#49527=DIRECTION ( 'NONE',  ( 0.000000000000000000, 0.000000000000000000, 1.000000000000000000 ) ) ;
#49535=EDGE_CURVE ( 'NONE', #53820, #63385, #46215, .T. ) ;
#49537=ADVANCED_FACE ( 'NONE', ( #57439 ), #30568, .F. ) ;
#49541=ORIENTED_EDGE ( 'NONE', *, *, #49823, .T. ) ;
#49546=CARTESIAN_POINT ( 'NONE',  ( 2.500000000000000000, 3.061616997868383141E-16, -29.90000000000000924 ) ) ;
#49553=AXIS2_PLACEMENT_3D ( 'NONE', #37566, #32253, #26957 ) ;
#49558=DIRECTION ( 'NONE',  ( 1.000000000000000000, -5.981805089575196197E-17, 0.000000000000000000 ) ) ;
#49571=CARTESIAN_POINT ( 'NONE',  ( -8.250000000000001776, 0.000000000000000000, -20.00000000000000000 ) ) ;
#49575=ADVANCED_FACE ( 'NONE', ( #19956 ), #47191, .T. ) ;
#49581=EDGE_CURVE ( 'NONE', #63059, #60163, #69448, .T. ) ;
#49584=CARTESIAN_POINT ( 'NONE',  ( -8.250000000000001776, 0.000000000000000000, -10.50000000000000000 ) ) ;
#49585=ADVANCED_FACE ( 'NONE', ( #4757 ), #15365, .T. ) ;
#49586=DIRECTION ( 'NONE',  ( 0.000000000000000000, 0.000000000000000000, 1.000000000000000000 ) ) ;
#49590=DIRECTION ( 'NONE',  ( -1.000000000000000000, 0.000000000000000000, 0.000000000000000000 ) ) ;
#49595=LINE ( 'NONE', #18096, #54235 ) ;
#49597=DIRECTION ( 'NONE',  ( 0.000000000000000000, 0.000000000000000000, 1.000000000000000000 ) ) ;
#49600=ORIENTED_EDGE ( 'NONE', *, *, #27644, .F. ) ;
#49616=ORIENTED_EDGE ( 'NONE', *, *, #30751, .F. ) ;
#49619=ORIENTED_EDGE ( 'NONE', *, *, #34410, .T. ) ;
#49620=CARTESIAN_POINT ( 'NONE',  ( 7.250000000000005329, -8.749999999999998224, -30.00000000000001066 ) ) ;
#49627=DIRECTION ( 'NONE',  ( 0.000000000000000000, -0.000000000000000000, 1.000000000000000000 ) ) ;
#49657=CIRCLE ( 'NONE', #38366, 2.500000000000000000 ) ;
#49658=EDGE_LOOP ( 'NONE', ( #2599, #52659, #41206, #29881 ) ) ;
#49666=PLANE ( 'NONE',  #8717 ) ;
#49673=EDGE_CURVE ( 'NONE', #67323, #20378, #66135, .T. ) ;
#49674=ADVANCED_FACE ( 'NONE', ( #60480 ), #65455, .F. ) ;
#49680=DIRECTION ( 'NONE',  ( 0.000000000000000000, 0.000000000000000000, 1.000000000000000000 ) ) ;
#49684=PLANE ( 'NONE',  #44847 ) ;
#49690=EDGE_CURVE ( 'NONE', #10351, #53691, #49657, .T. ) ;
#49701=FACE_OUTER_BOUND ( 'NONE', #16280, .T. ) ;
#49703=VERTEX_POINT ( 'NONE', #49876 ) ;
#49713=CARTESIAN_POINT ( 'NONE',  ( 7.450000000000004619, -1.336933437520057563E-15, -20.50000000000000000 ) ) ;
#49717=AXIS2_PLACEMENT_3D ( 'NONE', #38022, #54629, #16793 ) ;
#49721=ORIENTED_EDGE ( 'NONE', *, *, #55420, .T. ) ;
#49723=CYLINDRICAL_SURFACE ( 'NONE', #28347, 0.2000000000000005107 ) ;
#49726=EDGE_CURVE ( 'NONE', #40313, #8070, #61162, .T. ) ;
#49730=EDGE_LOOP ( 'NONE', ( #68830, #56399, #50373, #34524, #35830, #19892, #12237, #4456 ) ) ;
#49735=EDGE_LOOP ( 'NONE', ( #55802, #44151, #34504, #35744 ) ) ;
#49737=ORIENTED_EDGE ( 'NONE', *, *, #21924, .F. ) ;
#49741=ADVANCED_FACE ( 'NONE', ( #33277 ), #1432, .F. ) ;
#49759=CARTESIAN_POINT ( 'NONE',  ( 7.250000000000005329, -7.449999999999998401, -24.50000000000000000 ) ) ;
#49762=EDGE_LOOP ( 'NONE', ( #8690, #59990, #29963, #46444 ) ) ;
#49765=AXIS2_PLACEMENT_3D ( 'NONE', #36029, #25081, #62908 ) ;
#49766=DIRECTION ( 'NONE',  ( 0.000000000000000000, 0.000000000000000000, 1.000000000000000000 ) ) ;
#49779=DIRECTION ( 'NONE',  ( 0.000000000000000000, 0.000000000000000000, 1.000000000000000000 ) ) ;
#49785=CARTESIAN_POINT ( 'NONE',  ( -8.250000000000001776, 7.250000000000000888, -26.00000000000001066 ) ) ;
#49790=DIRECTION ( 'NONE',  ( -1.794541526872559352E-16, -1.000000000000000000, 0.000000000000000000 ) ) ;
#49805=ORIENTED_EDGE ( 'NONE', *, *, #16783, .T. ) ;
#49810=EDGE_CURVE ( 'NONE', #52907, #25548, #45097, .T. ) ;
#49815=ORIENTED_EDGE ( 'NONE', *, *, #10878, .F. ) ;
#49823=EDGE_CURVE ( 'NONE', #20448, #19122, #3377, .T. ) ;
#49824=VERTEX_POINT ( 'NONE', #66818 ) ;
#49837=ORIENTED_EDGE ( 'NONE', *, *, #18873, .F. ) ;
#49863=LINE ( 'NONE', #22987, #66246 ) ;
#49864=EDGE_CURVE ( 'NONE', #57893, #6619, #51623, .T. ) ;
#49869=DIRECTION ( 'NONE',  ( -0.000000000000000000, -0.000000000000000000, 1.000000000000000000 ) ) ;
#49870=CARTESIAN_POINT ( 'NONE',  ( 7.250000000000005329, 7.250000000000000888, -23.50000000000000000 ) ) ;
#49872=EDGE_LOOP ( 'NONE', ( #19021, #52732, #21738, #15128 ) ) ;
#49873=CARTESIAN_POINT ( 'NONE',  ( 7.250000000000005329, -7.249999999999998224, -18.00000000000000000 ) ) ;
#49874=LINE ( 'NONE', #54505, #63166 ) ;
#49876=CARTESIAN_POINT ( 'NONE',  ( 8.250000000000005329, 7.250000000000000888, -11.00000000000000000 ) ) ;
#49879=VECTOR ( 'NONE', #1926, 1000.000000000000000 ) ;
#49885=DIRECTION ( 'NONE',  ( -1.000000000000000000, 0.000000000000000000, 0.000000000000000000 ) ) ;
#49892=PRODUCT ( '6266N13_Heavy Duty Locking-Slotted Fitting1_6266N13', '6266N13_Heavy Duty Locking-Slotted Fitting1_6266N13', '', ( #35998 ) ) ;
#49894=DIRECTION ( 'NONE',  ( 0.000000000000000000, 0.000000000000000000, 1.000000000000000000 ) ) ;
#49895=DIRECTION ( 'NONE',  ( 0.000000000000000000, 0.000000000000000000, -1.000000000000000000 ) ) ;
#49897=DIRECTION ( 'NONE',  ( 0.000000000000000000, 0.000000000000000000, -1.000000000000000000 ) ) ;
#49900=DIRECTION ( 'NONE',  ( 0.000000000000000000, 0.000000000000000000, 1.000000000000000000 ) ) ;
#49904=VECTOR ( 'NONE', #38760, 1000.000000000000000 ) ;
#49908=DIRECTION ( 'NONE',  ( -0.000000000000000000, 0.000000000000000000, 1.000000000000000000 ) ) ;
#49921=EDGE_CURVE ( 'NONE', #62492, #17912, #18045, .T. ) ;
#49942=CARTESIAN_POINT ( 'NONE',  ( 7.250000000000005329, 8.250000000000001776, -18.00000000000000000 ) ) ;
#49955=DIRECTION ( 'NONE',  ( 0.000000000000000000, 0.000000000000000000, 1.000000000000000000 ) ) ;
#49959=VECTOR ( 'NONE', #49790, 1000.000000000000000 ) ;
#49965=ORIENTED_EDGE ( 'NONE', *, *, #22653, .T. ) ;
#49971=PLANE ( 'NONE',  #57157 ) ;
#49972=DIRECTION ( 'NONE',  ( -1.000000000000000000, 1.334402673828313093E-16, 0.000000000000000000 ) ) ;
#49988=ORIENTED_EDGE ( 'NONE', *, *, #35292, .T. ) ;
#50006=CARTESIAN_POINT ( 'NONE',  ( 7.450000000000003730, -7.249999999999997335, -18.50000000000000000 ) ) ;
#50008=DIRECTION ( 'NONE',  ( 1.000000000000000000, 0.000000000000000000, 0.000000000000000000 ) ) ;
#50010=CIRCLE ( 'NONE', #21763, 1.000000000000002665 ) ;
#50017=CARTESIAN_POINT ( 'NONE',  ( -8.250000000000001776, 7.250000000000000888, -24.50000000000000000 ) ) ;
#50020=EDGE_CURVE ( 'NONE', #42030, #50504, #68935, .T. ) ;
#50023=LINE ( 'NONE', #6889, #69178 ) ;
#50030=VECTOR ( 'NONE', #46956, 1000.000000000000000 ) ;
#50032=EDGE_CURVE ( 'NONE', #29129, #20614, #16228, .T. ) ;
#50034=ORIENTED_EDGE ( 'NONE', *, *, #9253, .F. ) ;
#50041=EDGE_LOOP ( 'NONE', ( #35036, #18851, #24859, #28056 ) ) ;
#50045=DIRECTION ( 'NONE',  ( 0.000000000000000000, 0.000000000000000000, 1.000000000000000000 ) ) ;
#50052=CARTESIAN_POINT ( 'NONE',  ( -7.450000000000001954, 7.250000000000000000, -15.00000000000000000 ) ) ;
#50065=EDGE_LOOP ( 'NONE', ( #44322, #8595, #55483, #25538 ) ) ;
#50070=EDGE_CURVE ( 'NONE', #26986, #42030, #67482, .T. ) ;
#50077=EDGE_CURVE ( 'NONE', #46187, #42553, #16590, .T. ) ;
#50092=EDGE_CURVE ( 'NONE', #2477, #23182, #28559, .T. ) ;
#50093=DIRECTION ( 'NONE',  ( 0.000000000000000000, 0.000000000000000000, 1.000000000000000000 ) ) ;
#50103=FACE_OUTER_BOUND ( 'NONE', #49658, .T. ) ;
#50107=CARTESIAN_POINT ( 'NONE',  ( 8.250000000000005329, 8.250000000000001776, -26.00000000000001066 ) ) ;
#50110=AXIS2_PLACEMENT_3D ( 'NONE', #31570, #53148, #6430 ) ;
#50112=LINE ( 'NONE', #62103, #61308 ) ;
#50115=DIRECTION ( 'NONE',  ( 0.000000000000000000, 0.000000000000000000, 1.000000000000000000 ) ) ;
#50123=ORIENTED_EDGE ( 'NONE', *, *, #49100, .F. ) ;
#50130=CARTESIAN_POINT ( 'NONE',  ( 6.500000000000000888, -6.500000000000002665, -1.000000000000000000 ) ) ;
#50136=ORIENTED_EDGE ( 'NONE', *, *, #38736, .T. ) ;
#50141=CIRCLE ( 'NONE', #68224, 0.1999999999999987899 ) ;
#50146=EDGE_LOOP ( 'NONE', ( #30469, #22787 ) ) ;
#50153=VECTOR ( 'NONE', #68356, 1000.000000000000000 ) ;
#50159=AXIS2_PLACEMENT_3D ( 'NONE', #57284, #57982, #3901 ) ;
#50167=CARTESIAN_POINT ( 'NONE',  ( -7.450000000000001954, 0.000000000000000000, -25.00000000000000000 ) ) ;
#50179=CARTESIAN_POINT ( 'NONE',  ( -8.250000000000001776, -7.249999999999998224, -26.00000000000001066 ) ) ;
#50183=CYLINDRICAL_SURFACE ( 'NONE', #66253, 1.000000000000000000 ) ;
#50187=ORIENTED_EDGE ( 'NONE', *, *, #22656, .T. ) ;
#50189=ORIENTED_EDGE ( 'NONE', *, *, #47112, .T. ) ;
#50191=CARTESIAN_POINT ( 'NONE',  ( 7.450000000000006395, 7.250000000000000888, -19.50000000000000000 ) ) ;
#50196=EDGE_LOOP ( 'NONE', ( #62072, #35403, #53144, #22913 ) ) ;
#50198=CARTESIAN_POINT ( 'NONE',  ( -7.450000000000001954, 0.000000000000000000, -8.500000000000000000 ) ) ;
#50203=VECTOR ( 'NONE', #9809, 1000.000000000000000 ) ;
#50204=AXIS2_PLACEMENT_3D ( 'NONE', #33899, #17294, #13018 ) ;
#50211=DIRECTION ( 'NONE',  ( 1.000000000000000000, 0.000000000000000000, 0.000000000000000000 ) ) ;
#50214=EDGE_CURVE ( 'NONE', #18722, #25188, #49102, .T. ) ;
#50215=VERTEX_POINT ( 'NONE', #38163 ) ;
#50221=EDGE_CURVE ( 'NONE', #54436, #28576, #45163, .T. ) ;
#50228=VERTEX_POINT ( 'NONE', #8028 ) ;
#50243=FACE_OUTER_BOUND ( 'NONE', #37387, .T. ) ;
#50244=DIRECTION ( 'NONE',  ( -1.000000000000000000, 0.000000000000000000, 0.000000000000000000 ) ) ;
#50248=CIRCLE ( 'NONE', #31083, 0.9999999999999991118 ) ;
#50258=ORIENTED_EDGE ( 'NONE', *, *, #56104, .F. ) ;
#50259=EDGE_CURVE ( 'NONE', #8234, #68958, #19223, .T. ) ;
#50262=LINE ( 'NONE', #23394, #56875 ) ;
#50265=ORIENTED_EDGE ( 'NONE', *, *, #10129, .T. ) ;
#50266=ORIENTED_EDGE ( 'NONE', *, *, #19025, .F. ) ;
#50271=CIRCLE ( 'NONE', #45776, 1.000000000000000000 ) ;
#50282=DIRECTION ( 'NONE',  ( 1.000000000000000000, 0.000000000000000000, 0.000000000000000000 ) ) ;
#50295=EDGE_LOOP ( 'NONE', ( #1347, #17217, #52820, #35294, #46031, #44255, #37475, #24617 ) ) ;
#50300=CARTESIAN_POINT ( 'NONE',  ( 9.690000000000001279, 9.750000000000001776, -7.000000000000000000 ) ) ;
#50303=AXIS2_PLACEMENT_3D ( 'NONE', #68885, #20784, #42355 ) ;
#50307=LINE ( 'NONE', #1873, #6753 ) ;
#50309=ORIENTED_EDGE ( 'NONE', *, *, #5600, .T. ) ;
#50312=VECTOR ( 'NONE', #25375, 1000.000000000000000 ) ;
#50313=CIRCLE ( 'NONE', #25499, 1.000000000000002665 ) ;
#50329=DIRECTION ( 'NONE',  ( 1.000000000000000000, -5.981805089575194965E-17, 0.000000000000000000 ) ) ;
#50338=EDGE_LOOP ( 'NONE', ( #6330, #41129, #62074, #49247, #69557, #8762, #12355, #8488 ) ) ;
#50344=AXIS2_PLACEMENT_3D ( 'NONE', #17882, #45439, #39783 ) ;
#50346=ADVANCED_FACE ( 'NONE', ( #57188 ), #41263, .F. ) ;
#50347=VERTEX_POINT ( 'NONE', #28910 ) ;
#50350=LINE ( 'NONE', #11475, #40670 ) ;
#50352=ORIENTED_EDGE ( 'NONE', *, *, #39260, .F. ) ;
#50353=LINE ( 'NONE', #19230, #9761 ) ;
#50354=AXIS2_PLACEMENT_3D ( 'NONE', #39316, #66532, #13125 ) ;
#50358=DIRECTION ( 'NONE',  ( -1.000000000000000000, 0.000000000000000000, 0.000000000000000000 ) ) ;
#50362=VECTOR ( 'NONE', #27998, 1000.000000000000000 ) ;
#50367=CIRCLE ( 'NONE', #67339, 1.000000000000000000 ) ;
#50373=ORIENTED_EDGE ( 'NONE', *, *, #66481, .F. ) ;
#50378=ORIENTED_EDGE ( 'NONE', *, *, #69320, .F. ) ;
#50383=EDGE_CURVE ( 'NONE', #41191, #21453, #35001, .T. ) ;
#50397=AXIS2_PLACEMENT_3D ( 'NONE', #55296, #61619, #13188 ) ;
#50401=CIRCLE ( 'NONE', #3018, 0.2000000000000005107 ) ;
#50403=LINE ( 'NONE', #27799, #12796 ) ;
#50404=ADVANCED_FACE ( 'NONE', ( #41622 ), #52232, .T. ) ;
#50406=ORIENTED_EDGE ( 'NONE', *, *, #196, .F. ) ;
#50411=VECTOR ( 'NONE', #45070, 1000.000000000000000 ) ;
#50412=LINE ( 'NONE', #68068, #40603 ) ;
#50420=AXIS2_PLACEMENT_3D ( 'NONE', #66782, #18337, #1398 ) ;
#50424=DIRECTION ( 'NONE',  ( 0.000000000000000000, 1.000000000000000000, 0.000000000000000000 ) ) ;
#50425=CARTESIAN_POINT ( 'NONE',  ( -7.250000000000000000, -7.449999999999998401, -23.00000000000000000 ) ) ;
#50427=PLANE ( 'NONE',  #3028 ) ;
#50433=VERTEX_POINT ( 'NONE', #26073 ) ;
#50435=ORIENTED_EDGE ( 'NONE', *, *, #15523, .T. ) ;
#50439=DIRECTION ( 'NONE',  ( 0.000000000000000000, 0.000000000000000000, -1.000000000000000000 ) ) ;
#50440=CARTESIAN_POINT ( 'NONE',  ( -7.250000000000000888, -8.249999999999998224, -23.00000000000000000 ) ) ;
#50442=ORIENTED_EDGE ( 'NONE', *, *, #17265, .F. ) ;
#50443=EDGE_LOOP ( 'NONE', ( #2397, #30949, #35614, #20272 ) ) ;
#50450=ADVANCED_FACE ( 'NONE', ( #42671 ), #36314, .T. ) ;
#50452=VECTOR ( 'NONE', #58228, 1000.000000000000000 ) ;
#50453=AXIS2_PLACEMENT_3D ( 'NONE', #31430, #31775, #53341 ) ;
#50455=DIRECTION ( 'NONE',  ( 0.000000000000000000, 0.000000000000000000, 1.000000000000000000 ) ) ;
#50461=VECTOR ( 'NONE', #47231, 1000.000000000000000 ) ;
#50480=CYLINDRICAL_SURFACE ( 'NONE', #6321, 0.2000000000000005107 ) ;
#50483=DIRECTION ( 'NONE',  ( 0.000000000000000000, 0.000000000000000000, 1.000000000000000000 ) ) ;
#50497=AXIS2_PLACEMENT_3D ( 'NONE', #1337, #7313, #55433 ) ;
#50498=VECTOR ( 'NONE', #51504, 1000.000000000000000 ) ;
#50503=ORIENTED_EDGE ( 'NONE', *, *, #34965, .T. ) ;
#50504=VERTEX_POINT ( 'NONE', #32754 ) ;
#50514=LINE ( 'NONE', #28247, #38378 ) ;
#50515=PLANE ( 'NONE',  #12992 ) ;
#50520=EDGE_CURVE ( 'NONE', #31198, #5559, #55370, .T. ) ;
#50523=EDGE_CURVE ( 'NONE', #29779, #47005, #23810, .T. ) ;
#50526=DIRECTION ( 'NONE',  ( 0.000000000000000000, 1.000000000000000000, 0.000000000000000000 ) ) ;
#50529=EDGE_CURVE ( 'NONE', #24826, #22518, #38414, .T. ) ;
#50536=EDGE_CURVE ( 'NONE', #53899, #26123, #11181, .T. ) ;
#50544=EDGE_LOOP ( 'NONE', ( #61090, #35346, #38787, #42426 ) ) ;
#50553=FACE_OUTER_BOUND ( 'NONE', #57370, .T. ) ;
#50556=DIRECTION ( 'NONE',  ( 0.000000000000000000, 0.000000000000000000, 1.000000000000000000 ) ) ;
#50561=CIRCLE ( 'NONE', #35875, 1.000000000000000000 ) ;
#50566=CARTESIAN_POINT ( 'NONE',  ( -7.450000000000001954, 0.000000000000000000, -20.50000000000000000 ) ) ;
#50569=EDGE_LOOP ( 'NONE', ( #65353, #26278, #40010, #40191 ) ) ;
#50572=ORIENTED_EDGE ( 'NONE', *, *, #69655, .F. ) ;
#50593=FACE_OUTER_BOUND ( 'NONE', #23825, .T. ) ;
#50594=CARTESIAN_POINT ( 'NONE',  ( -7.450000000000001954, -7.249999999999998224, -22.50000000000000000 ) ) ;
#50595=CARTESIAN_POINT ( 'NONE',  ( -8.250000000000001776, 7.250000000000000888, -26.00000000000001066 ) ) ;
#50598=DIRECTION ( 'NONE',  ( 0.000000000000000000, 0.000000000000000000, 1.000000000000000000 ) ) ;
#50605=CARTESIAN_POINT ( 'NONE',  ( -8.750000000000001776, -7.249999999999998224, -30.00000000000001066 ) ) ;
#50608=CARTESIAN_POINT ( 'NONE',  ( -8.250000000000001776, -7.249999999999998224, -26.00000000000001066 ) ) ;
#50614=EDGE_CURVE ( 'NONE', #44864, #23372, #47493, .T. ) ;
#50619=EDGE_CURVE ( 'NONE', #69217, #10277, #32796, .T. ) ;
#50620=ADVANCED_FACE ( 'NONE', ( #61340 ), #42992, .T. ) ;
#50636=LINE ( 'NONE', #3601, #33747 ) ;
#50641=LINE ( 'NONE', #45674, #53966 ) ;
#50644=ORIENTED_EDGE ( 'NONE', *, *, #56535, .F. ) ;
#50645=ORIENTED_EDGE ( 'NONE', *, *, #64188, .F. ) ;
#50649=CARTESIAN_POINT ( 'NONE',  ( -7.250000000000000000, -7.449999999999998401, -16.00000000000000000 ) ) ;
#50650=ORIENTED_EDGE ( 'NONE', *, *, #4303, .F. ) ;
#50652=ORIENTED_EDGE ( 'NONE', *, *, #41933, .T. ) ;
#50654=ORIENTED_EDGE ( 'NONE', *, *, #41234, .T. ) ;
#50657=CYLINDRICAL_SURFACE ( 'NONE', #45473, 1.000000000000000000 ) ;
#50658=ORIENTED_EDGE ( 'NONE', *, *, #65382, .T. ) ;
#50664=DIRECTION ( 'NONE',  ( 0.000000000000000000, 1.000000000000000000, 0.000000000000000000 ) ) ;
#50670=CYLINDRICAL_SURFACE ( 'NONE', #50397, 0.2000000000000005107 ) ;
#50675=ORIENTED_EDGE ( 'NONE', *, *, #12729, .T. ) ;
#50679=LINE ( 'NONE', #2595, #25889 ) ;
#50691=AXIS2_PLACEMENT_3D ( 'NONE', #32354, #48617, #69481 ) ;
#50698=VECTOR ( 'NONE', #6429, 1000.000000000000000 ) ;
#50700=CARTESIAN_POINT ( 'NONE',  ( -9.690000000000001279, 9.750000000000001776, -5.000000000000000000 ) ) ;
#50702=DIRECTION ( 'NONE',  ( 0.000000000000000000, 0.000000000000000000, -1.000000000000000000 ) ) ;
#50703=DIRECTION ( 'NONE',  ( -0.000000000000000000, 0.000000000000000000, 1.000000000000000000 ) ) ;
#50706=VECTOR ( 'NONE', #66548, 1000.000000000000000 ) ;
#50713=AXIS2_PLACEMENT_3D ( 'NONE', #9802, #16487, #22824 ) ;
#50717=ORIENTED_EDGE ( 'NONE', *, *, #13790, .T. ) ;
#50720=CARTESIAN_POINT ( 'NONE',  ( 8.250000000000005329, 0.000000000000000000, -16.00000000000000000 ) ) ;
#50724=FACE_OUTER_BOUND ( 'NONE', #5136, .T. ) ;
#50729=DIRECTION ( 'NONE',  ( 0.000000000000000000, 0.000000000000000000, 1.000000000000000000 ) ) ;
#50734=CARTESIAN_POINT ( 'NONE',  ( -7.450000000000001954, -7.249999999999998224, -16.00000000000000000 ) ) ;
#50738=PLANE ( 'NONE',  #45801 ) ;
#50743=VECTOR ( 'NONE', #56404, 1000.000000000000000 ) ;
#50744=PLANE ( 'NONE',  #62311 ) ;
#50745=ORIENTED_EDGE ( 'NONE', *, *, #26575, .F. ) ;
#50746=VECTOR ( 'NONE', #57989, 1000.000000000000000 ) ;
#50761=CARTESIAN_POINT ( 'NONE',  ( 7.250000000000005329, 8.250000000000001776, -26.00000000000001066 ) ) ;
#50771=EDGE_CURVE ( 'NONE', #34259, #8834, #45790, .T. ) ;
#50789=VECTOR ( 'NONE', #3095, 1000.000000000000000 ) ;
#50810=AXIS2_PLACEMENT_3D ( 'NONE', #60882, #6795, #12780 ) ;
#50828=CARTESIAN_POINT ( 'NONE',  ( 7.250000000000005329, -7.449999999999998401, -17.50000000000000000 ) ) ;
#50830=ORIENTED_EDGE ( 'NONE', *, *, #43588, .F. ) ;
#50833=ORIENTED_EDGE ( 'NONE', *, *, #28926, .F. ) ;
#50834=VERTEX_POINT ( 'NONE', #41890 ) ;
#50843=ORIENTED_EDGE ( 'NONE', *, *, #11569, .F. ) ;
#50847=DIRECTION ( 'NONE',  ( 1.000000000000000000, 0.000000000000000000, -0.000000000000000000 ) ) ;
#50859=CARTESIAN_POINT ( 'NONE',  ( 7.450000000000003730, -7.249999999999997335, -11.00000000000000000 ) ) ;
#50860=EDGE_CURVE ( 'NONE', #65338, #59076, #20665, .T. ) ;
#50861=VERTEX_POINT ( 'NONE', #42235 ) ;
#50863=AXIS2_PLACEMENT_3D ( 'NONE', #11327, #59781, #65435 ) ;
#50867=ADVANCED_FACE ( 'NONE', ( #14668 ), #57450, .T. ) ;
#50874=EDGE_CURVE ( 'NONE', #27858, #2479, #19976, .T. ) ;
#50876=VECTOR ( 'NONE', #57142, 1000.000000000000000 ) ;
#50879=ORIENTED_EDGE ( 'NONE', *, *, #54391, .T. ) ;
#50883=CARTESIAN_POINT ( 'NONE',  ( 7.749999999999998224, -7.348062532928000934, 5.000000000000000000 ) ) ;
#50884=EDGE_CURVE ( 'NONE', #58562, #56437, #30628, .T. ) ;
#50886=DIRECTION ( 'NONE',  ( -1.794541526872559352E-16, -1.000000000000000000, 0.000000000000000000 ) ) ;
#50889=CARTESIAN_POINT ( 'NONE',  ( 8.250000000000005329, 7.250000000000000888, -11.50000000000000000 ) ) ;
#50891=VECTOR ( 'NONE', #23840, 1000.000000000000000 ) ;
#50895=CARTESIAN_POINT ( 'NONE',  ( -7.250000000000000888, 7.450000000000003730, -8.500000000000000000 ) ) ;
#50904=AXIS2_PLACEMENT_3D ( 'NONE', #43114, #42772, #53742 ) ;
#50905=EDGE_CURVE ( 'NONE', #15739, #7880, #163, .T. ) ;
#50907=DIRECTION ( 'NONE',  ( -1.000000000000000000, 0.000000000000000000, 0.000000000000000000 ) ) ;
#50908=DIRECTION ( 'NONE',  ( 0.000000000000000000, 0.000000000000000000, 1.000000000000000000 ) ) ;
#50910=VECTOR ( 'NONE', #42592, 1000.000000000000000 ) ;
#50917=ORIENTED_EDGE ( 'NONE', *, *, #20163, .T. ) ;
#50927=ORIENTED_EDGE ( 'NONE', *, *, #31816, .F. ) ;
#50932=CARTESIAN_POINT ( 'NONE',  ( 0.000000000000000000, -7.449999999999998401, -18.50000000000000000 ) ) ;
#50934=ORIENTED_EDGE ( 'NONE', *, *, #61152, .F. ) ;
#50935=EDGE_CURVE ( 'NONE', #32668, #26887, #48706, .T. ) ;
#50936=PLANE ( 'NONE',  #61602 ) ;
#50941=ORIENTED_EDGE ( 'NONE', *, *, #40103, .T. ) ;
#50955=EDGE_CURVE ( 'NONE', #21453, #32498, #69819, .T. ) ;
#50956=PLANE ( 'NONE',  #47860 ) ;
#50959=VECTOR ( 'NONE', #5215, 1000.000000000000000 ) ;
#50962=CARTESIAN_POINT ( 'NONE',  ( -7.250000000000000888, 7.450000000000003730, -22.50000000000000000 ) ) ;
#50963=ADVANCED_FACE ( 'NONE', ( #54604 ), #1199, .F. ) ;
#50971=ORIENTED_EDGE ( 'NONE', *, *, #22465, .F. ) ;
#50980=CARTESIAN_POINT ( 'NONE',  ( 7.450000000000003730, -7.249999999999997335, -24.50000000000000000 ) ) ;
#50985=ORIENTED_EDGE ( 'NONE', *, *, #27557, .F. ) ;
#50986=DIRECTION ( 'NONE',  ( 0.000000000000000000, 0.000000000000000000, 1.000000000000000000 ) ) ;
#51001=DIRECTION ( 'NONE',  ( 1.000000000000000000, 0.000000000000000000, 0.000000000000000000 ) ) ;
#51004=ORIENTED_EDGE ( 'NONE', *, *, #51424, .T. ) ;
#51005=DIRECTION ( 'NONE',  ( -1.000000000000000000, 0.000000000000000000, 0.000000000000000000 ) ) ;
#51006=DIRECTION ( 'NONE',  ( 0.000000000000000000, 0.000000000000000000, 1.000000000000000000 ) ) ;
#51011=AXIS2_PLACEMENT_3D ( 'NONE', #59719, #21543, #58345 ) ;
#51013=EDGE_CURVE ( 'NONE', #27724, #56702, #65548, .T. ) ;
#51022=CARTESIAN_POINT ( 'NONE',  ( 9.689999999999999503, -10.50000000000000178, -4.250000000000000000 ) ) ;
#51039=ORIENTED_EDGE ( 'NONE', *, *, #11335, .T. ) ;
#51041=ORIENTED_EDGE ( 'NONE', *, *, #37165, .T. ) ;
#51045=VERTEX_POINT ( 'NONE', #40752 ) ;
#51050=EDGE_LOOP ( 'NONE', ( #54690, #19860, #64566, #65497 ) ) ;
#51053=EDGE_CURVE ( 'NONE', #36929, #9824, #47547, .T. ) ;
#51054=CARTESIAN_POINT ( 'NONE',  ( -7.250000000000000000, -7.449999999999998401, -12.50000000000000000 ) ) ;
#51057=VECTOR ( 'NONE', #16344, 1000.000000000000000 ) ;
#51059=EDGE_LOOP ( 'NONE', ( #28271, #41066, #69586, #66873 ) ) ;
#51065=ORIENTED_EDGE ( 'NONE', *, *, #30529, .F. ) ;
#51072=VECTOR ( 'NONE', #24296, 1000.000000000000000 ) ;
#51080=ORIENTED_EDGE ( 'NONE', *, *, #8385, .F. ) ;
#51105=ORIENTED_EDGE ( 'NONE', *, *, #8979, .T. ) ;
#51106=CIRCLE ( 'NONE', #56756, 0.1999999999999996503 ) ;
#51107=CARTESIAN_POINT ( 'NONE',  ( -7.450000000000001954, 0.000000000000000000, -11.50000000000000000 ) ) ;
#51108=ORIENTED_EDGE ( 'NONE', *, *, #52968, .F. ) ;
#51125=ORIENTED_EDGE ( 'NONE', *, *, #51541, .T. ) ;
#51126=CARTESIAN_POINT ( 'NONE',  ( -9.689999999999999503, -10.50000000000000178, 0.000000000000000000 ) ) ;
#51127=CARTESIAN_POINT ( 'NONE',  ( 8.250000000000005329, -8.249999999999998224, -26.00000000000001066 ) ) ;
#51129=CARTESIAN_POINT ( 'NONE',  ( 4.456444791733522252E-16, 7.450000000000002842, -17.50000000000000000 ) ) ;
#51131=VECTOR ( 'NONE', #53085, 1000.000000000000000 ) ;
#51159=EDGE_CURVE ( 'NONE', #4795, #47820, #12537, .T. ) ;
#51165=VECTOR ( 'NONE', #66325, 1000.000000000000000 ) ;
#51167=VECTOR ( 'NONE', #59141, 1000.000000000000000 ) ;
#51169=DIRECTION ( 'NONE',  ( 0.000000000000000000, 1.000000000000000000, 0.000000000000000000 ) ) ;
#51178=VERTEX_POINT ( 'NONE', #7526 ) ;
#51190=ORIENTED_EDGE ( 'NONE', *, *, #33843, .T. ) ;
#51191=VECTOR ( 'NONE', #40903, 1000.000000000000000 ) ;
#51202=FACE_BOUND ( 'NONE', #20910, .T. ) ;
#51208=VERTEX_POINT ( 'NONE', #67980 ) ;
#51210=AXIS2_PLACEMENT_3D ( 'NONE', #28297, #49869, #1424 ) ;
#51211=VECTOR ( 'NONE', #54351, 1000.000000000000000 ) ;
#51213=ORIENTED_EDGE ( 'NONE', *, *, #61200, .T. ) ;
#51219=CIRCLE ( 'NONE', #29767, 0.7499999999999997780 ) ;
#51223=CARTESIAN_POINT ( 'NONE',  ( 0.000000000000000000, -7.449999999999998401, -21.50000000000000000 ) ) ;
#51230=DIRECTION ( 'NONE',  ( 0.000000000000000000, 0.000000000000000000, -1.000000000000000000 ) ) ;
#51239=EDGE_CURVE ( 'NONE', #62306, #19389, #57366, .T. ) ;
#51256=FACE_OUTER_BOUND ( 'NONE', #7091, .T. ) ;
#51258=DIRECTION ( 'NONE',  ( -0.000000000000000000, -0.000000000000000000, 1.000000000000000000 ) ) ;
#51259=ADVANCED_FACE ( 'NONE', ( #69026 ), #30148, .F. ) ;
#51261=VECTOR ( 'NONE', #34193, 1000.000000000000000 ) ;
#51263=ORIENTED_EDGE ( 'NONE', *, *, #23183, .T. ) ;
#51265=DIRECTION ( 'NONE',  ( -1.000000000000000000, 0.000000000000000000, 0.000000000000000000 ) ) ;
#51270=AXIS2_PLACEMENT_3D ( 'NONE', #11836, #15169, #48995 ) ;
#51279=ORIENTED_EDGE ( 'NONE', *, *, #7806, .F. ) ;
#51288=ORIENTED_EDGE ( 'NONE', *, *, #1848, .T. ) ;
#51290=DIRECTION ( 'NONE',  ( 0.000000000000000000, 0.000000000000000000, 1.000000000000000000 ) ) ;
#51291=CARTESIAN_POINT ( 'NONE',  ( -7.450000000000001954, 0.000000000000000000, -15.00000000000000000 ) ) ;
#51294=DIRECTION ( 'NONE',  ( 0.000000000000000000, 0.000000000000000000, 1.000000000000000000 ) ) ;
#51298=DIRECTION ( 'NONE',  ( -0.000000000000000000, -0.000000000000000000, -1.000000000000000000 ) ) ;
#51299=LINE ( 'NONE', #34681, #41712 ) ;
#51325=DIRECTION ( 'NONE',  ( 0.000000000000000000, 0.000000000000000000, 1.000000000000000000 ) ) ;
#51336=DIRECTION ( 'NONE',  ( 1.000000000000000000, 0.000000000000000000, 0.000000000000000000 ) ) ;
#51337=DIRECTION ( 'NONE',  ( 1.000000000000000000, -0.000000000000000000, 0.000000000000000000 ) ) ;
#51338=CARTESIAN_POINT ( 'NONE',  ( 7.250000000000005329, 7.250000000000000888, -12.50000000000000000 ) ) ;
#51339=EDGE_CURVE ( 'NONE', #37116, #51208, #58439, .T. ) ;
#51340=EDGE_LOOP ( 'NONE', ( #46046, #64351, #55357, #19191 ) ) ;
#51355=CIRCLE ( 'NONE', #58132, 0.8100000000000017186 ) ;
#51356=DIRECTION ( 'NONE',  ( 0.000000000000000000, 0.000000000000000000, -1.000000000000000000 ) ) ;
#51363=EDGE_CURVE ( 'NONE', #15117, #28651, #37214, .T. ) ;
#51369=CARTESIAN_POINT ( 'NONE',  ( -8.250000000000000000, 7.250000000000001776, -8.000000000000000000 ) ) ;
#51377=EDGE_LOOP ( 'NONE', ( #30619, #36451, #56596, #61729 ) ) ;
#51380=CARTESIAN_POINT ( 'NONE',  ( 7.250000000000005329, 8.250000000000001776, -23.00000000000000000 ) ) ;
#51388=VECTOR ( 'NONE', #15430, 1000.000000000000000 ) ;
#51411=CARTESIAN_POINT ( 'NONE',  ( -7.250000000000000888, -8.249999999999998224, -21.00000000000000000 ) ) ;
#51416=CIRCLE ( 'NONE', #46871, 0.1999999999999996503 ) ;
#51421=VERTEX_POINT ( 'NONE', #53479 ) ;
#51424=EDGE_CURVE ( 'NONE', #60302, #65501, #64558, .T. ) ;
#51432=ORIENTED_EDGE ( 'NONE', *, *, #54969, .T. ) ;
#51436=EDGE_CURVE ( 'NONE', #17298, #61584, #65468, .T. ) ;
#51437=CIRCLE ( 'NONE', #25453, 0.9999999999999991118 ) ;
#51438=VERTEX_POINT ( 'NONE', #17024 ) ;
#51451=EDGE_CURVE ( 'NONE', #16300, #64382, #27298, .T. ) ;
#51455=ADVANCED_FACE ( 'NONE', ( #38257 ), #54861, .F. ) ;
#51459=ORIENTED_EDGE ( 'NONE', *, *, #24679, .F. ) ;
#51470=VECTOR ( 'NONE', #20271, 1000.000000000000000 ) ;
#51471=CIRCLE ( 'NONE', #20992, 0.9999999999999991118 ) ;
#51477=VECTOR ( 'NONE', #40084, 1000.000000000000000 ) ;
#51478=VECTOR ( 'NONE', #47294, 1000.000000000000000 ) ;
#51479=VECTOR ( 'NONE', #18058, 1000.000000000000000 ) ;
#51496=EDGE_CURVE ( 'NONE', #7623, #10256, #17716, .T. ) ;
#51500=EDGE_CURVE ( 'NONE', #32498, #34317, #39953, .T. ) ;
#51502=DIRECTION ( 'NONE',  ( 0.000000000000000000, 0.000000000000000000, -1.000000000000000000 ) ) ;
#51504=DIRECTION ( 'NONE',  ( -0.000000000000000000, -0.000000000000000000, -1.000000000000000000 ) ) ;
#51506=CARTESIAN_POINT ( 'NONE',  ( 7.450000000000004619, -1.336933437520057563E-15, -20.00000000000000000 ) ) ;
#51510=DIRECTION ( 'NONE',  ( 0.000000000000000000, 0.000000000000000000, 1.000000000000000000 ) ) ;
#51513=DIRECTION ( 'NONE',  ( 0.000000000000000000, -1.000000000000000000, -0.000000000000000000 ) ) ;
#51517=DIRECTION ( 'NONE',  ( 1.000000000000000000, 0.000000000000000000, 0.000000000000000000 ) ) ;
#51520=VECTOR ( 'NONE', #11414, 1000.000000000000000 ) ;
#51521=CIRCLE ( 'NONE', #26703, 1.000000000000000000 ) ;
#51528=LINE ( 'NONE', #20048, #40891 ) ;
#51535=VECTOR ( 'NONE', #49153, 1000.000000000000000 ) ;
#51537=CARTESIAN_POINT ( 'NONE',  ( -7.250000000000001776, -7.249999999999998224, -17.50000000000000000 ) ) ;
#51541=EDGE_CURVE ( 'NONE', #67695, #69235, #29507, .T. ) ;
#51566=ORIENTED_EDGE ( 'NONE', *, *, #18678, .F. ) ;
#51571=CIRCLE ( 'NONE', #25594, 1.000000000000000000 ) ;
#51573=CARTESIAN_POINT ( 'NONE',  ( 8.250000000000005329, 7.250000000000000888, -23.00000000000000000 ) ) ;
#51582=CIRCLE ( 'NONE', #42555, 0.8100000000000017186 ) ;
#51589=LINE ( 'NONE', #13744, #62201 ) ;
#51591=ORIENTED_EDGE ( 'NONE', *, *, #9938, .T. ) ;
#51593=EDGE_CURVE ( 'NONE', #40067, #15576, #29013, .T. ) ;
#51609=DIRECTION ( 'NONE',  ( -0.000000000000000000, -0.000000000000000000, -1.000000000000000000 ) ) ;
#51619=LINE ( 'NONE', #36399, #17535 ) ;
#51623=LINE ( 'NONE', #67885, #15798 ) ;
#51636=EDGE_CURVE ( 'NONE', #48269, #54080, #1443, .T. ) ;
#51637=CIRCLE ( 'NONE', #15512, 1.000000000000000000 ) ;
#51638=AXIS2_PLACEMENT_3D ( 'NONE', #62581, #30776, #67196 ) ;
#51641=VERTEX_POINT ( 'NONE', #26778 ) ;
#51643=CARTESIAN_POINT ( 'NONE',  ( 7.250000000000005329, 7.250000000000000888, -26.00000000000001066 ) ) ;
#51648=CARTESIAN_POINT ( 'NONE',  ( 7.450000000000004619, -1.336933437520057563E-15, -24.50000000000000000 ) ) ;
#51649=FACE_OUTER_BOUND ( 'NONE', #27637, .T. ) ;
#51665=DIRECTION ( 'NONE',  ( -0.000000000000000000, -0.000000000000000000, -1.000000000000000000 ) ) ;
#51669=CIRCLE ( 'NONE', #18907, 0.1999999999999996503 ) ;
#51681=EDGE_CURVE ( 'NONE', #59582, #64203, #20761, .T. ) ;
#51682=DIRECTION ( 'NONE',  ( -1.000000000000000000, 0.000000000000000000, 0.000000000000000000 ) ) ;
#51685=CARTESIAN_POINT ( 'NONE',  ( 7.250000000000005329, -7.249999999999998224, -26.00000000000001066 ) ) ;
#51688=AXIS2_PLACEMENT_3D ( 'NONE', #23197, #33804, #65317 ) ;
#51699=CARTESIAN_POINT ( 'NONE',  ( 7.250000000000005329, 7.250000000000000888, -21.00000000000000000 ) ) ;
#51706=CARTESIAN_POINT ( 'NONE',  ( -7.250000000000001776, -7.249999999999998224, -11.00000000000000000 ) ) ;
#51722=DIRECTION ( 'NONE',  ( -1.000000000000000000, 0.000000000000000000, 0.000000000000000000 ) ) ;
#51728=AXIS2_PLACEMENT_3D ( 'NONE', #67465, #1699, #17958 ) ;
#51732=CARTESIAN_POINT ( 'NONE',  ( 0.000000000000000000, -7.449999999999998401, -20.50000000000000000 ) ) ;
#51775=DIRECTION ( 'NONE',  ( 0.000000000000000000, 1.000000000000000000, 0.000000000000000000 ) ) ;
#51776=EDGE_CURVE ( 'NONE', #41058, #68319, #21462, .T. ) ;
#51783=AXIS2_PLACEMENT_3D ( 'NONE', #14464, #16817, #22119 ) ;
#51795=CYLINDRICAL_SURFACE ( 'NONE', #14374, 1.000000000000000000 ) ;
#51800=DIRECTION ( 'NONE',  ( -1.000000000000000000, 0.000000000000000000, 0.000000000000000000 ) ) ;
#51801=EDGE_CURVE ( 'NONE', #18984, #69246, #69205, .T. ) ;
#51804=CARTESIAN_POINT ( 'NONE',  ( 7.250000000000005329, -8.249999999999998224, -26.00000000000001066 ) ) ;
#51808=CARTESIAN_POINT ( 'NONE',  ( 9.690000000000001279, 8.750000000000000000, -7.000000000000000000 ) ) ;
#51815=CIRCLE ( 'NONE', #40496, 1.000000000000000000 ) ;
#51819=FACE_OUTER_BOUND ( 'NONE', #22515, .T. ) ;
#51832=EDGE_CURVE ( 'NONE', #51045, #52304, #5898, .T. ) ;
#51835=EDGE_CURVE ( 'NONE', #5241, #36344, #21809, .T. ) ;
#51839=FACE_OUTER_BOUND ( 'NONE', #5757, .T. ) ;
#51841=ORIENTED_EDGE ( 'NONE', *, *, #7408, .T. ) ;
#51844=VECTOR ( 'NONE', #56099, 1000.000000000000000 ) ;
#51851=CARTESIAN_POINT ( 'NONE',  ( -7.250000000000000000, -7.449999999999998401, -23.50000000000000000 ) ) ;
#51858=LINE ( 'NONE', #51506, #1717 ) ;
#51862=CARTESIAN_POINT ( 'NONE',  ( 7.250000000000005329, 7.250000000000000888, -26.00000000000001066 ) ) ;
#51867=ORIENTED_EDGE ( 'NONE', *, *, #11775, .F. ) ;
#51868=CARTESIAN_POINT ( 'NONE',  ( 7.450000000000003730, -7.249999999999997335, -23.00000000000000000 ) ) ;
#51872=AXIS2_PLACEMENT_3D ( 'NONE', #44154, #17283, #60409 ) ;
#51878=ORIENTED_EDGE ( 'NONE', *, *, #32575, .F. ) ;
#51880=LINE ( 'NONE', #23947, #32738 ) ;
#51882=DIRECTION ( 'NONE',  ( 1.000000000000000000, -5.981805089575194965E-17, 0.000000000000000000 ) ) ;
#51890=EDGE_CURVE ( 'NONE', #24192, #58614, #49391, .T. ) ;
#51891=DIRECTION ( 'NONE',  ( 0.000000000000000000, 1.000000000000000000, 0.000000000000000000 ) ) ;
#51898=CIRCLE ( 'NONE', #60912, 0.2000000000000005107 ) ;
#51899=ADVANCED_FACE ( 'NONE', ( #38090, #33108 ), #17189, .T. ) ;
#51901=CARTESIAN_POINT ( 'NONE',  ( 7.250000000000005329, 8.250000000000001776, -13.50000000000000178 ) ) ;
#51905=FACE_OUTER_BOUND ( 'NONE', #68894, .T. ) ;
#51912=ORIENTED_EDGE ( 'NONE', *, *, #13180, .F. ) ;
#51917=FACE_BOUND ( 'NONE', #65846, .T. ) ;
#51920=ADVANCED_FACE ( 'NONE', ( #45442 ), #57458, .F. ) ;
#51922=DIRECTION ( 'NONE',  ( 0.000000000000000000, 0.000000000000000000, -1.000000000000000000 ) ) ;
#51924=AXIS2_PLACEMENT_3D ( 'NONE', #34842, #7629, #62065 ) ;
#51929=DIRECTION ( 'NONE',  ( 1.000000000000000000, 0.000000000000000000, 0.000000000000000000 ) ) ;
#51930=ORIENTED_EDGE ( 'NONE', *, *, #33843, .F. ) ;
#51931=ORIENTED_EDGE ( 'NONE', *, *, #18678, .T. ) ;
#51935=LINE ( 'NONE', #34949, #31278 ) ;
#51949=CIRCLE ( 'NONE', #28213, 0.1999999999999996503 ) ;
#51957=DIRECTION ( 'NONE',  ( -0.000000000000000000, -0.000000000000000000, 1.000000000000000000 ) ) ;
#51958=CARTESIAN_POINT ( 'NONE',  ( 7.250000000000005329, 7.250000000000000888, -21.50000000000000000 ) ) ;
#51959=DIRECTION ( 'NONE',  ( 1.000000000000000000, -5.981805089575194965E-17, 0.000000000000000000 ) ) ;
#51962=VECTOR ( 'NONE', #20010, 1000.000000000000000 ) ;
#51964=ORIENTED_EDGE ( 'NONE', *, *, #31529, .T. ) ;
#51971=CIRCLE ( 'NONE', #23745, 0.1999999999999987899 ) ;
#51984=ADVANCED_FACE ( 'NONE', ( #7962 ), #35534, .T. ) ;
#51991=ADVANCED_FACE ( 'NONE', ( #66673 ), #30252, .F. ) ;
#51993=FACE_OUTER_BOUND ( 'NONE', #26888, .T. ) ;
#51995=ORIENTED_EDGE ( 'NONE', *, *, #62422, .F. ) ;
#52002=DIRECTION ( 'NONE',  ( 0.000000000000000000, 0.000000000000000000, -1.000000000000000000 ) ) ;
#52003=VECTOR ( 'NONE', #20554, 1000.000000000000000 ) ;
#52010=VERTEX_POINT ( 'NONE', #56068 ) ;
#52015=ORIENTED_EDGE ( 'NONE', *, *, #6875, .F. ) ;
#52018=CARTESIAN_POINT ( 'NONE',  ( -7.250000000000001776, -7.249999999999998224, -7.500000000000000000 ) ) ;
#52024=ORIENTED_EDGE ( 'NONE', *, *, #13487, .F. ) ;
#52037=LINE ( 'NONE', #68655, #8677 ) ;
#52039=VECTOR ( 'NONE', #11958, 1000.000000000000000 ) ;
#52041=FACE_OUTER_BOUND ( 'NONE', #35997, .T. ) ;
#52045=LINE ( 'NONE', #19503, #29984 ) ;
#52050=VECTOR ( 'NONE', #20814, 1000.000000000000000 ) ;
#52058=CYLINDRICAL_SURFACE ( 'NONE', #30483, 1.000000000000000000 ) ;
#52059=ORIENTED_EDGE ( 'NONE', *, *, #4552, .T. ) ;
#52060=ORIENTED_EDGE ( 'NONE', *, *, #43926, .F. ) ;
#52067=ORIENTED_EDGE ( 'NONE', *, *, #36789, .F. ) ;
#52071=ORIENTED_EDGE ( 'NONE', *, *, #13336, .T. ) ;
#52074=CARTESIAN_POINT ( 'NONE',  ( 7.450000000000003730, -7.249999999999997335, -19.00000000000000000 ) ) ;
#52075=CARTESIAN_POINT ( 'NONE',  ( 7.250000000000005329, 8.250000000000001776, -26.00000000000001066 ) ) ;
#52086=AXIS2_PLACEMENT_3D ( 'NONE', #59296, #11199, #59651 ) ;
#52089=LINE ( 'NONE', #20604, #69399 ) ;
#52103=ORIENTED_EDGE ( 'NONE', *, *, #51835, .F. ) ;
#52107=ORIENTED_EDGE ( 'NONE', *, *, #44140, .F. ) ;
#52110=CIRCLE ( 'NONE', #57761, 1.000000000000000000 ) ;
#52113=ORIENTED_EDGE ( 'NONE', *, *, #53056, .T. ) ;
#52122=DIRECTION ( 'NONE',  ( -1.000000000000000000, 0.000000000000000000, 0.000000000000000000 ) ) ;
#52132=EDGE_LOOP ( 'NONE', ( #65763, #28939, #6034, #19995 ) ) ;
#52137=DIRECTION ( 'NONE',  ( 0.000000000000000000, 0.000000000000000000, 1.000000000000000000 ) ) ;
#52144=FACE_OUTER_BOUND ( 'NONE', #45052, .T. ) ;
#52150=DIRECTION ( 'NONE',  ( 1.000000000000000000, 0.000000000000000000, 0.000000000000000000 ) ) ;
#52153=ORIENTED_EDGE ( 'NONE', *, *, #60821, .T. ) ;
#52165=EDGE_LOOP ( 'NONE', ( #64618, #8562, #37617, #17786 ) ) ;
#52195=CARTESIAN_POINT ( 'NONE',  ( -7.250000000000000888, 7.250000000000001776, -18.50000000000000000 ) ) ;
#52198=CARTESIAN_POINT ( 'NONE',  ( -6.749999999999998224, -7.348062532927999158, 5.000000000000000000 ) ) ;
#52202=CARTESIAN_POINT ( 'NONE',  ( 8.250000000000005329, -8.249999999999998224, -26.00000000000001066 ) ) ;
#52204=DIRECTION ( 'NONE',  ( -1.000000000000000000, 0.000000000000000000, 0.000000000000000000 ) ) ;
#52205=AXIS2_PLACEMENT_3D ( 'NONE', #63179, #20396, #14402 ) ;
#52206=ADVANCED_FACE ( 'NONE', ( #19991 ), #52521, .F. ) ;
#52209=DIRECTION ( 'NONE',  ( -1.000000000000000000, 0.000000000000000000, 0.000000000000000000 ) ) ;
#52214=CARTESIAN_POINT ( 'NONE',  ( 7.250000000000005329, 7.250000000000000888, -8.500000000000000000 ) ) ;
#52215=ADVANCED_FACE ( 'NONE', ( #20337 ), #41901, .T. ) ;
#52218=DIRECTION ( 'NONE',  ( -1.794541526872559352E-16, -1.000000000000000000, 0.000000000000000000 ) ) ;
#52219=CARTESIAN_POINT ( 'NONE',  ( -7.450000000000001954, 0.000000000000000000, -12.00000000000000000 ) ) ;
#52230=DIRECTION ( 'NONE',  ( -1.000000000000000000, 0.000000000000000000, 0.000000000000000000 ) ) ;
#52232=CYLINDRICAL_SURFACE ( 'NONE', #22662, 0.1999999999999996503 ) ;
#52245=AXIS2_PLACEMENT_3D ( 'NONE', #14529, #41398, #31509 ) ;
#52267=EDGE_CURVE ( 'NONE', #19060, #49394, #10767, .T. ) ;
#52280=EDGE_CURVE ( 'NONE', #57776, #62704, #47691, .T. ) ;
#52286=AXIS2_PLACEMENT_3D ( 'NONE', #11711, #34308, #38939 ) ;
#52304=VERTEX_POINT ( 'NONE', #16779 ) ;
#52305=LINE ( 'NONE', #63263, #7542 ) ;
#52310=DIRECTION ( 'NONE',  ( -1.000000000000000000, 0.000000000000000000, -0.000000000000000000 ) ) ;
#52311=CIRCLE ( 'NONE', #22922, 0.2000000000000005107 ) ;
#52319=ORIENTED_EDGE ( 'NONE', *, *, #42887, .T. ) ;
#52340=ADVANCED_FACE ( 'NONE', ( #45015 ), #34052, .T. ) ;
#52351=CIRCLE ( 'NONE', #48974, 1.000000000000000000 ) ;
#52355=CIRCLE ( 'NONE', #56815, 1.000000000000000000 ) ;
#52365=ORIENTED_EDGE ( 'NONE', *, *, #51500, .F. ) ;
#52381=PLANE ( 'NONE',  #23070 ) ;
#52387=DIRECTION ( 'NONE',  ( -0.000000000000000000, -0.000000000000000000, -1.000000000000000000 ) ) ;
#52389=EDGE_CURVE ( 'NONE', #43073, #39553, #18486, .T. ) ;
#52391=EDGE_LOOP ( 'NONE', ( #33067, #11449, #54862, #63168 ) ) ;
#52400=CARTESIAN_POINT ( 'NONE',  ( -7.250000000000001776, -7.249999999999998224, -22.00000000000000000 ) ) ;
#52402=VECTOR ( 'NONE', #36373, 1000.000000000000000 ) ;
#52415=VERTEX_POINT ( 'NONE', #57027 ) ;
#52426=CARTESIAN_POINT ( 'NONE',  ( 7.250000000000005329, -7.249999999999998224, -17.00000000000000000 ) ) ;
#52433=CARTESIAN_POINT ( 'NONE',  ( -7.450000000000001954, 7.250000000000000000, -21.50000000000000000 ) ) ;
#52435=EDGE_CURVE ( 'NONE', #27762, #60691, #18146, .T. ) ;
#52444=EDGE_LOOP ( 'NONE', ( #21466, #63942, #13769, #59135 ) ) ;
#52453=ORIENTED_EDGE ( 'NONE', *, *, #66985, .T. ) ;
#52456=ORIENTED_EDGE ( 'NONE', *, *, #49690, .F. ) ;
#52468=CARTESIAN_POINT ( 'NONE',  ( 7.250000000000005329, -7.449999999999998401, -19.50000000000000000 ) ) ;
#52479=DIRECTION ( 'NONE',  ( -1.794541526872559352E-16, -1.000000000000000000, 0.000000000000000000 ) ) ;
#52485=DIRECTION ( 'NONE',  ( -0.000000000000000000, -0.000000000000000000, 1.000000000000000000 ) ) ;
#52487=DIRECTION ( 'NONE',  ( -1.000000000000000000, 0.000000000000000000, 0.000000000000000000 ) ) ;
#52498=PLANE ( 'NONE',  #7595 ) ;
#52500=AXIS2_PLACEMENT_3D ( 'NONE', #18656, #12298, #66749 ) ;
#52501=EDGE_LOOP ( 'NONE', ( #14990, #67284, #36404, #51065 ) ) ;
#52507=DIRECTION ( 'NONE',  ( -1.000000000000000000, 0.000000000000000000, 0.000000000000000000 ) ) ;
#52513=FACE_OUTER_BOUND ( 'NONE', #29970, .T. ) ;
#52521=PLANE ( 'NONE',  #38658 ) ;
#52523=ORIENTED_EDGE ( 'NONE', *, *, #334, .F. ) ;
#52524=EDGE_CURVE ( 'NONE', #57275, #19769, #62586, .T. ) ;
#52525=ORIENTED_EDGE ( 'NONE', *, *, #47422, .F. ) ;
#52532=ORIENTED_EDGE ( 'NONE', *, *, #26223, .F. ) ;
#52543=ORIENTED_EDGE ( 'NONE', *, *, #11274, .F. ) ;
#52546=VECTOR ( 'NONE', #51959, 1000.000000000000000 ) ;
#52547=AXIS2_PLACEMENT_3D ( 'NONE', #1635, #49413, #43749 ) ;
#52550=CARTESIAN_POINT ( 'NONE',  ( -7.250000000000001776, -7.249999999999998224, -14.00000000000000000 ) ) ;
#52561=CARTESIAN_POINT ( 'NONE',  ( 7.250000000000005329, -8.249999999999998224, -13.50000000000000178 ) ) ;
#52574=EDGE_CURVE ( 'NONE', #58003, #36321, #42162, .T. ) ;
#52575=VERTEX_POINT ( 'NONE', #52804 ) ;
#52576=FACE_OUTER_BOUND ( 'NONE', #6179, .T. ) ;
#52583=DIRECTION ( 'NONE',  ( 0.000000000000000000, 0.000000000000000000, 1.000000000000000000 ) ) ;
#52606=AXIS2_PLACEMENT_3D ( 'NONE', #26961, #38268, #49558 ) ;
#52608=ORIENTED_EDGE ( 'NONE', *, *, #19390, .F. ) ;
#52610=CARTESIAN_POINT ( 'NONE',  ( 8.750000000000003553, 7.750000000000000000, 5.000000000000000000 ) ) ;
#52611=ORIENTED_EDGE ( 'NONE', *, *, #28874, .F. ) ;
#52634=VERTEX_POINT ( 'NONE', #47471 ) ;
#52635=CARTESIAN_POINT ( 'NONE',  ( 7.250000000000005329, -7.249999999999998224, -26.00000000000001066 ) ) ;
#52647=VECTOR ( 'NONE', #68768, 1000.000000000000000 ) ;
#52652=VECTOR ( 'NONE', #25853, 1000.000000000000000 ) ;
#52654=EDGE_CURVE ( 'NONE', #17991, #31578, #46763, .T. ) ;
#52658=LINE ( 'NONE', #31445, #52402 ) ;
#52659=ORIENTED_EDGE ( 'NONE', *, *, #66979, .F. ) ;
#52662=CIRCLE ( 'NONE', #30074, 0.9999999999999991118 ) ;
#52666=PLANE ( 'NONE',  #6853 ) ;
#52667=CIRCLE ( 'NONE', #49283, 0.06000000000000102474 ) ;
#52672=CARTESIAN_POINT ( 'NONE',  ( -8.250000000000001776, 0.000000000000000000, -15.00000000000000000 ) ) ;
#52692=VERTEX_POINT ( 'NONE', #33642 ) ;
#52697=ADVANCED_FACE ( 'NONE', ( #55214 ), #60160, .F. ) ;
#52699=VECTOR ( 'NONE', #63695, 1000.000000000000000 ) ;
#52705=EDGE_LOOP ( 'NONE', ( #32801, #25187, #15162, #40757 ) ) ;
#52708=CIRCLE ( 'NONE', #56105, 0.2000000000000005107 ) ;
#52716=DIRECTION ( 'NONE',  ( 0.000000000000000000, 1.000000000000000000, 0.000000000000000000 ) ) ;
#52732=ORIENTED_EDGE ( 'NONE', *, *, #26487, .F. ) ;
#52736=CARTESIAN_POINT ( 'NONE',  ( 7.250000000000005329, 8.250000000000001776, -26.00000000000001066 ) ) ;
#52743=ORIENTED_EDGE ( 'NONE', *, *, #68999, .T. ) ;
#52749=DIRECTION ( 'NONE',  ( -0.000000000000000000, -0.000000000000000000, -1.000000000000000000 ) ) ;
#52753=CARTESIAN_POINT ( 'NONE',  ( 4.456444791733522252E-16, 7.450000000000002842, -9.000000000000001776 ) ) ;
#52754=PLANE ( 'NONE',  #34612 ) ;
#52760=EDGE_CURVE ( 'NONE', #55829, #17506, #61409, .T. ) ;
#52765=VERTEX_POINT ( 'NONE', #65816 ) ;
#52766=CIRCLE ( 'NONE', #5369, 0.2000000000000005107 ) ;
#52767=VECTOR ( 'NONE', #20364, 1000.000000000000000 ) ;
#52793=ORIENTED_EDGE ( 'NONE', *, *, #53069, .F. ) ;
#52795=CARTESIAN_POINT ( 'NONE',  ( -9.690000000000001279, 9.690000000000001279, -4.250000000000000000 ) ) ;
#52798=EDGE_CURVE ( 'NONE', #53583, #65777, #484, .T. ) ;
#52804=CARTESIAN_POINT ( 'NONE',  ( -7.250000000000000888, -8.249999999999998224, -19.00000000000000000 ) ) ;
#52814=ADVANCED_FACE ( 'NONE', ( #7097 ), #19116, .T. ) ;
#52820=ORIENTED_EDGE ( 'NONE', *, *, #66438, .T. ) ;
#52829=EDGE_CURVE ( 'NONE', #59828, #18594, #33971, .T. ) ;
#52845=ADVANCED_FACE ( 'NONE', ( #50243 ), #66847, .F. ) ;
#52847=DIRECTION ( 'NONE',  ( 0.000000000000000000, 0.000000000000000000, -1.000000000000000000 ) ) ;
#52861=EDGE_LOOP ( 'NONE', ( #23186, #43733, #50406, #57310, #19020, #67132, #21749, #37763 ) ) ;
#52862=PLANE ( 'NONE',  #46221 ) ;
#52864=EDGE_CURVE ( 'NONE', #57125, #48543, #44939, .T. ) ;
#52866=AXIS2_PLACEMENT_3D ( 'NONE', #22732, #37970, #11088 ) ;
#52870=ORIENTED_EDGE ( 'NONE', *, *, #7420, .T. ) ;
#52885=ORIENTED_EDGE ( 'NONE', *, *, #41301, .F. ) ;
#52888=CARTESIAN_POINT ( 'NONE',  ( -7.250000000000000888, 7.250000000000001776, -26.00000000000001066 ) ) ;
#52901=ORIENTED_EDGE ( 'NONE', *, *, #37842, .F. ) ;
#52902=DIRECTION ( 'NONE',  ( 0.000000000000000000, 0.000000000000000000, -1.000000000000000000 ) ) ;
#52906=ORIENTED_EDGE ( 'NONE', *, *, #13366, .T. ) ;
#52907=VERTEX_POINT ( 'NONE', #58708 ) ;
#52908=CARTESIAN_POINT ( 'NONE',  ( 7.250000000000005329, 7.250000000000000888, -13.50000000000000178 ) ) ;
#52911=ORIENTED_EDGE ( 'NONE', *, *, #57016, .F. ) ;
#52913=CARTESIAN_POINT ( 'NONE',  ( 8.250000000000005329, -7.249999999999998224, -14.50000000000000000 ) ) ;
#52917=ORIENTED_EDGE ( 'NONE', *, *, #50935, .F. ) ;
#52920=DIRECTION ( 'NONE',  ( -0.000000000000000000, -0.000000000000000000, -1.000000000000000000 ) ) ;
#52933=DIRECTION ( 'NONE',  ( 0.000000000000000000, 0.000000000000000000, 1.000000000000000000 ) ) ;
#52944=CARTESIAN_POINT ( 'NONE',  ( 0.000000000000000000, 0.000000000000000000, -16.50000000000000000 ) ) ;
#52946=VERTEX_POINT ( 'NONE', #68619 ) ;
#52956=EDGE_LOOP ( 'NONE', ( #54411, #36590, #38589, #57765, #15283, #67023, #40959, #7989 ) ) ;
#52967=ORIENTED_EDGE ( 'NONE', *, *, #7151, .T. ) ;
#52968=EDGE_CURVE ( 'NONE', #13636, #34259, #24778, .T. ) ;
#52969=AXIS2_PLACEMENT_3D ( 'NONE', #5958, #5617, #309 ) ;
#52975=EDGE_CURVE ( 'NONE', #15576, #58661, #25353, .T. ) ;
#52979=DIRECTION ( 'NONE',  ( 0.000000000000000000, 0.000000000000000000, -1.000000000000000000 ) ) ;
#52991=DIRECTION ( 'NONE',  ( -1.000000000000000000, 0.000000000000000000, 0.000000000000000000 ) ) ;
#53017=VERTEX_POINT ( 'NONE', #30430 ) ;
#53018=DIRECTION ( 'NONE',  ( 0.000000000000000000, 1.000000000000000000, 0.000000000000000000 ) ) ;
#53019=DIRECTION ( 'NONE',  ( 1.000000000000000000, -5.981805089575196197E-17, 0.000000000000000000 ) ) ;
#53024=DIRECTION ( 'NONE',  ( -1.000000000000000000, 0.000000000000000000, 0.000000000000000000 ) ) ;
#53026=FACE_OUTER_BOUND ( 'NONE', #57280, .T. ) ;
#53032=ORIENTED_EDGE ( 'NONE', *, *, #6570, .T. ) ;
#53033=DIRECTION ( 'NONE',  ( 1.000000000000000000, -0.000000000000000000, 0.000000000000000000 ) ) ;
#53056=EDGE_CURVE ( 'NONE', #25235, #29129, #40014, .T. ) ;
#53060=ADVANCED_FACE ( 'NONE', ( #21567 ), #15918, .T. ) ;
#53066=CARTESIAN_POINT ( 'NONE',  ( 7.450000000000006395, 7.250000000000000888, -8.500000000000000000 ) ) ;
#53069=EDGE_CURVE ( 'NONE', #14810, #30263, #43414, .T. ) ;
#53070=ORIENTED_EDGE ( 'NONE', *, *, #45311, .T. ) ;
#53073=EDGE_CURVE ( 'NONE', #61999, #21563, #4960, .T. ) ;
#53076=AXIS2_PLACEMENT_3D ( 'NONE', #5724, #64090, #59803 ) ;
#53083=ORIENTED_EDGE ( 'NONE', *, *, #3178, .F. ) ;
#53085=DIRECTION ( 'NONE',  ( -1.000000000000000000, 0.000000000000000000, 0.000000000000000000 ) ) ;
#53099=CARTESIAN_POINT ( 'NONE',  ( 9.690000000000001279, 9.690000000000001279, -4.250000000000000000 ) ) ;
#53104=CARTESIAN_POINT ( 'NONE',  ( 7.450000000000006395, 7.250000000000000888, -16.50000000000000000 ) ) ;
#53111=VECTOR ( 'NONE', #21105, 1000.000000000000000 ) ;
#53115=CIRCLE ( 'NONE', #63234, 0.9999999999999991118 ) ;
#53120=VECTOR ( 'NONE', #37806, 1000.000000000000000 ) ;
#53121=PLANE ( 'NONE',  #57171 ) ;
#53124=VECTOR ( 'NONE', #14136, 1000.000000000000000 ) ;
#53131=EDGE_CURVE ( 'NONE', #17252, #2339, #21909, .T. ) ;
#53135=VECTOR ( 'NONE', #24955, 1000.000000000000000 ) ;
#53139=CARTESIAN_POINT ( 'NONE',  ( -7.450000000000001954, -7.249999999999998224, -21.50000000000000000 ) ) ;
#53140=DIRECTION ( 'NONE',  ( -0.000000000000000000, -0.000000000000000000, -1.000000000000000000 ) ) ;
#53144=ORIENTED_EDGE ( 'NONE', *, *, #34771, .F. ) ;
#53148=DIRECTION ( 'NONE',  ( -0.000000000000000000, -0.000000000000000000, 1.000000000000000000 ) ) ;
#53149=VECTOR ( 'NONE', #20964, 1000.000000000000000 ) ;
#53160=EDGE_CURVE ( 'NONE', #66073, #67897, #33556, .T. ) ;
#53167=EDGE_LOOP ( 'NONE', ( #38168, #25057, #49046, #63473 ) ) ;
#53171=EDGE_LOOP ( 'NONE', ( #20112, #32899, #39184, #38880 ) ) ;
#53172=LINE ( 'NONE', #69412, #5155 ) ;
#53191=FACE_OUTER_BOUND ( 'NONE', #19406, .T. ) ;
#53195=VERTEX_POINT ( 'NONE', #66426 ) ;
#53204=ORIENTED_EDGE ( 'NONE', *, *, #26705, .T. ) ;
#53209=DIRECTION ( 'NONE',  ( 0.000000000000000000, 0.000000000000000000, -1.000000000000000000 ) ) ;
#53213=CARTESIAN_POINT ( 'NONE',  ( -7.450000000000001954, 7.250000000000000000, -18.50000000000000000 ) ) ;
#53215=DIRECTION ( 'NONE',  ( 1.000000000000000000, 0.000000000000000000, 0.000000000000000000 ) ) ;
#53216=DIRECTION ( 'NONE',  ( -0.000000000000000000, 0.000000000000000000, 1.000000000000000000 ) ) ;
#53222=EDGE_CURVE ( 'NONE', #25548, #53017, #50514, .T. ) ;
#53225=ORIENTED_EDGE ( 'NONE', *, *, #22007, .F. ) ;
#53233=AXIS2_PLACEMENT_3D ( 'NONE', #21178, #69619, #41681 ) ;
#53238=EDGE_LOOP ( 'NONE', ( #55667, #15357, #44173, #18553, #19023, #66752, #10531, #24249 ) ) ;
#53241=DIRECTION ( 'NONE',  ( 1.000000000000000000, 0.000000000000000000, 0.000000000000000000 ) ) ;
#53242=FACE_OUTER_BOUND ( 'NONE', #13900, .T. ) ;
#53252=CARTESIAN_POINT ( 'NONE',  ( 8.689999999999999503, -8.750000000000000000, -7.000000000000000000 ) ) ;
#53256=CARTESIAN_POINT ( 'NONE',  ( 0.000000000000000000, -8.249999999999998224, -22.00000000000000000 ) ) ;
#53259=EDGE_LOOP ( 'NONE', ( #6858, #63876, #55607, #10584 ) ) ;
#53263=CARTESIAN_POINT ( 'NONE',  ( -8.750000000000001776, 0.000000000000000000, -26.00000000000001066 ) ) ;
#53268=PLANE ( 'NONE',  #10826 ) ;
#53290=CARTESIAN_POINT ( 'NONE',  ( 0.000000000000000000, -7.449999999999998401, -8.000000000000000000 ) ) ;
#53294=DIRECTION ( 'NONE',  ( 0.000000000000000000, 0.000000000000000000, 1.000000000000000000 ) ) ;
#53296=FACE_OUTER_BOUND ( 'NONE', #4274, .T. ) ;
#53300=AXIS2_PLACEMENT_3D ( 'NONE', #43504, #11661, #44 ) ;
#53302=VECTOR ( 'NONE', #17671, 1000.000000000000000 ) ;
#53307=LINE ( 'NONE', #67805, #10045 ) ;
#53312=DIRECTION ( 'NONE',  ( 1.000000000000000000, -0.000000000000000000, 0.000000000000000000 ) ) ;
#53315=CARTESIAN_POINT ( 'NONE',  ( 7.250000000000005329, 7.250000000000000888, -26.00000000000001066 ) ) ;
#53317=CARTESIAN_POINT ( 'NONE',  ( -7.250000000000001776, -7.249999999999998224, -19.00000000000000000 ) ) ;
#53337=LINE ( 'NONE', #10532, #8518 ) ;
#53341=DIRECTION ( 'NONE',  ( 1.000000000000000000, 0.000000000000000000, 0.000000000000000000 ) ) ;
#53343=ORIENTED_EDGE ( 'NONE', *, *, #47070, .F. ) ;
#53345=CARTESIAN_POINT ( 'NONE',  ( -7.450000000000001954, -7.249999999999998224, -10.50000000000000000 ) ) ;
#53346=DIRECTION ( 'NONE',  ( 0.000000000000000000, 0.000000000000000000, 1.000000000000000000 ) ) ;
#53351=DIRECTION ( 'NONE',  ( 0.000000000000000000, 0.000000000000000000, 1.000000000000000000 ) ) ;
#53359=DIRECTION ( 'NONE',  ( 1.000000000000000000, 0.000000000000000000, -0.000000000000000000 ) ) ;
#53363=ADVANCED_FACE ( 'NONE', ( #30698 ), #3818, .F. ) ;
#53370=ADVANCED_FACE ( 'NONE', ( #4184, #25756 ), #19374, .T. ) ;
#53376=CARTESIAN_POINT ( 'NONE',  ( -7.250000000000000000, -7.449999999999998401, -20.50000000000000000 ) ) ;
#53378=EDGE_LOOP ( 'NONE', ( #43792, #16542, #8311, #51964, #27550, #10581, #47938, #4921 ) ) ;
#53380=CARTESIAN_POINT ( 'NONE',  ( -8.250000000000001776, -8.249999999999998224, -26.00000000000001066 ) ) ;
#53387=EDGE_LOOP ( 'NONE', ( #47450, #30064, #57662, #38236 ) ) ;
#53400=ORIENTED_EDGE ( 'NONE', *, *, #43998, .F. ) ;
#53404=ORIENTED_EDGE ( 'NONE', *, *, #6846, .F. ) ;
#53406=CARTESIAN_POINT ( 'NONE',  ( 7.250000000000005329, 8.250000000000001776, -26.00000000000001066 ) ) ;
#53408=LINE ( 'NONE', #69307, #26458 ) ;
#53410=DIRECTION ( 'NONE',  ( 0.000000000000000000, 0.000000000000000000, 1.000000000000000000 ) ) ;
#53416=AXIS2_PLACEMENT_3D ( 'NONE', #47128, #68703, #20247 ) ;
#53424=DIRECTION ( 'NONE',  ( -1.000000000000000000, 0.000000000000000000, 0.000000000000000000 ) ) ;
#53431=CARTESIAN_POINT ( 'NONE',  ( -8.689999999999999503, 8.750000000000000000, -7.000000000000000000 ) ) ;
#53437=CYLINDRICAL_SURFACE ( 'NONE', #10235, 0.1999999999999996503 ) ;
#53455=CARTESIAN_POINT ( 'NONE',  ( -7.250000000000000888, 8.750000000000001776, -30.00000000000001066 ) ) ;
#53456=EDGE_CURVE ( 'NONE', #20195, #34803, #10174, .T. ) ;
#53469=DIRECTION ( 'NONE',  ( 0.000000000000000000, 0.000000000000000000, 1.000000000000000000 ) ) ;
#53471=ORIENTED_EDGE ( 'NONE', *, *, #9065, .T. ) ;
#53479=CARTESIAN_POINT ( 'NONE',  ( 7.450000000000003730, -7.249999999999997335, -8.500000000000000000 ) ) ;
#53480=VERTEX_POINT ( 'NONE', #64968 ) ;
#53481=ORIENTED_EDGE ( 'NONE', *, *, #4360, .F. ) ;
#53483=EDGE_LOOP ( 'NONE', ( #60328, #44114, #5235, #54140 ) ) ;
#53489=CARTESIAN_POINT ( 'NONE',  ( -7.250000000000001776, -7.249999999999998224, -7.500000000000000000 ) ) ;
#53490=DIRECTION ( 'NONE',  ( 0.000000000000000000, -1.000000000000000000, 0.000000000000000000 ) ) ;
#53494=ORIENTED_EDGE ( 'NONE', *, *, #7611, .F. ) ;
#53498=CARTESIAN_POINT ( 'NONE',  ( 7.250000000000005329, -8.249999999999998224, -9.000000000000001776 ) ) ;
#53503=ORIENTED_EDGE ( 'NONE', *, *, #23405, .T. ) ;
#53505=LINE ( 'NONE', #44861, #58787 ) ;
#53507=EDGE_CURVE ( 'NONE', #57928, #60252, #51898, .T. ) ;
#53509=DIRECTION ( 'NONE',  ( -1.000000000000000000, 0.000000000000000000, 0.000000000000000000 ) ) ;
#53512=DIRECTION ( 'NONE',  ( 0.000000000000000000, 0.000000000000000000, 1.000000000000000000 ) ) ;
#53515=ORIENTED_EDGE ( 'NONE', *, *, #57894, .T. ) ;
#53524=CARTESIAN_POINT ( 'NONE',  ( -7.450000000000001954, -7.249999999999998224, -20.50000000000000000 ) ) ;
#53530=CARTESIAN_POINT ( 'NONE',  ( 7.250000000000005329, -8.249999999999998224, -26.00000000000001066 ) ) ;
#53536=DIRECTION ( 'NONE',  ( 1.000000000000000000, -0.000000000000000000, 0.000000000000000000 ) ) ;
#53541=VERTEX_POINT ( 'NONE', #60963 ) ;
#53547=LINE ( 'NONE', #6139, #60903 ) ;
#53552=PLANE ( 'NONE',  #37640 ) ;
#53555=ADVANCED_FACE ( 'NONE', ( #17489 ), #39064, .F. ) ;
#53562=ORIENTED_EDGE ( 'NONE', *, *, #17405, .T. ) ;
#53567=DIRECTION ( 'NONE',  ( -1.000000000000000000, 0.000000000000000000, 0.000000000000000000 ) ) ;
#53573=VERTEX_POINT ( 'NONE', #12524 ) ;
#53583=VERTEX_POINT ( 'NONE', #33751 ) ;
#53603=VECTOR ( 'NONE', #69193, 1000.000000000000000 ) ;
#53610=AXIS2_PLACEMENT_3D ( 'NONE', #22498, #38742, #37371 ) ;
#53612=FACE_OUTER_BOUND ( 'NONE', #16248, .T. ) ;
#53617=CIRCLE ( 'NONE', #35565, 0.9999999999999991118 ) ;
#53628=VECTOR ( 'NONE', #36651, 1000.000000000000000 ) ;
#53631=PLANE ( 'NONE',  #63561 ) ;
#53637=CARTESIAN_POINT ( 'NONE',  ( -7.250000000000001776, -7.249999999999998224, -13.00000000000000178 ) ) ;
#53655=DIRECTION ( 'NONE',  ( 0.000000000000000000, 0.000000000000000000, -1.000000000000000000 ) ) ;
#53656=ORIENTED_EDGE ( 'NONE', *, *, #38041, .F. ) ;
#53665=EDGE_CURVE ( 'NONE', #26867, #59828, #24840, .T. ) ;
#53666=DIRECTION ( 'NONE',  ( 0.000000000000000000, 0.000000000000000000, 1.000000000000000000 ) ) ;
#53680=DIRECTION ( 'NONE',  ( -0.000000000000000000, -0.000000000000000000, -1.000000000000000000 ) ) ;
#53681=VECTOR ( 'NONE', #49286, 1000.000000000000000 ) ;
#53684=ORIENTED_EDGE ( 'NONE', *, *, #22950, .F. ) ;
#53689=CARTESIAN_POINT ( 'NONE',  ( 6.500000000000002665, 6.500000000000000888, -1.000000000000000000 ) ) ;
#53691=VERTEX_POINT ( 'NONE', #29842 ) ;
#53694=VERTEX_POINT ( 'NONE', #36552 ) ;
#53698=VECTOR ( 'NONE', #47288, 1000.000000000000000 ) ;
#53699=DIRECTION ( 'NONE',  ( -1.000000000000000000, 0.000000000000000000, 0.000000000000000000 ) ) ;
#53722=DIRECTION ( 'NONE',  ( 1.000000000000000000, -0.000000000000000000, 0.000000000000000000 ) ) ;
#53726=CIRCLE ( 'NONE', #36768, 1.000000000000000000 ) ;
#53731=ORIENTED_EDGE ( 'NONE', *, *, #61200, .F. ) ;
#53742=DIRECTION ( 'NONE',  ( -1.000000000000000000, 0.000000000000000000, 0.000000000000000000 ) ) ;
#53752=DIRECTION ( 'NONE',  ( -0.000000000000000000, -0.000000000000000000, 1.000000000000000000 ) ) ;
#53756=CARTESIAN_POINT ( 'NONE',  ( 7.450000000000003730, -7.249999999999997335, -12.50000000000000000 ) ) ;
#53761=EDGE_CURVE ( 'NONE', #32685, #35273, #24897, .T. ) ;
#53763=EDGE_CURVE ( 'NONE', #29352, #5145, #30904, .T. ) ;
#53771=VECTOR ( 'NONE', #41729, 1000.000000000000000 ) ;
#53779=CARTESIAN_POINT ( 'NONE',  ( 8.250000000000005329, 0.000000000000000000, -10.50000000000000000 ) ) ;
#53780=VERTEX_POINT ( 'NONE', #31616 ) ;
#53787=CYLINDRICAL_SURFACE ( 'NONE', #13143, 1.000000000000001776 ) ;
#53793=DIRECTION ( 'NONE',  ( 0.000000000000000000, 0.000000000000000000, 1.000000000000000000 ) ) ;
#53794=DIRECTION ( 'NONE',  ( 0.000000000000000000, 1.000000000000000000, 0.000000000000000000 ) ) ;
#53804=EDGE_CURVE ( 'NONE', #10955, #15345, #32650, .T. ) ;
#53807=ORIENTED_EDGE ( 'NONE', *, *, #5396, .T. ) ;
#53815=VECTOR ( 'NONE', #7125, 1000.000000000000000 ) ;
#53816=DIRECTION ( 'NONE',  ( 0.000000000000000000, 0.000000000000000000, 1.000000000000000000 ) ) ;
#53817=VECTOR ( 'NONE', #23756, 1000.000000000000000 ) ;
#53819=VECTOR ( 'NONE', #67503, 1000.000000000000000 ) ;
#53820=VERTEX_POINT ( 'NONE', #42204 ) ;
#53821=DIRECTION ( 'NONE',  ( 1.000000000000000000, 0.000000000000000000, 0.000000000000000000 ) ) ;
#53830=CARTESIAN_POINT ( 'NONE',  ( 7.250000000000005329, 7.250000000000000888, -15.00000000000000000 ) ) ;
#53859=DIRECTION ( 'NONE',  ( 0.000000000000000000, 0.000000000000000000, 1.000000000000000000 ) ) ;
#53871=EDGE_CURVE ( 'NONE', #8765, #59076, #51949, .T. ) ;
#53875=DIRECTION ( 'NONE',  ( -1.000000000000000000, 0.000000000000000000, 0.000000000000000000 ) ) ;
#53885=CARTESIAN_POINT ( 'NONE',  ( 9.750000000000001776, 9.690000000000001279, -4.250000000000000000 ) ) ;
#53886=CIRCLE ( 'NONE', #25497, 0.2000000000000005107 ) ;
#53890=CARTESIAN_POINT ( 'NONE',  ( 7.250000000000005329, 7.250000000000000888, -13.00000000000000178 ) ) ;
#53895=ADVANCED_FACE ( 'NONE', ( #53191 ), #10386, .T. ) ;
#53899=VERTEX_POINT ( 'NONE', #16042 ) ;
#53903=CARTESIAN_POINT ( 'NONE',  ( 0.000000000000000000, -8.249999999999998224, -11.00000000000000000 ) ) ;
#53907=DIRECTION ( 'NONE',  ( 1.000000000000000000, -5.981805089575194965E-17, 0.000000000000000000 ) ) ;
#53913=DIRECTION ( 'NONE',  ( 0.000000000000000000, 0.000000000000000000, 1.000000000000000000 ) ) ;
#53928=ORIENTED_EDGE ( 'NONE', *, *, #13366, .F. ) ;
#53934=DIRECTION ( 'NONE',  ( 0.000000000000000000, 0.000000000000000000, 1.000000000000000000 ) ) ;
#53950=CARTESIAN_POINT ( 'NONE',  ( -8.250000000000001776, -7.249999999999998224, -26.00000000000001066 ) ) ;
#53954=CARTESIAN_POINT ( 'NONE',  ( 0.000000000000000000, -7.449999999999998401, -17.50000000000000000 ) ) ;
#53960=CIRCLE ( 'NONE', #62817, 1.000000000000000000 ) ;
#53962=DIRECTION ( 'NONE',  ( 0.000000000000000000, 0.000000000000000000, 1.000000000000000000 ) ) ;
#53964=ORIENTED_EDGE ( 'NONE', *, *, #31063, .T. ) ;
#53966=VECTOR ( 'NONE', #56645, 1000.000000000000000 ) ;
#53975=ADVANCED_FACE ( 'NONE', ( #55939 ), #38981, .F. ) ;
#53982=PLANE ( 'NONE',  #26749 ) ;
#53989=DIRECTION ( 'NONE',  ( 0.000000000000000000, 0.000000000000000000, 1.000000000000000000 ) ) ;
#53996=CARTESIAN_POINT ( 'NONE',  ( 7.250000000000005329, -8.249999999999998224, -26.00000000000001066 ) ) ;
#54004=ORIENTED_EDGE ( 'NONE', *, *, #65634, .T. ) ;
#54013=EDGE_CURVE ( 'NONE', #23929, #28003, #49595, .T. ) ;
#54022=AXIS2_PLACEMENT_3D ( 'NONE', #14084, #18328, #40952 ) ;
#54024=CARTESIAN_POINT ( 'NONE',  ( -7.450000000000001954, 7.250000000000000000, -7.000000000000000000 ) ) ;
#54026=VERTEX_POINT ( 'NONE', #45312 ) ;
#54029=LINE ( 'NONE', #69923, #60445 ) ;
#54033=EDGE_CURVE ( 'NONE', #32512, #62786, #837, .T. ) ;
#54045=DIRECTION ( 'NONE',  ( 1.000000000000000000, 0.000000000000000000, 0.000000000000000000 ) ) ;
#54046=ORIENTED_EDGE ( 'NONE', *, *, #23920, .F. ) ;
#54053=ORIENTED_EDGE ( 'NONE', *, *, #407, .F. ) ;
#54055=LINE ( 'NONE', #52672, #48555 ) ;
#54059=CARTESIAN_POINT ( 'NONE',  ( 8.250000000000005329, 7.250000000000000888, -26.00000000000001066 ) ) ;
#54060=ORIENTED_EDGE ( 'NONE', *, *, #59543, .F. ) ;
#54062=CYLINDRICAL_SURFACE ( 'NONE', #52969, 1.000000000000000000 ) ;
#54064=EDGE_CURVE ( 'NONE', #31930, #44295, #57335, .T. ) ;
#54067=ORIENTED_EDGE ( 'NONE', *, *, #38041, .T. ) ;
#54070=DIRECTION ( 'NONE',  ( 0.000000000000000000, 0.000000000000000000, 1.000000000000000000 ) ) ;
#54074=CARTESIAN_POINT ( 'NONE',  ( 8.250000000000005329, 7.250000000000000888, -18.00000000000000000 ) ) ;
#54080=VERTEX_POINT ( 'NONE', #56972 ) ;
#54085=LINE ( 'NONE', #65039, #43845 ) ;
#54100=DIRECTION ( 'NONE',  ( 0.000000000000000000, 0.000000000000000000, 1.000000000000000000 ) ) ;
#54104=ORIENTED_EDGE ( 'NONE', *, *, #20622, .T. ) ;
#54105=ORIENTED_EDGE ( 'NONE', *, *, #63649, .T. ) ;
#54110=EDGE_CURVE ( 'NONE', #57928, #2646, #57684, .T. ) ;
#54113=EDGE_CURVE ( 'NONE', #28873, #17252, #68657, .T. ) ;
#54119=VERTEX_POINT ( 'NONE', #30110 ) ;
#54120=VECTOR ( 'NONE', #62805, 1000.000000000000000 ) ;
#54121=CARTESIAN_POINT ( 'NONE',  ( 7.450000000000004619, -1.336933437520057563E-15, -21.50000000000000000 ) ) ;
#54135=CARTESIAN_POINT ( 'NONE',  ( -7.250000000000001776, -7.249999999999998224, -25.00000000000000000 ) ) ;
#54139=CARTESIAN_POINT ( 'NONE',  ( 8.250000000000005329, -8.249999999999998224, -26.00000000000001066 ) ) ;
#54140=ORIENTED_EDGE ( 'NONE', *, *, #61369, .T. ) ;
#54146=ORIENTED_EDGE ( 'NONE', *, *, #56429, .F. ) ;
#54155=EDGE_CURVE ( 'NONE', #26887, #16332, #13495, .T. ) ;
#54158=DIRECTION ( 'NONE',  ( 0.000000000000000000, -1.000000000000000000, -0.000000000000000000 ) ) ;
#54159=FACE_OUTER_BOUND ( 'NONE', #14721, .T. ) ;
#54164=CIRCLE ( 'NONE', #8962, 1.000000000000000888 ) ;
#54166=VERTEX_POINT ( 'NONE', #50980 ) ;
#54174=DIRECTION ( 'NONE',  ( 1.000000000000000000, 0.000000000000000000, 0.000000000000000000 ) ) ;
#54181=CIRCLE ( 'NONE', #34903, 0.1999999999999996503 ) ;
#54185=FACE_BOUND ( 'NONE', #12921, .T. ) ;
#54188=DIRECTION ( 'NONE',  ( -0.000000000000000000, -0.000000000000000000, 1.000000000000000000 ) ) ;
#54194=CARTESIAN_POINT ( 'NONE',  ( -6.500000000000002665, 6.500000000000002665, 0.000000000000000000 ) ) ;
#54195=PLANE ( 'NONE',  #28697 ) ;
#54199=ORIENTED_EDGE ( 'NONE', *, *, #57016, .T. ) ;
#54217=VERTEX_POINT ( 'NONE', #14908 ) ;
#54221=LINE ( 'NONE', #21688, #51520 ) ;
#54227=EDGE_LOOP ( 'NONE', ( #54238, #42220, #36691, #54606 ) ) ;
#54234=DIRECTION ( 'NONE',  ( -0.000000000000000000, -0.000000000000000000, 1.000000000000000000 ) ) ;
#54235=VECTOR ( 'NONE', #39661, 1000.000000000000000 ) ;
#54238=ORIENTED_EDGE ( 'NONE', *, *, #50221, .T. ) ;
#54245=DIRECTION ( 'NONE',  ( -0.000000000000000000, -0.000000000000000000, -1.000000000000000000 ) ) ;
#54247=ORIENTED_EDGE ( 'NONE', *, *, #36968, .T. ) ;
#54249=DIRECTION ( 'NONE',  ( -8.951101527228104953E-17, -1.000000000000000000, 0.000000000000000000 ) ) ;
#54257=DIRECTION ( 'NONE',  ( 1.000000000000000000, -8.951101527228104953E-17, 0.000000000000000000 ) ) ;
#54259=ADVANCED_FACE ( 'NONE', ( #47773 ), #10637, .T. ) ;
#54262=DIRECTION ( 'NONE',  ( -5.981805089575196197E-17, -1.000000000000000000, 0.000000000000000000 ) ) ;
#54274=DIRECTION ( 'NONE',  ( 0.000000000000000000, 0.000000000000000000, 1.000000000000000000 ) ) ;
#54281=ORIENTED_EDGE ( 'NONE', *, *, #33560, .F. ) ;
#54285=ORIENTED_EDGE ( 'NONE', *, *, #60026, .F. ) ;
#54296=DIRECTION ( 'NONE',  ( -5.981805089575196197E-17, -1.000000000000000000, 0.000000000000000000 ) ) ;
#54305=ORIENTED_EDGE ( 'NONE', *, *, #33563, .F. ) ;
#54306=AXIS2_PLACEMENT_3D ( 'NONE', #44208, #23680, #66128 ) ;
#54318=EDGE_CURVE ( 'NONE', #55467, #1208, #58404, .T. ) ;
#54331=CARTESIAN_POINT ( 'NONE',  ( 8.250000000000005329, 0.000000000000000000, -13.50000000000000178 ) ) ;
#54332=EDGE_CURVE ( 'NONE', #18330, #10391, #48480, .T. ) ;
#54342=ORIENTED_EDGE ( 'NONE', *, *, #744, .T. ) ;
#54349=VECTOR ( 'NONE', #3329, 1000.000000000000000 ) ;
#54351=DIRECTION ( 'NONE',  ( 0.000000000000000000, 1.000000000000000000, 0.000000000000000000 ) ) ;
#54354=AXIS2_PLACEMENT_3D ( 'NONE', #14540, #36824, #51682 ) ;
#54356=ORIENTED_EDGE ( 'NONE', *, *, #31816, .T. ) ;
#54357=ORIENTED_EDGE ( 'NONE', *, *, #49480, .F. ) ;
#54358=VECTOR ( 'NONE', #54070, 1000.000000000000000 ) ;
#54363=VECTOR ( 'NONE', #11446, 1000.000000000000000 ) ;
#54376=CIRCLE ( 'NONE', #63409, 1.000000000000000000 ) ;
#54385=DIRECTION ( 'NONE',  ( 1.000000000000000000, -0.000000000000000000, 0.000000000000000000 ) ) ;
#54388=ADVANCED_FACE ( 'NONE', ( #50553 ), #27947, .F. ) ;
#54391=EDGE_CURVE ( 'NONE', #1029, #41033, #54488, .T. ) ;
#54395=LINE ( 'NONE', #44112, #59960 ) ;
#54403=CARTESIAN_POINT ( 'NONE',  ( 4.456444791733522252E-16, 7.450000000000002842, -11.00000000000000000 ) ) ;
#54404=EDGE_LOOP ( 'NONE', ( #42878, #11893, #1864, #37728, #7170, #15271, #60317, #40291 ) ) ;
#54405=LINE ( 'NONE', #27185, #18901 ) ;
#54407=FACE_OUTER_BOUND ( 'NONE', #9840, .T. ) ;
#54411=ORIENTED_EDGE ( 'NONE', *, *, #62344, .T. ) ;
#54414=VERTEX_POINT ( 'NONE', #16657 ) ;
#54423=PLANE ( 'NONE',  #57839 ) ;
#54429=AXIS2_PLACEMENT_3D ( 'NONE', #42482, #26930, #32585 ) ;
#54436=VERTEX_POINT ( 'NONE', #27598 ) ;
#54437=ORIENTED_EDGE ( 'NONE', *, *, #60023, .F. ) ;
#54444=DIRECTION ( 'NONE',  ( -1.000000000000000000, 0.000000000000000000, 0.000000000000000000 ) ) ;
#54452=ADVANCED_FACE ( 'NONE', ( #11667 ), #19067, .F. ) ;
#54453=DIRECTION ( 'NONE',  ( -1.000000000000000000, 0.000000000000000000, 0.000000000000000000 ) ) ;
#54454=AXIS2_PLACEMENT_3D ( 'NONE', #643, #22215, #48036 ) ;
#54456=DIRECTION ( 'NONE',  ( 0.000000000000000000, 0.000000000000000000, 1.000000000000000000 ) ) ;
#54465=ORIENTED_EDGE ( 'NONE', *, *, #6353, .F. ) ;
#54488=LINE ( 'NONE', #16993, #56523 ) ;
#54494=ORIENTED_EDGE ( 'NONE', *, *, #5143, .F. ) ;
#54495=CARTESIAN_POINT ( 'NONE',  ( 8.250000000000005329, -8.249999999999998224, -26.00000000000001066 ) ) ;
#54497=CARTESIAN_POINT ( 'NONE',  ( -8.250000000000001776, -7.249999999999998224, -8.500000000000000000 ) ) ;
#54499=VERTEX_POINT ( 'NONE', #67860 ) ;
#54505=CARTESIAN_POINT ( 'NONE',  ( 7.250000000000004441, 7.450000000000001954, -24.50000000000000000 ) ) ;
#54506=LINE ( 'NONE', #38583, #40450 ) ;
#54507=VECTOR ( 'NONE', #13673, 1000.000000000000000 ) ;
#54508=EDGE_CURVE ( 'NONE', #60224, #24588, #8444, .T. ) ;
#54527=CARTESIAN_POINT ( 'NONE',  ( -7.250000000000000888, -8.249999999999998224, -14.00000000000000000 ) ) ;
#54532=VECTOR ( 'NONE', #3263, 1000.000000000000000 ) ;
#54533=ORIENTED_EDGE ( 'NONE', *, *, #60009, .T. ) ;
#54538=CARTESIAN_POINT ( 'NONE',  ( 7.250000000000005329, 7.250000000000000888, -10.50000000000000000 ) ) ;
#54542=CARTESIAN_POINT ( 'NONE',  ( 7.450000000000004619, -1.336933437520057563E-15, -13.50000000000000178 ) ) ;
#54543=AXIS2_PLACEMENT_3D ( 'NONE', #31166, #9947, #53424 ) ;
#54546=ADVANCED_FACE ( 'NONE', ( #46634 ), #30380, .F. ) ;
#54555=CARTESIAN_POINT ( 'NONE',  ( -7.250000000000000888, 7.250000000000001776, -14.00000000000000000 ) ) ;
#54557=ADVANCED_FACE ( 'NONE', ( #20124 ), #16209, .T. ) ;
#54558=VECTOR ( 'NONE', #1140, 1000.000000000000000 ) ;
#54560=VERTEX_POINT ( 'NONE', #57945 ) ;
#54573=CARTESIAN_POINT ( 'NONE',  ( 8.250000000000005329, 7.250000000000000888, -16.50000000000000000 ) ) ;
#54576=VECTOR ( 'NONE', #65143, 1000.000000000000000 ) ;
#54587=CIRCLE ( 'NONE', #24075, 0.9999999999999991118 ) ;
#54602=ADVANCED_FACE ( 'NONE', ( #25426 ), #32486, .T. ) ;
#54604=FACE_OUTER_BOUND ( 'NONE', #50338, .T. ) ;
#54605=AXIS2_PLACEMENT_3D ( 'NONE', #2381, #62457, #34546 ) ;
#54606=ORIENTED_EDGE ( 'NONE', *, *, #23266, .T. ) ;
#54609=DIRECTION ( 'NONE',  ( 0.000000000000000000, 1.000000000000000000, 0.000000000000000000 ) ) ;
#54617=EDGE_LOOP ( 'NONE', ( #56096, #67504, #27785, #39212 ) ) ;
#54620=DIRECTION ( 'NONE',  ( 0.000000000000000000, -0.000000000000000000, 1.000000000000000000 ) ) ;
#54621=DIRECTION ( 'NONE',  ( 0.000000000000000000, 0.000000000000000000, 1.000000000000000000 ) ) ;
#54629=DIRECTION ( 'NONE',  ( 0.000000000000000000, 0.000000000000000000, 1.000000000000000000 ) ) ;
#54641=ORIENTED_EDGE ( 'NONE', *, *, #22810, .T. ) ;
#54647=DIRECTION ( 'NONE',  ( -1.000000000000000000, 0.000000000000000000, 0.000000000000000000 ) ) ;
#54652=FACE_OUTER_BOUND ( 'NONE', #37050, .T. ) ;
#54667=ADVANCED_FACE ( 'NONE', ( #68914 ), #52666, .T. ) ;
#54668=EDGE_CURVE ( 'NONE', #21320, #62492, #26135, .T. ) ;
#54678=EDGE_CURVE ( 'NONE', #29937, #7966, #42380, .T. ) ;
#54686=DIRECTION ( 'NONE',  ( -1.000000000000000000, 0.000000000000000000, -0.000000000000000000 ) ) ;
#54690=ORIENTED_EDGE ( 'NONE', *, *, #16461, .F. ) ;
#54691=DIRECTION ( 'NONE',  ( 0.000000000000000000, 0.000000000000000000, 1.000000000000000000 ) ) ;
#54723=ORIENTED_EDGE ( 'NONE', *, *, #58050, .F. ) ;
#54727=ORIENTED_EDGE ( 'NONE', *, *, #46551, .F. ) ;
#54734=AXIS2_PLACEMENT_3D ( 'NONE', #10266, #53752, #54444 ) ;
#54745=DIRECTION ( 'NONE',  ( 0.000000000000000000, 1.000000000000000000, 0.000000000000000000 ) ) ;
#54754=CARTESIAN_POINT ( 'NONE',  ( -7.250000000000000888, 7.450000000000003730, -24.00000000000000000 ) ) ;
#54757=CYLINDRICAL_SURFACE ( 'NONE', #2568, 0.1999999999999996503 ) ;
#54778=CARTESIAN_POINT ( 'NONE',  ( 8.689999999999999503, 8.750000000000000000, -7.000000000000000000 ) ) ;
#54795=FACE_OUTER_BOUND ( 'NONE', #25944, .T. ) ;
#54796=EDGE_CURVE ( 'NONE', #39018, #44299, #54395, .T. ) ;
#54805=AXIS2_PLACEMENT_3D ( 'NONE', #57267, #25809, #8829 ) ;
#54810=AXIS2_PLACEMENT_3D ( 'NONE', #43675, #64208, #198 ) ;
#54827=VECTOR ( 'NONE', #68546, 1000.000000000000000 ) ;
#54828=DIRECTION ( 'NONE',  ( -1.000000000000000000, 0.000000000000000000, -0.000000000000000000 ) ) ;
#54830=PLANE ( 'NONE',  #63177 ) ;
#54831=LINE ( 'NONE', #44199, #63869 ) ;
#54833=CARTESIAN_POINT ( 'NONE',  ( 7.250000000000005329, 8.250000000000001776, -9.500000000000001776 ) ) ;
#54838=DIRECTION ( 'NONE',  ( 1.000000000000000000, 0.000000000000000000, 0.000000000000000000 ) ) ;
#54839=DIRECTION ( 'NONE',  ( -0.000000000000000000, -0.000000000000000000, 1.000000000000000000 ) ) ;
#54854=CARTESIAN_POINT ( 'NONE',  ( -7.450000000000001954, 0.000000000000000000, -20.00000000000000000 ) ) ;
#54855=FACE_OUTER_BOUND ( 'NONE', #53171, .T. ) ;
#54859=AXIS2_PLACEMENT_3D ( 'NONE', #69884, #21448, #27102 ) ;
#54861=PLANE ( 'NONE',  #65659 ) ;
#54862=ORIENTED_EDGE ( 'NONE', *, *, #49275, .T. ) ;
#54871=DIRECTION ( 'NONE',  ( -1.000000000000000000, 0.000000000000000000, 0.000000000000000000 ) ) ;
#54872=FACE_BOUND ( 'NONE', #15253, .T. ) ;
#54888=AXIS2_PLACEMENT_3D ( 'NONE', #49339, #22107, #23130 ) ;
#54893=CARTESIAN_POINT ( 'NONE',  ( -7.250000000000000888, -8.249999999999998224, -13.50000000000000178 ) ) ;
#54895=ORIENTED_EDGE ( 'NONE', *, *, #9650, .F. ) ;
#54909=VECTOR ( 'NONE', #4047, 1000.000000000000000 ) ;
#54910=LINE ( 'NONE', #28027, #12530 ) ;
#54916=FACE_OUTER_BOUND ( 'NONE', #64081, .T. ) ;
#54919=CIRCLE ( 'NONE', #63949, 0.2000000000000005107 ) ;
#54922=CARTESIAN_POINT ( 'NONE',  ( 0.000000000000000000, -7.449999999999998401, -22.00000000000000000 ) ) ;
#54925=VECTOR ( 'NONE', #47443, 1000.000000000000000 ) ;
#54938=CARTESIAN_POINT ( 'NONE',  ( 8.250000000000005329, -7.249999999999998224, -26.00000000000001066 ) ) ;
#54948=DIRECTION ( 'NONE',  ( 0.000000000000000000, 1.000000000000000000, 0.000000000000000000 ) ) ;
#54956=EDGE_LOOP ( 'NONE', ( #58813, #13861, #19565, #68009 ) ) ;
#54957=DIRECTION ( 'NONE',  ( -0.000000000000000000, -0.000000000000000000, 1.000000000000000000 ) ) ;
#54962=ORIENTED_EDGE ( 'NONE', *, *, #38797, .F. ) ;
#54963=VECTOR ( 'NONE', #12706, 1000.000000000000000 ) ;
#54969=EDGE_CURVE ( 'NONE', #31578, #31212, #12548, .T. ) ;
#54973=DIRECTION ( 'NONE',  ( -1.000000000000000000, 0.000000000000000000, 0.000000000000000000 ) ) ;
#54974=DIRECTION ( 'NONE',  ( 1.000000000000000000, 0.000000000000000000, -0.000000000000000000 ) ) ;
#54975=CARTESIAN_POINT ( 'NONE',  ( -7.250000000000000000, -7.449999999999998401, -9.500000000000001776 ) ) ;
#54987=ORIENTED_EDGE ( 'NONE', *, *, #33563, .T. ) ;
#54991=ADVANCED_FACE ( 'NONE', ( #9704 ), #42569, .T. ) ;
#54992=CARTESIAN_POINT ( 'NONE',  ( -7.250000000000001776, -7.249999999999998224, -20.00000000000000000 ) ) ;
#54993=EDGE_LOOP ( 'NONE', ( #44438, #12981, #57709, #45088 ) ) ;
#55012=DIRECTION ( 'NONE',  ( -0.000000000000000000, -0.000000000000000000, -1.000000000000000000 ) ) ;
#55021=EDGE_CURVE ( 'NONE', #39380, #47318, #24987, .T. ) ;
#55028=DIRECTION ( 'NONE',  ( -1.000000000000000000, 0.000000000000000000, -0.000000000000000000 ) ) ;
#55029=VECTOR ( 'NONE', #24421, 1000.000000000000000 ) ;
#55041=ORIENTED_EDGE ( 'NONE', *, *, #285, .T. ) ;
#55051=ORIENTED_EDGE ( 'NONE', *, *, #30443, .T. ) ;
#55055=LINE ( 'NONE', #49399, #67711 ) ;
#55071=VECTOR ( 'NONE', #53875, 1000.000000000000000 ) ;
#55073=CARTESIAN_POINT ( 'NONE',  ( -7.250000000000000888, 8.250000000000001776, -26.00000000000001066 ) ) ;
#55074=FACE_OUTER_BOUND ( 'NONE', #51340, .T. ) ;
#55082=DIRECTION ( 'NONE',  ( 0.000000000000000000, 0.000000000000000000, -1.000000000000000000 ) ) ;
#55083=AXIS2_PLACEMENT_3D ( 'NONE', #65684, #64643, #24645 ) ;
#55084=CARTESIAN_POINT ( 'NONE',  ( 7.450000000000003730, -7.249999999999997335, -25.50000000000000355 ) ) ;
#55093=CARTESIAN_POINT ( 'NONE',  ( 7.250000000000004441, 7.450000000000001954, -9.500000000000001776 ) ) ;
#55096=CARTESIAN_POINT ( 'NONE',  ( 0.000000000000000000, -7.449999999999998401, -19.50000000000000000 ) ) ;
#55100=CARTESIAN_POINT ( 'NONE',  ( -8.750000000000001776, 0.000000000000000000, -30.00000000000001066 ) ) ;
#55101=CARTESIAN_POINT ( 'NONE',  ( -7.250000000000000888, 7.250000000000001776, -9.000000000000001776 ) ) ;
#55105=ORIENTED_EDGE ( 'NONE', *, *, #28916, .T. ) ;
#55133=CARTESIAN_POINT ( 'NONE',  ( -8.250000000000001776, 7.250000000000000888, -26.00000000000001066 ) ) ;
#55140=EDGE_LOOP ( 'NONE', ( #50265, #57289, #13024, #13831, #42363, #11311, #59385, #17897 ) ) ;
#55149=ORIENTED_EDGE ( 'NONE', *, *, #56407, .T. ) ;
#55151=CARTESIAN_POINT ( 'NONE',  ( -8.250000000000001776, 7.250000000000000888, -26.00000000000001066 ) ) ;
#55153=CARTESIAN_POINT ( 'NONE',  ( 7.250000000000005329, -7.449999999999998401, -19.00000000000000000 ) ) ;
#55160=ORIENTED_EDGE ( 'NONE', *, *, #8296, .F. ) ;
#55168=CARTESIAN_POINT ( 'NONE',  ( -7.450000000000001954, -7.249999999999998224, -7.500000000000000000 ) ) ;
#55171=DIRECTION ( 'NONE',  ( 0.000000000000000000, -1.000000000000000000, 0.000000000000000000 ) ) ;
#55174=DIRECTION ( 'NONE',  ( 0.000000000000000000, 0.000000000000000000, 1.000000000000000000 ) ) ;
#55180=ORIENTED_EDGE ( 'NONE', *, *, #61318, .F. ) ;
#55181=DIRECTION ( 'NONE',  ( 1.000000000000000000, 0.000000000000000000, 0.000000000000000000 ) ) ;
#55182=LINE ( 'NONE', #33271, #62210 ) ;
#55183=ORIENTED_EDGE ( 'NONE', *, *, #12121, .F. ) ;
#55185=CYLINDRICAL_SURFACE ( 'NONE', #15740, 0.2000000000000005107 ) ;
#55196=LINE ( 'NONE', #27980, #58460 ) ;
#55200=DIRECTION ( 'NONE',  ( 1.000000000000000000, -5.981805089575194965E-17, 0.000000000000000000 ) ) ;
#55203=VERTEX_POINT ( 'NONE', #49942 ) ;
#55206=EDGE_CURVE ( 'NONE', #47162, #29352, #66556, .T. ) ;
#55209=CARTESIAN_POINT ( 'NONE',  ( 8.250000000000005329, -8.249999999999998224, -26.00000000000001066 ) ) ;
#55214=FACE_OUTER_BOUND ( 'NONE', #46791, .T. ) ;
#55217=CYLINDRICAL_SURFACE ( 'NONE', #28483, 0.1999999999999987899 ) ;
#55222=CARTESIAN_POINT ( 'NONE',  ( 7.250000000000005329, -7.449999999999998401, -7.000000000000000000 ) ) ;
#55225=LINE ( 'NONE', #6767, #62460 ) ;
#55236=DIRECTION ( 'NONE',  ( 0.000000000000000000, 0.000000000000000000, 1.000000000000000000 ) ) ;
#55254=VECTOR ( 'NONE', #46224, 1000.000000000000000 ) ;
#55255=CIRCLE ( 'NONE', #31603, 0.1999999999999996503 ) ;
#55257=DIRECTION ( 'NONE',  ( 0.000000000000000000, 0.000000000000000000, 1.000000000000000000 ) ) ;
#55267=EDGE_CURVE ( 'NONE', #38943, #59582, #45305, .T. ) ;
#55268=EDGE_CURVE ( 'NONE', #58882, #1276, #13509, .T. ) ;
#55270=AXIS2_PLACEMENT_3D ( 'NONE', #68050, #14315, #13948 ) ;
#55273=EDGE_CURVE ( 'NONE', #47489, #18717, #54376, .T. ) ;
#55276=EDGE_CURVE ( 'NONE', #15671, #9143, #41075, .T. ) ;
#55291=LINE ( 'NONE', #34044, #4706 ) ;
#55292=ORIENTED_EDGE ( 'NONE', *, *, #34772, .F. ) ;
#55293=ADVANCED_FACE ( 'NONE', ( #41778 ), #36478, .F. ) ;
#55296=CARTESIAN_POINT ( 'NONE',  ( 7.250000000000005329, 7.250000000000000888, -18.50000000000000000 ) ) ;
#55316=LINE ( 'NONE', #530, #59921 ) ;
#55322=VERTEX_POINT ( 'NONE', #24480 ) ;
#55323=DIRECTION ( 'NONE',  ( 1.000000000000000000, -5.981805089575194965E-17, 0.000000000000000000 ) ) ;
#55327=CIRCLE ( 'NONE', #7907, 0.9999999999999991118 ) ;
#55329=CARTESIAN_POINT ( 'NONE',  ( -9.690000000000001279, 10.50000000000000178, 0.000000000000000000 ) ) ;
#55334=VECTOR ( 'NONE', #47514, 1000.000000000000000 ) ;
#55337=LINE ( 'NONE', #1571, #43556 ) ;
#55346=DIRECTION ( 'NONE',  ( -1.000000000000000000, 0.000000000000000000, 0.000000000000000000 ) ) ;
#55350=ORIENTED_EDGE ( 'NONE', *, *, #25166, .T. ) ;
#55357=ORIENTED_EDGE ( 'NONE', *, *, #49293, .F. ) ;
#55359=LINE ( 'NONE', #12887, #453 ) ;
#55360=DIRECTION ( 'NONE',  ( -1.000000000000000000, 0.000000000000000000, -0.000000000000000000 ) ) ;
#55365=DIRECTION ( 'NONE',  ( 1.000000000000000000, -5.981805089575194965E-17, 0.000000000000000000 ) ) ;
#55366=DIRECTION ( 'NONE',  ( -0.000000000000000000, -0.000000000000000000, -1.000000000000000000 ) ) ;
#55368=VECTOR ( 'NONE', #15889, 1000.000000000000000 ) ;
#55370=LINE ( 'NONE', #44733, #21548 ) ;
#55374=VERTEX_POINT ( 'NONE', #36123 ) ;
#55390=AXIS2_PLACEMENT_3D ( 'NONE', #43576, #39892, #37938 ) ;
#55396=ORIENTED_EDGE ( 'NONE', *, *, #45673, .T. ) ;
#55407=DIRECTION ( 'NONE',  ( 0.000000000000000000, 0.000000000000000000, -1.000000000000000000 ) ) ;
#55411=ORIENTED_EDGE ( 'NONE', *, *, #41242, .F. ) ;
#55414=AXIS2_PLACEMENT_3D ( 'NONE', #63815, #57800, #52150 ) ;
#55416=CARTESIAN_POINT ( 'NONE',  ( 7.250000000000005329, 7.250000000000000888, -25.50000000000000355 ) ) ;
#55420=EDGE_CURVE ( 'NONE', #3957, #20305, #48145, .T. ) ;
#55433=DIRECTION ( 'NONE',  ( -1.000000000000000000, 0.000000000000000000, 0.000000000000000000 ) ) ;
#55439=CARTESIAN_POINT ( 'NONE',  ( 8.689999999999999503, -9.750000000000001776, -7.000000000000000000 ) ) ;
#55449=CARTESIAN_POINT ( 'NONE',  ( 8.750000000000005329, -7.249999999999997335, -30.00000000000001066 ) ) ;
#55457=EDGE_LOOP ( 'NONE', ( #43905, #468, #49616, #48047 ) ) ;
#55467=VERTEX_POINT ( 'NONE', #15270 ) ;
#55473=DIRECTION ( 'NONE',  ( -0.000000000000000000, -0.000000000000000000, -1.000000000000000000 ) ) ;
#55477=PLANE ( 'NONE',  #36869 ) ;
#55481=ORIENTED_EDGE ( 'NONE', *, *, #43594, .T. ) ;
#55483=ORIENTED_EDGE ( 'NONE', *, *, #66136, .F. ) ;
#55484=EDGE_LOOP ( 'NONE', ( #69336, #48973, #978, #42617 ) ) ;
#55487=EDGE_CURVE ( 'NONE', #28850, #3957, #27326, .T. ) ;
#55489=VECTOR ( 'NONE', #26029, 1000.000000000000000 ) ;
#55491=ORIENTED_EDGE ( 'NONE', *, *, #30598, .T. ) ;
#55498=CARTESIAN_POINT ( 'NONE',  ( -7.450000000000001954, -7.249999999999998224, -14.00000000000000000 ) ) ;
#55510=CYLINDRICAL_SURFACE ( 'NONE', #67968, 1.000000000000001776 ) ;
#55512=VECTOR ( 'NONE', #32601, 1000.000000000000000 ) ;
#55532=DIRECTION ( 'NONE',  ( 0.000000000000000000, 0.000000000000000000, 1.000000000000000000 ) ) ;
#55534=ORIENTED_EDGE ( 'NONE', *, *, #44717, .T. ) ;
#55551=DIRECTION ( 'NONE',  ( -1.000000000000000000, 0.000000000000000000, 0.000000000000000000 ) ) ;
#55556=DIRECTION ( 'NONE',  ( -1.000000000000000000, 0.000000000000000000, 0.000000000000000000 ) ) ;
#55557=ORIENTED_EDGE ( 'NONE', *, *, #41007, .F. ) ;
#55560=ORIENTED_EDGE ( 'NONE', *, *, #25933, .F. ) ;
#55562=AXIS2_PLACEMENT_3D ( 'NONE', #40845, #13276, #29535 ) ;
#55574=LINE ( 'NONE', #18076, #10842 ) ;
#55575=ORIENTED_EDGE ( 'NONE', *, *, #18507, .F. ) ;
#55577=CARTESIAN_POINT ( 'NONE',  ( 8.250000000000005329, -8.249999999999998224, -26.00000000000001066 ) ) ;
#55581=EDGE_CURVE ( 'NONE', #41772, #61464, #41998, .T. ) ;
#55582=DIRECTION ( 'NONE',  ( -0.000000000000000000, -0.000000000000000000, 1.000000000000000000 ) ) ;
#55583=EDGE_CURVE ( 'NONE', #9544, #31253, #33605, .T. ) ;
#55597=VERTEX_POINT ( 'NONE', #22654 ) ;
#55607=ORIENTED_EDGE ( 'NONE', *, *, #30709, .T. ) ;
#55609=DIRECTION ( 'NONE',  ( 0.000000000000000000, 0.000000000000000000, 1.000000000000000000 ) ) ;
#55618=LINE ( 'NONE', #17095, #21151 ) ;
#55625=DIRECTION ( 'NONE',  ( -1.000000000000000000, 0.000000000000000000, 0.000000000000000000 ) ) ;
#55627=DIRECTION ( 'NONE',  ( 0.000000000000000000, 0.000000000000000000, 1.000000000000000000 ) ) ;
#55630=VECTOR ( 'NONE', #61555, 1000.000000000000000 ) ;
#55631=CYLINDRICAL_SURFACE ( 'NONE', #64405, 0.1999999999999987899 ) ;
#55632=CARTESIAN_POINT ( 'NONE',  ( 7.250000000000005329, 8.250000000000001776, -22.50000000000000000 ) ) ;
#55636=EDGE_CURVE ( 'NONE', #67039, #65777, #44204, .T. ) ;
#55651=DIRECTION ( 'NONE',  ( -0.000000000000000000, -0.000000000000000000, 1.000000000000000000 ) ) ;
#55652=ORIENTED_EDGE ( 'NONE', *, *, #29787, .F. ) ;
#55654=EDGE_CURVE ( 'NONE', #10277, #16237, #34276, .T. ) ;
#55661=DIRECTION ( 'NONE',  ( -0.000000000000000000, -0.000000000000000000, -1.000000000000000000 ) ) ;
#55665=DIRECTION ( 'NONE',  ( 0.000000000000000000, -0.000000000000000000, 1.000000000000000000 ) ) ;
#55667=ORIENTED_EDGE ( 'NONE', *, *, #50383, .T. ) ;
#55690=CARTESIAN_POINT ( 'NONE',  ( 7.250000000000005329, -7.249999999999998224, -19.50000000000000000 ) ) ;
#55691=CYLINDRICAL_SURFACE ( 'NONE', #25542, 1.000000000000000000 ) ;
#55695=DIRECTION ( 'NONE',  ( 0.000000000000000000, 1.000000000000000000, 0.000000000000000000 ) ) ;
#55701=DIRECTION ( 'NONE',  ( -0.000000000000000000, 0.000000000000000000, 1.000000000000000000 ) ) ;
#55704=DIRECTION ( 'NONE',  ( 1.000000000000000000, 0.000000000000000000, 0.000000000000000000 ) ) ;
#55705=CARTESIAN_POINT ( 'NONE',  ( 7.450000000000003730, -7.249999999999997335, -7.500000000000000000 ) ) ;
#55709=CIRCLE ( 'NONE', #51210, 1.000000000000000000 ) ;
#55720=ORIENTED_EDGE ( 'NONE', *, *, #61731, .T. ) ;
#55726=VERTEX_POINT ( 'NONE', #34980 ) ;
#55727=CARTESIAN_POINT ( 'NONE',  ( 7.250000000000005329, -7.449999999999998401, -13.00000000000000178 ) ) ;
#55734=DIRECTION ( 'NONE',  ( 0.000000000000000000, 0.000000000000000000, -1.000000000000000000 ) ) ;
#55760=ORIENTED_EDGE ( 'NONE', *, *, #10008, .F. ) ;
#55769=DIRECTION ( 'NONE',  ( -0.000000000000000000, -0.000000000000000000, 1.000000000000000000 ) ) ;
#55770=ORIENTED_EDGE ( 'NONE', *, *, #54391, .F. ) ;
#55781=DIRECTION ( 'NONE',  ( -0.000000000000000000, -0.000000000000000000, -1.000000000000000000 ) ) ;
#55783=LINE ( 'NONE', #40209, #63922 ) ;
#55786=LINE ( 'NONE', #33530, #44348 ) ;
#55787=CARTESIAN_POINT ( 'NONE',  ( -8.250000000000001776, -8.249999999999998224, -26.00000000000001066 ) ) ;
#55788=VERTEX_POINT ( 'NONE', #32496 ) ;
#55795=EDGE_CURVE ( 'NONE', #26023, #43043, #58671, .T. ) ;
#55802=ORIENTED_EDGE ( 'NONE', *, *, #11639, .T. ) ;
#55815=DIRECTION ( 'NONE',  ( 0.000000000000000000, 0.000000000000000000, 1.000000000000000000 ) ) ;
#55824=VECTOR ( 'NONE', #67906, 1000.000000000000000 ) ;
#55829=VERTEX_POINT ( 'NONE', #310 ) ;
#55834=DIRECTION ( 'NONE',  ( 0.000000000000000000, -0.000000000000000000, 1.000000000000000000 ) ) ;
#55843=ADVANCED_FACE ( 'NONE', ( #4237 ), #58329, .F. ) ;
#55848=DIRECTION ( 'NONE',  ( 0.000000000000000000, 1.000000000000000000, 0.000000000000000000 ) ) ;
#55854=CARTESIAN_POINT ( 'NONE',  ( -7.250000000000001776, -7.249999999999998224, -10.50000000000000000 ) ) ;
#55860=AXIS2_PLACEMENT_3D ( 'NONE', #14880, #47397, #36437 ) ;
#55862=ADVANCED_FACE ( 'NONE', ( #53026 ), #9889, .T. ) ;
#55865=VERTEX_POINT ( 'NONE', #42047 ) ;
#55873=EDGE_CURVE ( 'NONE', #69741, #9508, #4581, .T. ) ;
#55874=DIRECTION ( 'NONE',  ( -1.000000000000000000, 1.794541526872559352E-16, 0.000000000000000000 ) ) ;
#55879=VERTEX_POINT ( 'NONE', #37451 ) ;
#55884=CARTESIAN_POINT ( 'NONE',  ( -7.450000000000001954, 7.250000000000000000, -23.50000000000000000 ) ) ;
#55887=EDGE_CURVE ( 'NONE', #40613, #14714, #21527, .T. ) ;
#55891=VECTOR ( 'NONE', #9782, 1000.000000000000000 ) ;
#55897=CARTESIAN_POINT ( 'NONE',  ( 7.450000000000003730, -7.249999999999997335, -17.00000000000000000 ) ) ;
#55898=DIRECTION ( 'NONE',  ( 1.000000000000000000, 0.000000000000000000, 0.000000000000000000 ) ) ;
#55900=ORIENTED_EDGE ( 'NONE', *, *, #2864, .T. ) ;
#55903=VECTOR ( 'NONE', #68687, 1000.000000000000000 ) ;
#55921=FACE_OUTER_BOUND ( 'NONE', #23439, .T. ) ;
#55923=PLANE ( 'NONE',  #10840 ) ;
#55925=VECTOR ( 'NONE', #46126, 1000.000000000000000 ) ;
#55934=CARTESIAN_POINT ( 'NONE',  ( 0.000000000000000000, -8.249999999999998224, -24.50000000000000000 ) ) ;
#55939=FACE_OUTER_BOUND ( 'NONE', #59646, .T. ) ;
#55942=CARTESIAN_POINT ( 'NONE',  ( -7.250000000000000888, -8.249999999999998224, -11.00000000000000000 ) ) ;
#55951=ORIENTED_EDGE ( 'NONE', *, *, #31426, .F. ) ;
#55959=ORIENTED_EDGE ( 'NONE', *, *, #22789, .T. ) ;
#55964=DIRECTION ( 'NONE',  ( 1.000000000000000000, -5.981805089575194965E-17, 0.000000000000000000 ) ) ;
#55967=ORIENTED_EDGE ( 'NONE', *, *, #21821, .T. ) ;
#55969=CIRCLE ( 'NONE', #22117, 0.7499999999999997780 ) ;
#55972=ORIENTED_EDGE ( 'NONE', *, *, #49823, .F. ) ;
#55974=CARTESIAN_POINT ( 'NONE',  ( 8.250000000000005329, 0.000000000000000000, -18.00000000000000000 ) ) ;
#55975=ORIENTED_EDGE ( 'NONE', *, *, #45013, .F. ) ;
#55993=EDGE_CURVE ( 'NONE', #18999, #10507, #38154, .T. ) ;
#55995=EDGE_CURVE ( 'NONE', #63788, #28850, #22904, .T. ) ;
#56006=ORIENTED_EDGE ( 'NONE', *, *, #37315, .F. ) ;
#56008=CARTESIAN_POINT ( 'NONE',  ( 7.250000000000005329, 7.250000000000000888, -17.50000000000000000 ) ) ;
#56016=DIRECTION ( 'NONE',  ( 1.000000000000000000, 0.000000000000000000, 0.000000000000000000 ) ) ;
#56017=DIRECTION ( 'NONE',  ( 0.000000000000000000, 0.000000000000000000, -1.000000000000000000 ) ) ;
#56018=ORIENTED_EDGE ( 'NONE', *, *, #20163, .F. ) ;
#56040=DIRECTION ( 'NONE',  ( 1.000000000000000000, -0.000000000000000000, -0.000000000000000000 ) ) ;
#56045=PLANE ( 'NONE',  #45458 ) ;
#56049=DIRECTION ( 'NONE',  ( 0.000000000000000000, -1.000000000000000000, -0.000000000000000000 ) ) ;
#56057=VERTEX_POINT ( 'NONE', #55439 ) ;
#56061=AXIS2_PLACEMENT_3D ( 'NONE', #9858, #69241, #37766 ) ;
#56068=CARTESIAN_POINT ( 'NONE',  ( 8.250000000000005329, -7.249999999999998224, -25.00000000000000000 ) ) ;
#56075=FACE_OUTER_BOUND ( 'NONE', #47317, .T. ) ;
#56077=CARTESIAN_POINT ( 'NONE',  ( -7.250000000000000000, -7.449999999999998401, -7.500000000000000000 ) ) ;
#56081=VECTOR ( 'NONE', #30108, 1000.000000000000000 ) ;
#56087=ORIENTED_EDGE ( 'NONE', *, *, #30931, .F. ) ;
#56096=ORIENTED_EDGE ( 'NONE', *, *, #12876, .T. ) ;
#56099=DIRECTION ( 'NONE',  ( -0.000000000000000000, -0.000000000000000000, -1.000000000000000000 ) ) ;
#56104=EDGE_CURVE ( 'NONE', #21736, #5314, #18992, .T. ) ;
#56105=AXIS2_PLACEMENT_3D ( 'NONE', #30655, #23350, #50907 ) ;
#56106=CIRCLE ( 'NONE', #25695, 1.000000000000000000 ) ;
#56108=CARTESIAN_POINT ( 'NONE',  ( -7.250000000000000888, 7.250000000000001776, -9.500000000000001776 ) ) ;
#56119=AXIS2_PLACEMENT_3D ( 'NONE', #38791, #34165, #28523 ) ;
#56124=CARTESIAN_POINT ( 'NONE',  ( -7.250000000000001776, -7.249999999999998224, -11.50000000000000000 ) ) ;
#56152=ORIENTED_EDGE ( 'NONE', *, *, #9011, .F. ) ;
#56158=ORIENTED_EDGE ( 'NONE', *, *, #10347, .T. ) ;
#56167=CARTESIAN_POINT ( 'NONE',  ( 7.450000000000004619, -1.336933437520057563E-15, -8.000000000000000000 ) ) ;
#56169=PRODUCT_DEFINITION_FORMATION_WITH_SPECIFIED_SOURCE ( 'ANY', '', #49892, .NOT_KNOWN. ) ;
#56173=CARTESIAN_POINT ( 'NONE',  ( 0.000000000000000000, 0.000000000000000000, -7.000000000000000000 ) ) ;
#56177=ORIENTED_EDGE ( 'NONE', *, *, #57209, .T. ) ;
#56182=DIRECTION ( 'NONE',  ( 0.000000000000000000, 0.000000000000000000, 1.000000000000000000 ) ) ;
#56186=DIRECTION ( 'NONE',  ( -1.000000000000000000, 0.000000000000000000, 0.000000000000000000 ) ) ;
#56188=DIRECTION ( 'NONE',  ( 0.000000000000000000, 0.000000000000000000, -1.000000000000000000 ) ) ;
#56201=CARTESIAN_POINT ( 'NONE',  ( -7.250000000000001776, -7.249999999999998224, -26.00000000000001066 ) ) ;
#56205=AXIS2_PLACEMENT_3D ( 'NONE', #15158, #26463, #30718 ) ;
#56219=VECTOR ( 'NONE', #10734, 1000.000000000000000 ) ;
#56229=VECTOR ( 'NONE', #62374, 1000.000000000000000 ) ;
#56231=ORIENTED_EDGE ( 'NONE', *, *, #34464, .F. ) ;
#56234=EDGE_LOOP ( 'NONE', ( #3405, #38631, #64778, #51279 ) ) ;
#56236=CARTESIAN_POINT ( 'NONE',  ( 4.456444791733522252E-16, 7.450000000000002842, -23.50000000000000000 ) ) ;
#56240=ORIENTED_EDGE ( 'NONE', *, *, #8918, .F. ) ;
#56247=FACE_OUTER_BOUND ( 'NONE', #61624, .T. ) ;
#56250=CARTESIAN_POINT ( 'NONE',  ( 0.000000000000000000, 0.000000000000000000, -8.500000000000000000 ) ) ;
#56268=LINE ( 'NONE', #50962, #4817 ) ;
#56270=ORIENTED_EDGE ( 'NONE', *, *, #36325, .T. ) ;
#56272=EDGE_CURVE ( 'NONE', #5559, #33795, #63540, .T. ) ;
#56278=EDGE_CURVE ( 'NONE', #31600, #69380, #48874, .T. ) ;
#56279=DIRECTION ( 'NONE',  ( -0.000000000000000000, 0.000000000000000000, 1.000000000000000000 ) ) ;
#56282=EDGE_CURVE ( 'NONE', #10769, #39380, #59270, .T. ) ;
#56283=DIRECTION ( 'NONE',  ( 1.000000000000000000, -0.000000000000000000, 0.000000000000000000 ) ) ;
#56285=CARTESIAN_POINT ( 'NONE',  ( 7.450000000000004619, -1.336933437520057563E-15, -21.50000000000000000 ) ) ;
#56295=CARTESIAN_POINT ( 'NONE',  ( 8.250000000000005329, -7.249999999999998224, -10.50000000000000000 ) ) ;
#56307=CARTESIAN_POINT ( 'NONE',  ( 7.250000000000005329, 8.250000000000001776, -15.00000000000000000 ) ) ;
#56308=VERTEX_POINT ( 'NONE', #15095 ) ;
#56309=DIRECTION ( 'NONE',  ( -1.000000000000000000, 0.000000000000000000, 0.000000000000000000 ) ) ;
#56312=CIRCLE ( 'NONE', #25851, 0.2000000000000005107 ) ;
#56317=PLANE ( 'NONE',  #7195 ) ;
#56327=LINE ( 'NONE', #51022, #67022 ) ;
#56328=DIRECTION ( 'NONE',  ( -1.000000000000000000, 0.000000000000000000, 0.000000000000000000 ) ) ;
#56330=ADVANCED_FACE ( 'NONE', ( #69534, #63884 ), #53631, .T. ) ;
#56334=VERTEX_POINT ( 'NONE', #33090 ) ;
#56337=ORIENTED_EDGE ( 'NONE', *, *, #10610, .F. ) ;
#56350=EDGE_LOOP ( 'NONE', ( #43324, #55951, #55575, #40442 ) ) ;
#56355=ORIENTED_EDGE ( 'NONE', *, *, #37842, .T. ) ;
#56360=DIRECTION ( 'NONE',  ( -1.794541526872559352E-16, -1.000000000000000000, 0.000000000000000000 ) ) ;
#56367=AXIS2_PLACEMENT_3D ( 'NONE', #14373, #51502, #63863 ) ;
#56373=LINE ( 'NONE', #45760, #3838 ) ;
#56385=EDGE_CURVE ( 'NONE', #3293, #41058, #3689, .T. ) ;
#56387=AXIS2_PLACEMENT_3D ( 'NONE', #39972, #13117, #19470 ) ;
#56397=CARTESIAN_POINT ( 'NONE',  ( -8.250000000000001776, -7.249999999999998224, -24.50000000000000000 ) ) ;
#56399=ORIENTED_EDGE ( 'NONE', *, *, #38736, .F. ) ;
#56400=VECTOR ( 'NONE', #58943, 1000.000000000000000 ) ;
#56404=DIRECTION ( 'NONE',  ( 1.000000000000000000, -5.981805089575194965E-17, 0.000000000000000000 ) ) ;
#56406=VERTEX_POINT ( 'NONE', #64931 ) ;
#56407=EDGE_CURVE ( 'NONE', #11123, #15298, #11853, .T. ) ;
#56416=CARTESIAN_POINT ( 'NONE',  ( 0.000000000000000000, 8.250000000000001776, -18.00000000000000000 ) ) ;
#56417=DIRECTION ( 'NONE',  ( -1.794541526872559352E-16, -1.000000000000000000, 0.000000000000000000 ) ) ;
#56423=CARTESIAN_POINT ( 'NONE',  ( 0.000000000000000000, 0.000000000000000000, -17.50000000000000000 ) ) ;
#56428=EDGE_LOOP ( 'NONE', ( #38251, #1039, #50927, #7119, #69175, #65134, #60090, #7553 ) ) ;
#56429=EDGE_CURVE ( 'NONE', #36185, #48836, #50010, .T. ) ;
#56437=VERTEX_POINT ( 'NONE', #65615 ) ;
#56440=CARTESIAN_POINT ( 'NONE',  ( -7.450000000000001954, 7.250000000000000000, -19.50000000000000000 ) ) ;
#56449=ORIENTED_EDGE ( 'NONE', *, *, #7910, .F. ) ;
#56452=VECTOR ( 'NONE', #21865, 1000.000000000000000 ) ;
#56453=DIRECTION ( 'NONE',  ( -0.000000000000000000, -0.000000000000000000, 1.000000000000000000 ) ) ;
#56461=ORIENTED_EDGE ( 'NONE', *, *, #24193, .F. ) ;
#56474=CARTESIAN_POINT ( 'NONE',  ( 7.450000000000003730, -7.249999999999997335, -24.50000000000000000 ) ) ;
#56481=ORIENTED_EDGE ( 'NONE', *, *, #10877, .T. ) ;
#56484=CIRCLE ( 'NONE', #55390, 0.2000000000000005107 ) ;
#56504=ORIENTED_EDGE ( 'NONE', *, *, #9944, .T. ) ;
#56508=FACE_OUTER_BOUND ( 'NONE', #40136, .T. ) ;
#56523=VECTOR ( 'NONE', #49515, 1000.000000000000000 ) ;
#56525=CARTESIAN_POINT ( 'NONE',  ( -7.450000000000001954, 0.000000000000000000, -11.00000000000000000 ) ) ;
#56528=ADVANCED_FACE ( 'NONE', ( #68054 ), #56045, .F. ) ;
#56530=DIRECTION ( 'NONE',  ( 0.000000000000000000, 1.000000000000000000, 0.000000000000000000 ) ) ;
#56534=DIRECTION ( 'NONE',  ( 0.000000000000000000, 0.000000000000000000, 1.000000000000000000 ) ) ;
#56535=EDGE_CURVE ( 'NONE', #36733, #39553, #40475, .T. ) ;
#56537=CYLINDRICAL_SURFACE ( 'NONE', #62300, 0.1999999999999996503 ) ;
#56540=ORIENTED_EDGE ( 'NONE', *, *, #1758, .F. ) ;
#56541=EDGE_CURVE ( 'NONE', #46508, #21984, #14320, .T. ) ;
#56560=CIRCLE ( 'NONE', #54306, 0.1999999999999996503 ) ;
#56562=ORIENTED_EDGE ( 'NONE', *, *, #54064, .T. ) ;
#56587=LINE ( 'NONE', #51648, #11011 ) ;
#56589=VECTOR ( 'NONE', #65588, 1000.000000000000000 ) ;
#56594=CARTESIAN_POINT ( 'NONE',  ( 7.450000000000004619, -1.336933437520057563E-15, -18.50000000000000000 ) ) ;
#56595=DIRECTION ( 'NONE',  ( -1.000000000000000000, 0.000000000000000000, 0.000000000000000000 ) ) ;
#56596=ORIENTED_EDGE ( 'NONE', *, *, #55887, .T. ) ;
#56603=CARTESIAN_POINT ( 'NONE',  ( -7.250000000000000888, -8.249999999999998224, -26.00000000000001066 ) ) ;
#56604=AXIS2_PLACEMENT_3D ( 'NONE', #43247, #48559, #132 ) ;
#56611=DIRECTION ( 'NONE',  ( 1.000000000000000000, 0.000000000000000000, 0.000000000000000000 ) ) ;
#56614=VECTOR ( 'NONE', #45263, 1000.000000000000000 ) ;
#56618=ORIENTED_EDGE ( 'NONE', *, *, #56104, .T. ) ;
#56619=LINE ( 'NONE', #40354, #68049 ) ;
#56620=FACE_OUTER_BOUND ( 'NONE', #50569, .T. ) ;
#56623=EDGE_CURVE ( 'NONE', #36081, #5045, #30572, .T. ) ;
#56626=ORIENTED_EDGE ( 'NONE', *, *, #64151, .T. ) ;
#56627=ORIENTED_EDGE ( 'NONE', *, *, #12422, .T. ) ;
#56634=CARTESIAN_POINT ( 'NONE',  ( 4.456444791733522252E-16, 7.450000000000002842, -14.00000000000000000 ) ) ;
#56641=ORIENTED_EDGE ( 'NONE', *, *, #8467, .F. ) ;
#56645=DIRECTION ( 'NONE',  ( -1.794541526872559352E-16, -1.000000000000000000, 0.000000000000000000 ) ) ;
#56652=CIRCLE ( 'NONE', #45331, 0.1999999999999996503 ) ;
#56655=CARTESIAN_POINT ( 'NONE',  ( 8.750000000000000000, -7.348062532928000934, -5.000000000000000000 ) ) ;
#56660=DIRECTION ( 'NONE',  ( -1.000000000000000000, 0.000000000000000000, 0.000000000000000000 ) ) ;
#56662=ORIENTED_EDGE ( 'NONE', *, *, #334, .T. ) ;
#56663=CYLINDRICAL_SURFACE ( 'NONE', #16446, 1.000000000000000000 ) ;
#56665=CYLINDRICAL_SURFACE ( 'NONE', #27563, 1.000000000000000000 ) ;
#56671=VECTOR ( 'NONE', #57986, 1000.000000000000000 ) ;
#56676=CARTESIAN_POINT ( 'NONE',  ( -7.250000000000000888, 7.250000000000001776, -7.500000000000000000 ) ) ;
#56677=PLANE ( 'NONE',  #34186 ) ;
#56694=ORIENTED_EDGE ( 'NONE', *, *, #21821, .F. ) ;
#56695=ORIENTED_EDGE ( 'NONE', *, *, #10331, .F. ) ;
#56702=VERTEX_POINT ( 'NONE', #15013 ) ;
#56710=CARTESIAN_POINT ( 'NONE',  ( -7.250000000000000888, 7.450000000000003730, -13.00000000000000178 ) ) ;
#56713=ORIENTED_EDGE ( 'NONE', *, *, #29288, .T. ) ;
#56720=LINE ( 'NONE', #24899, #32614 ) ;
#56725=ORIENTED_EDGE ( 'NONE', *, *, #56984, .T. ) ;
#56726=ADVANCED_FACE ( 'NONE', ( #17015 ), #46825, .F. ) ;
#56738=CARTESIAN_POINT ( 'NONE',  ( -10.50000000000000178, 9.690000000000001279, 0.000000000000000000 ) ) ;
#56740=CYLINDRICAL_SURFACE ( 'NONE', #7070, 0.2000000000000005107 ) ;
#56750=FACE_OUTER_BOUND ( 'NONE', #20737, .T. ) ;
#56756=AXIS2_PLACEMENT_3D ( 'NONE', #41031, #24781, #58373 ) ;
#56764=CARTESIAN_POINT ( 'NONE',  ( -7.450000000000001954, 0.000000000000000000, -13.00000000000000178 ) ) ;
#56765=DIRECTION ( 'NONE',  ( -1.000000000000000000, 0.000000000000000000, 0.000000000000000000 ) ) ;
#56767=AXIS2_PLACEMENT_3D ( 'NONE', #15031, #14677, #36239 ) ;
#56770=VERTEX_POINT ( 'NONE', #44215 ) ;
#56777=ORIENTED_EDGE ( 'NONE', *, *, #22005, .F. ) ;
#56783=VECTOR ( 'NONE', #5681, 1000.000000000000000 ) ;
#56797=ADVANCED_FACE ( 'NONE', ( #2131 ), #6408, .F. ) ;
#56808=DIRECTION ( 'NONE',  ( -0.000000000000000000, -0.000000000000000000, 1.000000000000000000 ) ) ;
#56815=AXIS2_PLACEMENT_3D ( 'NONE', #6230, #17525, #28473 ) ;
#56821=CARTESIAN_POINT ( 'NONE',  ( 4.456444791733522252E-16, 7.450000000000002842, -12.50000000000000000 ) ) ;
#56840=ORIENTED_EDGE ( 'NONE', *, *, #39147, .F. ) ;
#56841=ORIENTED_EDGE ( 'NONE', *, *, #15119, .T. ) ;
#56848=ORIENTED_EDGE ( 'NONE', *, *, #64705, .F. ) ;
#56875=VECTOR ( 'NONE', #13120, 1000.000000000000000 ) ;
#56877=EDGE_LOOP ( 'NONE', ( #20181, #15640, #65472, #38365 ) ) ;
#56883=ORIENTED_EDGE ( 'NONE', *, *, #61779, .T. ) ;
#56886=LINE ( 'NONE', #8443, #5384 ) ;
#56889=ORIENTED_EDGE ( 'NONE', *, *, #62803, .F. ) ;
#56898=ADVANCED_FACE ( 'NONE', ( #1779 ), #23357, .F. ) ;
#56906=DIRECTION ( 'NONE',  ( -0.000000000000000000, -0.000000000000000000, -1.000000000000000000 ) ) ;
#56911=LINE ( 'NONE', #35335, #65522 ) ;
#56915=ORIENTED_EDGE ( 'NONE', *, *, #9792, .T. ) ;
#56940=LINE ( 'NONE', #41733, #4838 ) ;
#56941=VERTEX_POINT ( 'NONE', #25452 ) ;
#56943=ORIENTED_EDGE ( 'NONE', *, *, #5782, .T. ) ;
#56954=VERTEX_POINT ( 'NONE', #35333 ) ;
#56956=LINE ( 'NONE', #8874, #7063 ) ;
#56960=DIRECTION ( 'NONE',  ( 0.000000000000000000, 0.000000000000000000, -1.000000000000000000 ) ) ;
#56969=LINE ( 'NONE', #8182, #61726 ) ;
#56972=CARTESIAN_POINT ( 'NONE',  ( 7.250000000000004441, 7.450000000000001954, -20.00000000000000000 ) ) ;
#56975=EDGE_LOOP ( 'NONE', ( #63142, #59195, #55292, #39154 ) ) ;
#56984=EDGE_CURVE ( 'NONE', #17866, #13194, #47363, .T. ) ;
#56987=DIRECTION ( 'NONE',  ( -1.000000000000000000, 0.000000000000000000, 0.000000000000000000 ) ) ;
#56989=ORIENTED_EDGE ( 'NONE', *, *, #57099, .F. ) ;
#57002=EDGE_CURVE ( 'NONE', #63059, #59074, #30843, .T. ) ;
#57005=CARTESIAN_POINT ( 'NONE',  ( 7.250000000000005329, -7.449999999999998401, -15.00000000000000000 ) ) ;
#57012=ORIENTED_EDGE ( 'NONE', *, *, #57933, .F. ) ;
#57016=EDGE_CURVE ( 'NONE', #30915, #34406, #41707, .T. ) ;
#57020=CARTESIAN_POINT ( 'NONE',  ( 7.250000000000005329, -7.249999999999998224, -25.50000000000000355 ) ) ;
#57027=CARTESIAN_POINT ( 'NONE',  ( -7.250000000000000000, -7.449999999999998401, -19.00000000000000000 ) ) ;
#57030=ORIENTED_EDGE ( 'NONE', *, *, #38282, .F. ) ;
#57034=LINE ( 'NONE', #15310, #50153 ) ;
#57035=ADVANCED_FACE ( 'NONE', ( #63640 ), #69283, .F. ) ;
#57039=ORIENTED_EDGE ( 'NONE', *, *, #44412, .F. ) ;
#57044=ORIENTED_EDGE ( 'NONE', *, *, #35860, .F. ) ;
#57050=ORIENTED_EDGE ( 'NONE', *, *, #69088, .T. ) ;
#57053=EDGE_CURVE ( 'NONE', #61584, #64098, #4936, .T. ) ;
#57057=ORIENTED_EDGE ( 'NONE', *, *, #47921, .F. ) ;
#57064=VECTOR ( 'NONE', #61072, 1000.000000000000000 ) ;
#57065=VERTEX_POINT ( 'NONE', #58682 ) ;
#57067=EDGE_CURVE ( 'NONE', #22518, #43019, #24115, .T. ) ;
#57069=CIRCLE ( 'NONE', #36806, 1.000000000000003553 ) ;
#57082=VECTOR ( 'NONE', #32790, 1000.000000000000000 ) ;
#57087=CARTESIAN_POINT ( 'NONE',  ( 7.250000000000004441, 7.450000000000001954, -23.50000000000000000 ) ) ;
#57088=ORIENTED_EDGE ( 'NONE', *, *, #13240, .T. ) ;
#57089=CARTESIAN_POINT ( 'NONE',  ( 7.250000000000004441, 7.450000000000001954, -20.50000000000000000 ) ) ;
#57091=CARTESIAN_POINT ( 'NONE',  ( -7.250000000000000888, 8.250000000000001776, -26.00000000000001066 ) ) ;
#57094=CARTESIAN_POINT ( 'NONE',  ( 7.250000000000005329, 7.250000000000000888, -19.50000000000000000 ) ) ;
#57097=CARTESIAN_POINT ( 'NONE',  ( 2.500000000000000000, 3.061616997868383141E-16, -29.90000000000000924 ) ) ;
#57099=EDGE_CURVE ( 'NONE', #13987, #9996, #21539, .T. ) ;
#57109=VECTOR ( 'NONE', #24201, 1000.000000000000000 ) ;
#57116=FACE_BOUND ( 'NONE', #32514, .T. ) ;
#57119=DIRECTION ( 'NONE',  ( -0.000000000000000000, -0.000000000000000000, 1.000000000000000000 ) ) ;
#57124=EDGE_LOOP ( 'NONE', ( #64047, #17076, #37146, #28144 ) ) ;
#57125=VERTEX_POINT ( 'NONE', #20837 ) ;
#57129=AXIS2_PLACEMENT_3D ( 'NONE', #14718, #57845, #59247 ) ;
#57142=DIRECTION ( 'NONE',  ( -1.000000000000000000, 0.000000000000000000, 0.000000000000000000 ) ) ;
#57148=DIRECTION ( 'NONE',  ( -1.000000000000000000, 0.000000000000000000, 0.000000000000000000 ) ) ;
#57157=AXIS2_PLACEMENT_3D ( 'NONE', #1889, #34388, #67293 ) ;
#57158=LINE ( 'NONE', #63165, #15580 ) ;
#57159=ADVANCED_FACE ( 'NONE', ( #26861 ), #54423, .F. ) ;
#57171=AXIS2_PLACEMENT_3D ( 'NONE', #6059, #54158, #10660 ) ;
#57173=ADVANCED_FACE ( 'NONE', ( #22243 ), #43801, .T. ) ;
#57178=CARTESIAN_POINT ( 'NONE',  ( -7.250000000000000888, -8.249999999999998224, -26.00000000000001066 ) ) ;
#57188=FACE_OUTER_BOUND ( 'NONE', #18839, .T. ) ;
#57195=ORIENTED_EDGE ( 'NONE', *, *, #67993, .F. ) ;
#57205=LINE ( 'NONE', #18310, #22323 ) ;
#57209=EDGE_CURVE ( 'NONE', #43309, #17252, #52351, .T. ) ;
#57215=CARTESIAN_POINT ( 'NONE',  ( 0.000000000000000000, 0.000000000000000000, -30.00000000000001066 ) ) ;
#57216=VERTEX_POINT ( 'NONE', #39183 ) ;
#57223=ORIENTED_EDGE ( 'NONE', *, *, #57692, .F. ) ;
#57224=VECTOR ( 'NONE', #32055, 1000.000000000000000 ) ;
#57230=VECTOR ( 'NONE', #742, 1000.000000000000000 ) ;
#57232=CARTESIAN_POINT ( 'NONE',  ( 0.000000000000000000, 0.000000000000000000, -18.50000000000000000 ) ) ;
#57235=VECTOR ( 'NONE', #38131, 1000.000000000000000 ) ;
#57236=DIRECTION ( 'NONE',  ( -0.000000000000000000, -0.000000000000000000, -1.000000000000000000 ) ) ;
#57248=DIRECTION ( 'NONE',  ( -0.000000000000000000, -0.000000000000000000, 1.000000000000000000 ) ) ;
#57254=CARTESIAN_POINT ( 'NONE',  ( -7.250000000000000000, -7.449999999999998401, -8.500000000000000000 ) ) ;
#57259=EDGE_CURVE ( 'NONE', #38565, #48363, #60388, .T. ) ;
#57267=CARTESIAN_POINT ( 'NONE',  ( 8.250000000000005329, 8.250000000000001776, -26.00000000000001066 ) ) ;
#57273=AXIS2_PLACEMENT_3D ( 'NONE', #44010, #32716, #39057 ) ;
#57275=VERTEX_POINT ( 'NONE', #44821 ) ;
#57280=EDGE_LOOP ( 'NONE', ( #8807, #57341, #17907, #64965 ) ) ;
#57282=AXIS2_PLACEMENT_3D ( 'NONE', #6560, #17854, #55346 ) ;
#57284=CARTESIAN_POINT ( 'NONE',  ( 4.456444791733522252E-16, 7.450000000000002842, -12.50000000000000000 ) ) ;
#57285=DIRECTION ( 'NONE',  ( 0.000000000000000000, 0.000000000000000000, -1.000000000000000000 ) ) ;
#57286=ORIENTED_EDGE ( 'NONE', *, *, #33032, .T. ) ;
#57289=ORIENTED_EDGE ( 'NONE', *, *, #23700, .T. ) ;
#57293=CARTESIAN_POINT ( 'NONE',  ( -7.450000000000001954, -7.249999999999998224, -18.50000000000000000 ) ) ;
#57303=ORIENTED_EDGE ( 'NONE', *, *, #501, .T. ) ;
#57307=DIRECTION ( 'NONE',  ( -1.000000000000000000, 0.000000000000000000, 0.000000000000000000 ) ) ;
#57310=ORIENTED_EDGE ( 'NONE', *, *, #69494, .F. ) ;
#57319=EDGE_CURVE ( 'NONE', #40613, #9508, #11604, .T. ) ;
#57324=LINE ( 'NONE', #58391, #30111 ) ;
#57328=ORIENTED_EDGE ( 'NONE', *, *, #14844, .F. ) ;
#57333=CARTESIAN_POINT ( 'NONE',  ( 0.000000000000000000, -8.249999999999998224, -15.00000000000000000 ) ) ;
#57335=LINE ( 'NONE', #56634, #68910 ) ;
#57339=EDGE_CURVE ( 'NONE', #19122, #33105, #39517, .T. ) ;
#57340=DIRECTION ( 'NONE',  ( -0.000000000000000000, -0.000000000000000000, 1.000000000000000000 ) ) ;
#57341=ORIENTED_EDGE ( 'NONE', *, *, #45108, .F. ) ;
#57346=DIRECTION ( 'NONE',  ( 0.000000000000000000, 0.000000000000000000, -1.000000000000000000 ) ) ;
#57356=CARTESIAN_POINT ( 'NONE',  ( 4.456444791733522252E-16, 7.450000000000002842, -25.50000000000000355 ) ) ;
#57361=EDGE_LOOP ( 'NONE', ( #10294, #32245, #51004, #2020 ) ) ;
#57364=CARTESIAN_POINT ( 'NONE',  ( 7.250000000000005329, 8.250000000000001776, -15.50000000000000000 ) ) ;
#57366=LINE ( 'NONE', #47805, #32906 ) ;
#57370=EDGE_LOOP ( 'NONE', ( #32027, #56087, #26131, #47395 ) ) ;
#57373=DIRECTION ( 'NONE',  ( 0.000000000000000000, -0.000000000000000000, 1.000000000000000000 ) ) ;
#57376=EDGE_CURVE ( 'NONE', #39010, #32501, #67797, .T. ) ;
#57379=AXIS2_PLACEMENT_3D ( 'NONE', #42611, #26014, #63486 ) ;
#57400=ORIENTED_EDGE ( 'NONE', *, *, #4429, .T. ) ;
#57420=CARTESIAN_POINT ( 'NONE',  ( 7.250000000000004441, 7.450000000000001954, -21.50000000000000000 ) ) ;
#57422=CARTESIAN_POINT ( 'NONE',  ( 7.250000000000005329, 7.250000000000000888, -25.00000000000000000 ) ) ;
#57424=CARTESIAN_POINT ( 'NONE',  ( 6.500000000000002665, 6.500000000000000888, -1.000000000000000000 ) ) ;
#57431=VECTOR ( 'NONE', #17492, 1000.000000000000000 ) ;
#57432=DIRECTION ( 'NONE',  ( 0.000000000000000000, 0.000000000000000000, 1.000000000000000000 ) ) ;
#57439=FACE_OUTER_BOUND ( 'NONE', #68178, .T. ) ;
#57440=EDGE_LOOP ( 'NONE', ( #19679, #64015, #54962, #6010 ) ) ;
#57444=DIRECTION ( 'NONE',  ( 0.000000000000000000, -0.000000000000000000, -1.000000000000000000 ) ) ;
#57449=DIRECTION ( 'NONE',  ( 1.000000000000000000, -5.981805089575196197E-17, 0.000000000000000000 ) ) ;
#57450=CYLINDRICAL_SURFACE ( 'NONE', #55414, 0.8100000000000017186 ) ;
#57458=PLANE ( 'NONE',  #55562 ) ;
#57459=EDGE_LOOP ( 'NONE', ( #28774, #47608, #17019, #40681 ) ) ;
#57460=VERTEX_POINT ( 'NONE', #42242 ) ;
#57468=DIRECTION ( 'NONE',  ( 1.000000000000000000, 0.000000000000000000, 0.000000000000000000 ) ) ;
#57470=VERTEX_POINT ( 'NONE', #3370 ) ;
#57493=CIRCLE ( 'NONE', #41696, 0.2000000000000005107 ) ;
#57496=FACE_OUTER_BOUND ( 'NONE', #67622, .T. ) ;
#57509=ORIENTED_EDGE ( 'NONE', *, *, #44364, .T. ) ;
#57517=ADVANCED_FACE ( 'NONE', ( #20333 ), #25654, .T. ) ;
#57521=CARTESIAN_POINT ( 'NONE',  ( 7.450000000000004619, -1.336933437520057563E-15, -20.50000000000000000 ) ) ;
#57525=CARTESIAN_POINT ( 'NONE',  ( 0.000000000000000000, -8.749999999999998224, -30.00000000000001066 ) ) ;
#57530=DIRECTION ( 'NONE',  ( -0.000000000000000000, -0.000000000000000000, 1.000000000000000000 ) ) ;
#57559=CARTESIAN_POINT ( 'NONE',  ( -7.450000000000001954, 7.250000000000000000, -18.00000000000000000 ) ) ;
#57562=ORIENTED_EDGE ( 'NONE', *, *, #41454, .T. ) ;
#57563=ADVANCED_FACE ( 'NONE', ( #58533, #26001 ), #69121, .T. ) ;
#57573=ORIENTED_EDGE ( 'NONE', *, *, #8794, .T. ) ;
#57581=AXIS2_PLACEMENT_3D ( 'NONE', #17344, #32927, #38919 ) ;
#57582=FACE_OUTER_BOUND ( 'NONE', #59706, .T. ) ;
#57594=CARTESIAN_POINT ( 'NONE',  ( -7.250000000000001776, -7.249999999999998224, -23.00000000000000000 ) ) ;
#57601=ORIENTED_EDGE ( 'NONE', *, *, #52829, .T. ) ;
#57606=ORIENTED_EDGE ( 'NONE', *, *, #64540, .T. ) ;
#57610=EDGE_CURVE ( 'NONE', #60006, #26902, #37303, .T. ) ;
#57612=ADVANCED_FACE ( 'NONE', ( #38000 ), #60236, .F. ) ;
#57616=DIRECTION ( 'NONE',  ( 1.000000000000000000, -5.981805089575194965E-17, 0.000000000000000000 ) ) ;
#57617=EDGE_CURVE ( 'NONE', #35171, #68411, #5482, .T. ) ;
#57636=VECTOR ( 'NONE', #53512, 1000.000000000000000 ) ;
#57637=DIRECTION ( 'NONE',  ( 1.000000000000000000, 0.000000000000000000, 0.000000000000000000 ) ) ;
#57646=LINE ( 'NONE', #36076, #53771 ) ;
#57650=CARTESIAN_POINT ( 'NONE',  ( 0.000000000000000000, -8.249999999999998224, -10.50000000000000000 ) ) ;
#57652=CARTESIAN_POINT ( 'NONE',  ( -7.250000000000000000, -7.449999999999998401, -11.00000000000000000 ) ) ;
#57662=ORIENTED_EDGE ( 'NONE', *, *, #31953, .T. ) ;
#57675=DIRECTION ( 'NONE',  ( 0.000000000000000000, 0.000000000000000000, 1.000000000000000000 ) ) ;
#57684=LINE ( 'NONE', #47083, #42959 ) ;
#57689=DIRECTION ( 'NONE',  ( -1.000000000000000000, 1.794541526872559352E-16, 0.000000000000000000 ) ) ;
#57691=CARTESIAN_POINT ( 'NONE',  ( -7.250000000000000888, 8.250000000000001776, -17.50000000000000000 ) ) ;
#57692=EDGE_CURVE ( 'NONE', #66827, #69141, #16429, .T. ) ;
#57703=CARTESIAN_POINT ( 'NONE',  ( 7.250000000000005329, 7.250000000000000888, -26.00000000000001066 ) ) ;
#57704=DIRECTION ( 'NONE',  ( -5.981805089575196197E-17, -1.000000000000000000, 0.000000000000000000 ) ) ;
#57709=ORIENTED_EDGE ( 'NONE', *, *, #60518, .F. ) ;
#57716=ORIENTED_EDGE ( 'NONE', *, *, #3423, .F. ) ;
#57720=ORIENTED_EDGE ( 'NONE', *, *, #22371, .F. ) ;
#57738=EDGE_CURVE ( 'NONE', #33741, #25825, #45453, .T. ) ;
#57748=ADVANCED_FACE ( 'NONE', ( #7535 ), #6833, .F. ) ;
#57751=EDGE_LOOP ( 'NONE', ( #56626, #34761, #54199, #1909, #14055, #34459, #33045, #5989 ) ) ;
#57761=AXIS2_PLACEMENT_3D ( 'NONE', #42973, #10794, #9406 ) ;
#57762=CARTESIAN_POINT ( 'NONE',  ( -7.250000000000000888, 7.250000000000001776, -20.00000000000000000 ) ) ;
#57765=ORIENTED_EDGE ( 'NONE', *, *, #30751, .T. ) ;
#57771=VERTEX_POINT ( 'NONE', #23804 ) ;
#57772=CARTESIAN_POINT ( 'NONE',  ( -7.250000000000000888, 7.250000000000001776, -7.500000000000000000 ) ) ;
#57775=CARTESIAN_POINT ( 'NONE',  ( 0.000000000000000000, -7.449999999999998401, -23.50000000000000000 ) ) ;
#57776=VERTEX_POINT ( 'NONE', #29109 ) ;
#57785=DIRECTION ( 'NONE',  ( 0.000000000000000000, 0.000000000000000000, 1.000000000000000000 ) ) ;
#57790=VECTOR ( 'NONE', #43172, 1000.000000000000000 ) ;
#57795=DIRECTION ( 'NONE',  ( -1.000000000000000000, 0.000000000000000000, 0.000000000000000000 ) ) ;
#57800=DIRECTION ( 'NONE',  ( 0.000000000000000000, 0.000000000000000000, 1.000000000000000000 ) ) ;
#57802=FACE_OUTER_BOUND ( 'NONE', #35618, .T. ) ;
#57805=CARTESIAN_POINT ( 'NONE',  ( -7.250000000000000888, -8.249999999999998224, -22.00000000000000000 ) ) ;
#57807=EDGE_CURVE ( 'NONE', #17836, #26867, #45359, .T. ) ;
#57833=ADVANCED_FACE ( 'NONE', ( #22763 ), #61264, .F. ) ;
#57839=AXIS2_PLACEMENT_3D ( 'NONE', #42411, #9903, #31473 ) ;
#57845=DIRECTION ( 'NONE',  ( 0.000000000000000000, 0.000000000000000000, -1.000000000000000000 ) ) ;
#57851=EDGE_LOOP ( 'NONE', ( #25096, #13724, #59429, #44996 ) ) ;
#57853=CARTESIAN_POINT ( 'NONE',  ( -7.250000000000001776, -7.249999999999998224, -10.50000000000000000 ) ) ;
#57854=CARTESIAN_POINT ( 'NONE',  ( -9.690000000000001279, 8.750000000000000000, -5.000000000000000000 ) ) ;
#57864=EDGE_CURVE ( 'NONE', #42030, #62306, #37619, .T. ) ;
#57865=DIRECTION ( 'NONE',  ( 0.000000000000000000, -0.000000000000000000, 1.000000000000000000 ) ) ;
#57872=EDGE_LOOP ( 'NONE', ( #27574, #50644, #12705, #7114 ) ) ;
#57879=PLANE ( 'NONE',  #15052 ) ;
#57880=ADVANCED_FACE ( 'NONE', ( #8583, #41469 ), #56677, .F. ) ;
#57884=ORIENTED_EDGE ( 'NONE', *, *, #44076, .T. ) ;
#57893=VERTEX_POINT ( 'NONE', #30506 ) ;
#57894=EDGE_CURVE ( 'NONE', #42070, #64467, #40765, .T. ) ;
#57896=LINE ( 'NONE', #26425, #50312 ) ;
#57898=CIRCLE ( 'NONE', #1464, 0.7499999999999997780 ) ;
#57899=VERTEX_POINT ( 'NONE', #25921 ) ;
#57902=EDGE_LOOP ( 'NONE', ( #61627, #21744, #48069, #54104 ) ) ;
#57903=ADVANCED_FACE ( 'NONE', ( #2935 ), #30158, .F. ) ;
#57918=VECTOR ( 'NONE', #65331, 1000.000000000000000 ) ;
#57920=CARTESIAN_POINT ( 'NONE',  ( -7.250000000000000888, -8.249999999999998224, -23.50000000000000000 ) ) ;
#57923=DIRECTION ( 'NONE',  ( -1.000000000000000000, 0.000000000000000000, 0.000000000000000000 ) ) ;
#57928=VERTEX_POINT ( 'NONE', #52433 ) ;
#57933=EDGE_CURVE ( 'NONE', #13530, #20828, #1451, .T. ) ;
#57945=CARTESIAN_POINT ( 'NONE',  ( 8.250000000000005329, -7.249999999999998224, -18.00000000000000000 ) ) ;
#57957=DIRECTION ( 'NONE',  ( 0.000000000000000000, -1.000000000000000000, 0.000000000000000000 ) ) ;
#57959=CARTESIAN_POINT ( 'NONE',  ( 0.000000000000000000, 8.250000000000001776, -23.50000000000000000 ) ) ;
#57969=EDGE_CURVE ( 'NONE', #57893, #16799, #59823, .T. ) ;
#57971=AXIS2_PLACEMENT_3D ( 'NONE', #48015, #36351, #26110 ) ;
#57972=DIRECTION ( 'NONE',  ( 0.000000000000000000, 0.000000000000000000, 1.000000000000000000 ) ) ;
#57975=DIRECTION ( 'NONE',  ( 0.000000000000000000, 0.000000000000000000, 1.000000000000000000 ) ) ;
#57982=DIRECTION ( 'NONE',  ( -5.981805089575196197E-17, -1.000000000000000000, 0.000000000000000000 ) ) ;
#57986=DIRECTION ( 'NONE',  ( -0.000000000000000000, -0.000000000000000000, -1.000000000000000000 ) ) ;
#57989=DIRECTION ( 'NONE',  ( -1.794541526872559352E-16, -1.000000000000000000, 0.000000000000000000 ) ) ;
#57996=FACE_OUTER_BOUND ( 'NONE', #52444, .T. ) ;
#57998=LINE ( 'NONE', #53066, #36640 ) ;
#58002=FACE_OUTER_BOUND ( 'NONE', #32566, .T. ) ;
#58003=VERTEX_POINT ( 'NONE', #54527 ) ;
#58009=EDGE_CURVE ( 'NONE', #48363, #35816, #9390, .T. ) ;
#58014=CARTESIAN_POINT ( 'NONE',  ( -9.689999999999999503, -10.50000000000000178, -5.000000000000000000 ) ) ;
#58027=CARTESIAN_POINT ( 'NONE',  ( -7.250000000000000888, -8.249999999999998224, -8.500000000000000000 ) ) ;
#58029=FACE_OUTER_BOUND ( 'NONE', #58348, .T. ) ;
#58044=DIRECTION ( 'NONE',  ( -1.000000000000000000, 0.000000000000000000, 0.000000000000000000 ) ) ;
#58047=CIRCLE ( 'NONE', #51270, 1.000000000000000000 ) ;
#58050=EDGE_CURVE ( 'NONE', #61156, #46508, #42517, .T. ) ;
#58054=LINE ( 'NONE', #46735, #50411 ) ;
#58055=AXIS2_PLACEMENT_3D ( 'NONE', #46678, #4272, #4617 ) ;
#58068=CARTESIAN_POINT ( 'NONE',  ( 7.250000000000005329, 8.250000000000001776, -26.00000000000001066 ) ) ;
#58069=DIRECTION ( 'NONE',  ( -0.000000000000000000, -0.000000000000000000, 1.000000000000000000 ) ) ;
#58071=ORIENTED_EDGE ( 'NONE', *, *, #51776, .F. ) ;
#58101=CIRCLE ( 'NONE', #28707, 0.9999999999999991118 ) ;
#58102=VECTOR ( 'NONE', #31621, 1000.000000000000000 ) ;
#58113=DIRECTION ( 'NONE',  ( -0.000000000000000000, -0.000000000000000000, -1.000000000000000000 ) ) ;
#58124=VERTEX_POINT ( 'NONE', #21993 ) ;
#58127=CARTESIAN_POINT ( 'NONE',  ( 8.250000000000005329, 7.250000000000000888, -26.00000000000001066 ) ) ;
#58132=AXIS2_PLACEMENT_3D ( 'NONE', #32421, #53989, #5542 ) ;
#58133=ORIENTED_EDGE ( 'NONE', *, *, #65490, .T. ) ;
#58137=ADVANCED_FACE ( 'NONE', ( #56247 ), #23377, .F. ) ;
#58148=LINE ( 'NONE', #30575, #9363 ) ;
#58151=DIRECTION ( 'NONE',  ( -0.000000000000000000, -0.000000000000000000, 1.000000000000000000 ) ) ;
#58152=CARTESIAN_POINT ( 'NONE',  ( 0.000000000000000000, 0.000000000000000000, -21.50000000000000000 ) ) ;
#58154=VECTOR ( 'NONE', #8771, 1000.000000000000000 ) ;
#58160=VERTEX_POINT ( 'NONE', #17369 ) ;
#58161=EDGE_CURVE ( 'NONE', #17846, #11392, #66844, .T. ) ;
#58162=CIRCLE ( 'NONE', #22026, 0.1999999999999987899 ) ;
#58184=ADVANCED_FACE ( 'NONE', ( #54872, #22353 ), #7449, .F. ) ;
#58186=ORIENTED_EDGE ( 'NONE', *, *, #38243, .T. ) ;
#58194=CARTESIAN_POINT ( 'NONE',  ( -7.450000000000001954, 0.000000000000000000, -22.50000000000000000 ) ) ;
#58201=PLANE ( 'NONE',  #44693 ) ;
#58207=CARTESIAN_POINT ( 'NONE',  ( 7.250000000000005329, -7.249999999999998224, -10.50000000000000000 ) ) ;
#58221=FACE_OUTER_BOUND ( 'NONE', #63735, .T. ) ;
#58225=ADVANCED_FACE ( 'NONE', ( #18395 ), #38606, .F. ) ;
#58228=DIRECTION ( 'NONE',  ( 0.000000000000000000, 0.000000000000000000, 1.000000000000000000 ) ) ;
#58229=CARTESIAN_POINT ( 'NONE',  ( 7.450000000000006395, 7.250000000000000888, -23.00000000000000000 ) ) ;
#58231=FACE_OUTER_BOUND ( 'NONE', #6829, .T. ) ;
#58238=EDGE_CURVE ( 'NONE', #127, #34015, #45272, .T. ) ;
#58240=EDGE_LOOP ( 'NONE', ( #13146, #44437, #24870, #45626 ) ) ;
#58245=EDGE_LOOP ( 'NONE', ( #57562, #44646, #55160, #67834 ) ) ;
#58246=FACE_OUTER_BOUND ( 'NONE', #69735, .T. ) ;
#58252=AXIS2_PLACEMENT_3D ( 'NONE', #58791, #69038, #20595 ) ;
#58254=EDGE_LOOP ( 'NONE', ( #66741, #48793, #17480, #7956 ) ) ;
#58276=ORIENTED_EDGE ( 'NONE', *, *, #49673, .F. ) ;
#58284=VECTOR ( 'NONE', #15074, 1000.000000000000000 ) ;
#58294=DIRECTION ( 'NONE',  ( -1.000000000000000000, 0.000000000000000000, -0.000000000000000000 ) ) ;
#58295=ORIENTED_EDGE ( 'NONE', *, *, #53160, .T. ) ;
#58296=AXIS2_PLACEMENT_3D ( 'NONE', #61214, #12775, #7131 ) ;
#58298=CIRCLE ( 'NONE', #69608, 1.000000000000000000 ) ;
#58312=ADVANCED_FACE ( 'NONE', ( #19799 ), #41378, .F. ) ;
#58316=DIRECTION ( 'NONE',  ( -0.000000000000000000, 0.000000000000000000, 1.000000000000000000 ) ) ;
#58319=VERTEX_POINT ( 'NONE', #8138 ) ;
#58324=ORIENTED_EDGE ( 'NONE', *, *, #22793, .T. ) ;
#58328=DIRECTION ( 'NONE',  ( -1.000000000000000000, 0.000000000000000000, 0.000000000000000000 ) ) ;
#58329=PLANE ( 'NONE',  #6999 ) ;
#58330=EDGE_CURVE ( 'NONE', #17298, #67142, #67908, .T. ) ;
#58333=DIRECTION ( 'NONE',  ( 0.000000000000000000, 0.000000000000000000, 1.000000000000000000 ) ) ;
#58344=ORIENTED_EDGE ( 'NONE', *, *, #6355, .F. ) ;
#58345=DIRECTION ( 'NONE',  ( 1.000000000000000000, 0.000000000000000000, 0.000000000000000000 ) ) ;
#58347=AXIS2_PLACEMENT_3D ( 'NONE', #10049, #53536, #5090 ) ;
#58348=EDGE_LOOP ( 'NONE', ( #45834, #47500, #20101, #32594 ) ) ;
#58353=VECTOR ( 'NONE', #49508, 1000.000000000000000 ) ;
#58367=CARTESIAN_POINT ( 'NONE',  ( 7.250000000000005329, -7.249999999999998224, -16.00000000000000000 ) ) ;
#58368=AXIS2_PLACEMENT_3D ( 'NONE', #24100, #45662, #8531 ) ;
#58373=DIRECTION ( 'NONE',  ( -1.000000000000000000, 0.000000000000000000, 0.000000000000000000 ) ) ;
#58376=DIRECTION ( 'NONE',  ( 1.000000000000000000, -0.000000000000000000, 0.000000000000000000 ) ) ;
#58379=CYLINDRICAL_SURFACE ( 'NONE', #8993, 0.7499999999999997780 ) ;
#58391=CARTESIAN_POINT ( 'NONE',  ( 7.250000000000005329, -8.249999999999998224, -26.00000000000001066 ) ) ;
#58395=EDGE_LOOP ( 'NONE', ( #43312, #30150, #9758, #718, #29758, #508, #11024, #68365 ) ) ;
#58403=EDGE_CURVE ( 'NONE', #2479, #30178, #22854, .T. ) ;
#58404=LINE ( 'NONE', #4318, #45208 ) ;
#58407=CARTESIAN_POINT ( 'NONE',  ( -7.250000000000000888, 7.450000000000003730, -13.50000000000000178 ) ) ;
#58413=VECTOR ( 'NONE', #25687, 1000.000000000000000 ) ;
#58423=LINE ( 'NONE', #37539, #12487 ) ;
#58434=ORIENTED_EDGE ( 'NONE', *, *, #19731, .T. ) ;
#58439=LINE ( 'NONE', #31563, #44192 ) ;
#58449=PLANE ( 'NONE',  #58252 ) ;
#58453=ORIENTED_EDGE ( 'NONE', *, *, #51832, .T. ) ;
#58457=AXIS2_PLACEMENT_3D ( 'NONE', #7657, #40179, #2360 ) ;
#58460=VECTOR ( 'NONE', #22671, 1000.000000000000000 ) ;
#58463=LINE ( 'NONE', #103, #51167 ) ;
#58464=ORIENTED_EDGE ( 'NONE', *, *, #50523, .T. ) ;
#58478=DIRECTION ( 'NONE',  ( 0.000000000000000000, 0.000000000000000000, 1.000000000000000000 ) ) ;
#58485=DIRECTION ( 'NONE',  ( 1.000000000000000000, 0.000000000000000000, 0.000000000000000000 ) ) ;
#58493=DIRECTION ( 'NONE',  ( 0.000000000000000000, -0.000000000000000000, 1.000000000000000000 ) ) ;
#58499=DIRECTION ( 'NONE',  ( 0.000000000000000000, 1.000000000000000000, 0.000000000000000000 ) ) ;
#58507=CARTESIAN_POINT ( 'NONE',  ( -7.250000000000000888, 7.250000000000001776, -13.50000000000000178 ) ) ;
#58515=EDGE_CURVE ( 'NONE', #28003, #14054, #28836, .T. ) ;
#58524=EDGE_CURVE ( 'NONE', #11076, #59106, #7270, .T. ) ;
#58527=DIRECTION ( 'NONE',  ( -1.000000000000000000, 0.000000000000000000, 0.000000000000000000 ) ) ;
#58533=FACE_BOUND ( 'NONE', #59975, .T. ) ;
#58539=ORIENTED_EDGE ( 'NONE', *, *, #59813, .F. ) ;
#58543=EDGE_CURVE ( 'NONE', #65577, #48640, #24605, .T. ) ;
#58551=ORIENTED_EDGE ( 'NONE', *, *, #27751, .T. ) ;
#58557=CIRCLE ( 'NONE', #19006, 0.8100000000000017186 ) ;
#58561=DIRECTION ( 'NONE',  ( -0.000000000000000000, -0.000000000000000000, 1.000000000000000000 ) ) ;
#58562=VERTEX_POINT ( 'NONE', #50425 ) ;
#58563=ORIENTED_EDGE ( 'NONE', *, *, #7658, .F. ) ;
#58565=CARTESIAN_POINT ( 'NONE',  ( 8.750000000000003553, 7.750000000000000000, -5.000000000000000000 ) ) ;
#58574=DIRECTION ( 'NONE',  ( 0.000000000000000000, 0.000000000000000000, -1.000000000000000000 ) ) ;
#58575=DIRECTION ( 'NONE',  ( 0.000000000000000000, 0.000000000000000000, 1.000000000000000000 ) ) ;
#58589=ORIENTED_EDGE ( 'NONE', *, *, #35862, .T. ) ;
#58590=LINE ( 'NONE', #15459, #50203 ) ;
#58611=ORIENTED_EDGE ( 'NONE', *, *, #59248, .T. ) ;
#58614=VERTEX_POINT ( 'NONE', #2673 ) ;
#58616=CARTESIAN_POINT ( 'NONE',  ( 7.250000000000005329, -7.249999999999998224, -11.50000000000000000 ) ) ;
#58622=CARTESIAN_POINT ( 'NONE',  ( 7.250000000000005329, -8.249999999999998224, -7.500000000000000000 ) ) ;
#58629=ORIENTED_EDGE ( 'NONE', *, *, #36199, .F. ) ;
#58633=ADVANCED_FACE ( 'NONE', ( #66339 ), #61013, .F. ) ;
#58656=DIRECTION ( 'NONE',  ( 0.000000000000000000, 0.000000000000000000, 1.000000000000000000 ) ) ;
#58659=VECTOR ( 'NONE', #43326, 1000.000000000000000 ) ;
#58661=VERTEX_POINT ( 'NONE', #67728 ) ;
#58664=DIRECTION ( 'NONE',  ( -5.981805089575196197E-17, -1.000000000000000000, 0.000000000000000000 ) ) ;
#58671=LINE ( 'NONE', #26845, #37572 ) ;
#58675=CARTESIAN_POINT ( 'NONE',  ( 7.450000000000006395, 7.250000000000000888, -18.00000000000000000 ) ) ;
#58682=CARTESIAN_POINT ( 'NONE',  ( -7.250000000000000888, -8.249999999999998224, -21.50000000000000000 ) ) ;
#58696=FACE_OUTER_BOUND ( 'NONE', #49735, .T. ) ;
#58702=CARTESIAN_POINT ( 'NONE',  ( 8.250000000000005329, 0.000000000000000000, -11.00000000000000000 ) ) ;
#58705=ORIENTED_EDGE ( 'NONE', *, *, #36187, .T. ) ;
#58708=CARTESIAN_POINT ( 'NONE',  ( 7.250000000000004441, 7.450000000000001954, -11.50000000000000000 ) ) ;
#58709=CYLINDRICAL_SURFACE ( 'NONE', #60300, 1.000000000000000000 ) ;
#58720=ADVANCED_FACE ( 'NONE', ( #41906 ), #15041, .F. ) ;
#58728=LINE ( 'NONE', #25236, #26715 ) ;
#58750=FACE_OUTER_BOUND ( 'NONE', #32928, .T. ) ;
#58755=VECTOR ( 'NONE', #62821, 1000.000000000000000 ) ;
#58764=AXIS2_PLACEMENT_3D ( 'NONE', #1920, #23484, #61286 ) ;
#58768=ORIENTED_EDGE ( 'NONE', *, *, #8300, .F. ) ;
#58787=VECTOR ( 'NONE', #53859, 1000.000000000000000 ) ;
#58790=ADVANCED_FACE ( 'NONE', ( #62772 ), #9028, .T. ) ;
#58791=CARTESIAN_POINT ( 'NONE',  ( 8.250000000000005329, 8.250000000000001776, -26.00000000000001066 ) ) ;
#58798=ADVANCED_FACE ( 'NONE', ( #896 ), #37317, .T. ) ;
#58812=CARTESIAN_POINT ( 'NONE',  ( -7.250000000000001776, -7.249999999999998224, -21.00000000000000000 ) ) ;
#58813=ORIENTED_EDGE ( 'NONE', *, *, #9158, .T. ) ;
#58831=DIRECTION ( 'NONE',  ( -1.794541526872559352E-16, -1.000000000000000000, 0.000000000000000000 ) ) ;
#58833=EDGE_LOOP ( 'NONE', ( #52870, #50572, #58589, #36069 ) ) ;
#58842=ORIENTED_EDGE ( 'NONE', *, *, #62478, .F. ) ;
#58862=VECTOR ( 'NONE', #36232, 1000.000000000000000 ) ;
#58867=ADVANCED_FACE ( 'NONE', ( #21741 ), #22772, .F. ) ;
#58871=CIRCLE ( 'NONE', #8048, 1.000000000000000000 ) ;
#58874=DIRECTION ( 'NONE',  ( -1.794541526872559352E-16, -1.000000000000000000, 0.000000000000000000 ) ) ;
#58878=FACE_OUTER_BOUND ( 'NONE', #26345, .T. ) ;
#58882=VERTEX_POINT ( 'NONE', #10434 ) ;
#58892=EDGE_LOOP ( 'NONE', ( #44853, #50034 ) ) ;
#58897=ORIENTED_EDGE ( 'NONE', *, *, #11995, .F. ) ;
#58911=PLANE ( 'NONE',  #18743 ) ;
#58914=LINE ( 'NONE', #42290, #30180 ) ;
#58923=DIRECTION ( 'NONE',  ( -1.000000000000000000, 0.000000000000000000, 0.000000000000000000 ) ) ;
#58925=ORIENTED_EDGE ( 'NONE', *, *, #19924, .F. ) ;
#58941=ORIENTED_EDGE ( 'NONE', *, *, #43588, .T. ) ;
#58943=DIRECTION ( 'NONE',  ( 0.000000000000000000, 1.000000000000000000, 0.000000000000000000 ) ) ;
#58945=ORIENTED_EDGE ( 'NONE', *, *, #54508, .T. ) ;
#58956=VECTOR ( 'NONE', #3553, 1000.000000000000000 ) ;
#58961=ORIENTED_EDGE ( 'NONE', *, *, #21479, .F. ) ;
#58962=DIRECTION ( 'NONE',  ( 0.000000000000000000, 0.000000000000000000, 1.000000000000000000 ) ) ;
#58966=EDGE_LOOP ( 'NONE', ( #8171, #19841, #56841, #55900 ) ) ;
#58971=VERTEX_POINT ( 'NONE', #2946 ) ;
#58972=DIRECTION ( 'NONE',  ( -0.000000000000000000, -0.000000000000000000, 1.000000000000000000 ) ) ;
#58974=ORIENTED_EDGE ( 'NONE', *, *, #26288, .F. ) ;
#58980=AXIS2_PLACEMENT_3D ( 'NONE', #38454, #5580, #39129 ) ;
#58989=LINE ( 'NONE', #49431, #28998 ) ;
#58990=PLANE ( 'NONE',  #25251 ) ;
#58994=CYLINDRICAL_SURFACE ( 'NONE', #25140, 0.2000000000000005107 ) ;
#59001=CARTESIAN_POINT ( 'NONE',  ( 7.250000000000004441, 7.450000000000001954, -22.50000000000000000 ) ) ;
#59008=DIRECTION ( 'NONE',  ( 0.000000000000000000, 0.000000000000000000, -1.000000000000000000 ) ) ;
#59014=LINE ( 'NONE', #10572, #54358 ) ;
#59041=ORIENTED_EDGE ( 'NONE', *, *, #28749, .F. ) ;
#59055=DIRECTION ( 'NONE',  ( -1.000000000000000000, 0.000000000000000000, 0.000000000000000000 ) ) ;
#59074=VERTEX_POINT ( 'NONE', #18858 ) ;
#59076=VERTEX_POINT ( 'NONE', #40430 ) ;
#59077=CARTESIAN_POINT ( 'NONE',  ( 7.450000000000006395, 7.250000000000000888, -9.500000000000001776 ) ) ;
#59080=AXIS2_PLACEMENT_3D ( 'NONE', #9359, #53216, #37288 ) ;
#59090=EDGE_LOOP ( 'NONE', ( #54067, #31319, #12749, #67301 ) ) ;
#59092=ORIENTED_EDGE ( 'NONE', *, *, #36009, .F. ) ;
#59096=EDGE_LOOP ( 'NONE', ( #67839, #3761, #24024, #26220 ) ) ;
#59100=ORIENTED_EDGE ( 'NONE', *, *, #3222, .F. ) ;
#59106=VERTEX_POINT ( 'NONE', #47142 ) ;
#59108=DIRECTION ( 'NONE',  ( -1.000000000000000000, 0.000000000000000000, 0.000000000000000000 ) ) ;
#59113=DIRECTION ( 'NONE',  ( -1.000000000000000000, 0.000000000000000000, 0.000000000000000000 ) ) ;
#59116=DIRECTION ( 'NONE',  ( 0.000000000000000000, 0.000000000000000000, 1.000000000000000000 ) ) ;
#59122=EDGE_LOOP ( 'NONE', ( #30747, #68599, #66363, #33178 ) ) ;
#59130=CARTESIAN_POINT ( 'NONE',  ( 7.450000000000003730, -7.249999999999997335, -11.50000000000000000 ) ) ;
#59135=ORIENTED_EDGE ( 'NONE', *, *, #29936, .T. ) ;
#59139=DIRECTION ( 'NONE',  ( 1.000000000000000000, 0.000000000000000000, 0.000000000000000000 ) ) ;
#59141=DIRECTION ( 'NONE',  ( 1.000000000000000000, -0.000000000000000000, 0.000000000000000000 ) ) ;
#59148=ORIENTED_EDGE ( 'NONE', *, *, #275, .F. ) ;
#59150=VERTEX_POINT ( 'NONE', #30515 ) ;
#59152=CARTESIAN_POINT ( 'NONE',  ( 0.000000000000000000, -7.449999999999998401, -23.50000000000000000 ) ) ;
#59164=VECTOR ( 'NONE', #45696, 1000.000000000000000 ) ;
#59173=EDGE_CURVE ( 'NONE', #6619, #57899, #52089, .T. ) ;
#59177=DIRECTION ( 'NONE',  ( -1.000000000000000000, 0.000000000000000000, 0.000000000000000000 ) ) ;
#59182=EDGE_CURVE ( 'NONE', #26651, #15828, #57034, .T. ) ;
#59195=ORIENTED_EDGE ( 'NONE', *, *, #2545, .F. ) ;
#59198=FACE_OUTER_BOUND ( 'NONE', #4000, .T. ) ;
#59212=LINE ( 'NONE', #33027, #42889 ) ;
#59223=VERTEX_POINT ( 'NONE', #53498 ) ;
#59235=UNCERTAINTY_MEASURE_WITH_UNIT (LENGTH_MEASURE( 1.000000000000000082E-05 ), #1868, 'distance_accuracy_value', 'NONE');
#59247=DIRECTION ( 'NONE',  ( -1.000000000000000000, 0.000000000000000000, 0.000000000000000000 ) ) ;
#59248=EDGE_CURVE ( 'NONE', #32586, #12501, #26501, .T. ) ;
#59249=LINE ( 'NONE', #34008, #40564 ) ;
#59252=VECTOR ( 'NONE', #49380, 1000.000000000000000 ) ;
#59253=VECTOR ( 'NONE', #1725, 1000.000000000000000 ) ;
#59258=CYLINDRICAL_SURFACE ( 'NONE', #31941, 0.8100000000000017186 ) ;
#59262=CARTESIAN_POINT ( 'NONE',  ( 6.750000000000000000, 7.750000000000000000, 5.000000000000000000 ) ) ;
#59265=CARTESIAN_POINT ( 'NONE',  ( -8.250000000000001776, -7.249999999999998224, -26.00000000000001066 ) ) ;
#59268=EDGE_LOOP ( 'NONE', ( #25738, #25879, #619, #60212 ) ) ;
#59269=DIRECTION ( 'NONE',  ( 0.000000000000000000, 0.000000000000000000, -1.000000000000000000 ) ) ;
#59270=LINE ( 'NONE', #32054, #34146 ) ;
#59272=CARTESIAN_POINT ( 'NONE',  ( 8.250000000000005329, 8.250000000000001776, -26.00000000000001066 ) ) ;
#59274=EDGE_LOOP ( 'NONE', ( #24695, #56889, #19523, #5041 ) ) ;
#59275=CARTESIAN_POINT ( 'NONE',  ( 7.250000000000005329, -7.449999999999998401, -14.50000000000000000 ) ) ;
#59279=DIRECTION ( 'NONE',  ( 0.000000000000000000, 0.000000000000000000, -1.000000000000000000 ) ) ;
#59284=ORIENTED_EDGE ( 'NONE', *, *, #22656, .F. ) ;
#59289=LINE ( 'NONE', #33713, #64210 ) ;
#59296=CARTESIAN_POINT ( 'NONE',  ( 7.250000000000005329, -7.249999999999998224, -10.50000000000000000 ) ) ;
#59317=ADVANCED_FACE ( 'NONE', ( #32624 ), #54195, .T. ) ;
#59320=CARTESIAN_POINT ( 'NONE',  ( 8.250000000000005329, -7.249999999999998224, -8.500000000000000000 ) ) ;
#59322=VERTEX_POINT ( 'NONE', #447 ) ;
#59345=DIRECTION ( 'NONE',  ( -1.000000000000000000, 0.000000000000000000, 0.000000000000000000 ) ) ;
#59353=VECTOR ( 'NONE', #31457, 1000.000000000000000 ) ;
#59367=VECTOR ( 'NONE', #7644, 1000.000000000000000 ) ;
#59372=VECTOR ( 'NONE', #47009, 1000.000000000000000 ) ;
#59375=CARTESIAN_POINT ( 'NONE',  ( -7.250000000000000888, 7.450000000000003730, -8.500000000000000000 ) ) ;
#59385=ORIENTED_EDGE ( 'NONE', *, *, #48744, .T. ) ;
#59390=DIRECTION ( 'NONE',  ( -0.000000000000000000, 0.000000000000000000, 1.000000000000000000 ) ) ;
#59404=DIRECTION ( 'NONE',  ( 0.000000000000000000, 1.000000000000000000, 0.000000000000000000 ) ) ;
#59411=CIRCLE ( 'NONE', #26661, 0.2000000000000005107 ) ;
#59414=DIRECTION ( 'NONE',  ( 0.000000000000000000, 0.000000000000000000, -1.000000000000000000 ) ) ;
#59416=VERTEX_POINT ( 'NONE', #55222 ) ;
#59421=DIRECTION ( 'NONE',  ( 0.000000000000000000, 0.000000000000000000, -1.000000000000000000 ) ) ;
#59425=EDGE_CURVE ( 'NONE', #63788, #48129, #6443, .T. ) ;
#59427=CYLINDRICAL_SURFACE ( 'NONE', #24913, 0.1999999999999996503 ) ;
#59429=ORIENTED_EDGE ( 'NONE', *, *, #42795, .F. ) ;
#59433=CARTESIAN_POINT ( 'NONE',  ( 8.250000000000005329, -7.249999999999998224, -18.50000000000000000 ) ) ;
#59439=DIRECTION ( 'NONE',  ( -0.000000000000000000, -1.000000000000000000, -0.000000000000000000 ) ) ;
#59442=DIRECTION ( 'NONE',  ( -1.000000000000000000, 0.000000000000000000, 0.000000000000000000 ) ) ;
#59447=CIRCLE ( 'NONE', #38005, 0.9999999999999991118 ) ;
#59449=CARTESIAN_POINT ( 'NONE',  ( 7.250000000000005329, -8.249999999999998224, -25.50000000000000355 ) ) ;
#59464=VECTOR ( 'NONE', #62279, 1000.000000000000000 ) ;
#59466=VECTOR ( 'NONE', #58962, 1000.000000000000000 ) ;
#59509=CIRCLE ( 'NONE', #18808, 1.000000000000000000 ) ;
#59526=VECTOR ( 'NONE', #38466, 1000.000000000000000 ) ;
#59540=DIRECTION ( 'NONE',  ( -0.000000000000000000, -0.000000000000000000, 1.000000000000000000 ) ) ;
#59543=EDGE_CURVE ( 'NONE', #57065, #18717, #30788, .T. ) ;
#59546=ORIENTED_EDGE ( 'NONE', *, *, #26705, .F. ) ;
#59547=DIRECTION ( 'NONE',  ( -0.000000000000000000, -0.000000000000000000, 1.000000000000000000 ) ) ;
#59548=DIRECTION ( 'NONE',  ( -0.000000000000000000, -0.000000000000000000, -1.000000000000000000 ) ) ;
#59549=ORIENTED_EDGE ( 'NONE', *, *, #1282, .T. ) ;
#59556=DIRECTION ( 'NONE',  ( -0.000000000000000000, -0.000000000000000000, 1.000000000000000000 ) ) ;
#59557=VERTEX_POINT ( 'NONE', #30440 ) ;
#59573=DIRECTION ( 'NONE',  ( 0.000000000000000000, 0.000000000000000000, -1.000000000000000000 ) ) ;
#59575=AXIS2_PLACEMENT_3D ( 'NONE', #20727, #52933, #62446 ) ;
#59576=ORIENTED_EDGE ( 'NONE', *, *, #60777, .F. ) ;
#59582=VERTEX_POINT ( 'NONE', #62250 ) ;
#59589=CARTESIAN_POINT ( 'NONE',  ( -7.250000000000000888, 7.450000000000003730, -16.50000000000000000 ) ) ;
#59594=LINE ( 'NONE', #11144, #56589 ) ;
#59595=ADVANCED_FACE ( 'NONE', ( #41738 ), #63316, .F. ) ;
#59606=AXIS2_PLACEMENT_3D ( 'NONE', #12095, #37948, #826 ) ;
#59608=DIRECTION ( 'NONE',  ( 0.000000000000000000, -1.000000000000000000, 0.000000000000000000 ) ) ;
#59613=CIRCLE ( 'NONE', #41537, 1.000000000000000000 ) ;
#59616=EDGE_CURVE ( 'NONE', #12839, #39380, #69318, .T. ) ;
#59621=PLANE ( 'NONE',  #17594 ) ;
#59626=PLANE ( 'NONE',  #42547 ) ;
#59627=DIRECTION ( 'NONE',  ( 0.000000000000000000, 0.000000000000000000, 1.000000000000000000 ) ) ;
#59634=CARTESIAN_POINT ( 'NONE',  ( 7.250000000000005329, -7.449999999999998401, -19.50000000000000000 ) ) ;
#59644=CARTESIAN_POINT ( 'NONE',  ( 0.000000000000000000, 0.000000000000000000, -9.000000000000001776 ) ) ;
#59645=EDGE_CURVE ( 'NONE', #36435, #32668, #69681, .T. ) ;
#59646=EDGE_LOOP ( 'NONE', ( #67106, #44346, #62411, #10342 ) ) ;
#59650=ORIENTED_EDGE ( 'NONE', *, *, #13033, .F. ) ;
#59651=DIRECTION ( 'NONE',  ( -1.000000000000000000, 0.000000000000000000, 0.000000000000000000 ) ) ;
#59668=ORIENTED_EDGE ( 'NONE', *, *, #32909, .T. ) ;
#59677=FACE_OUTER_BOUND ( 'NONE', #17976, .T. ) ;
#59681=ADVANCED_FACE ( 'NONE', ( #22282, #43832 ), #357, .F. ) ;
#59693=AXIS2_PLACEMENT_3D ( 'NONE', #53317, #15484, #4868 ) ;
#59700=ORIENTED_EDGE ( 'NONE', *, *, #38049, .T. ) ;
#59704=AXIS2_PLACEMENT_3D ( 'NONE', #57772, #52847, #8273 ) ;
#59706=EDGE_LOOP ( 'NONE', ( #39042, #45850, #56540, #37011 ) ) ;
#59708=CARTESIAN_POINT ( 'NONE',  ( 8.250000000000005329, 7.250000000000000888, -24.50000000000000000 ) ) ;
#59715=EDGE_CURVE ( 'NONE', #68411, #61023, #32200, .T. ) ;
#59718=ORIENTED_EDGE ( 'NONE', *, *, #34956, .T. ) ;
#59719=CARTESIAN_POINT ( 'NONE',  ( -7.250000000000000888, 7.250000000000001776, -18.50000000000000000 ) ) ;
#59722=ORIENTED_EDGE ( 'NONE', *, *, #53456, .T. ) ;
#59730=ADVANCED_FACE ( 'NONE', ( #7719 ), #12319, .F. ) ;
#59734=ORIENTED_EDGE ( 'NONE', *, *, #12454, .F. ) ;
#59736=CARTESIAN_POINT ( 'NONE',  ( 0.000000000000000000, 0.000000000000000000, -5.000000000000000000 ) ) ;
#59742=CARTESIAN_POINT ( 'NONE',  ( -8.250000000000001776, 0.000000000000000000, -9.500000000000001776 ) ) ;
#59748=EDGE_LOOP ( 'NONE', ( #39602, #41015, #64979, #47149, #64084, #14057, #3442, #26610 ) ) ;
#59749=VECTOR ( 'NONE', #54621, 1000.000000000000000 ) ;
#59754=ORIENTED_EDGE ( 'NONE', *, *, #24209, .F. ) ;
#59760=CARTESIAN_POINT ( 'NONE',  ( 8.250000000000005329, 7.250000000000000888, -26.00000000000001066 ) ) ;
#59762=DIRECTION ( 'NONE',  ( -1.000000000000000000, 0.000000000000000000, -0.000000000000000000 ) ) ;
#59775=AXIS2_PLACEMENT_3D ( 'NONE', #49174, #1415, #54828 ) ;
#59776=CARTESIAN_POINT ( 'NONE',  ( 7.450000000000003730, -7.249999999999997335, -21.50000000000000000 ) ) ;
#59778=DIRECTION ( 'NONE',  ( -1.000000000000000000, 0.000000000000000000, 0.000000000000000000 ) ) ;
#59781=DIRECTION ( 'NONE',  ( 1.000000000000000000, -1.334402673828313093E-16, 0.000000000000000000 ) ) ;
#59782=FACE_OUTER_BOUND ( 'NONE', #13208, .T. ) ;
#59783=ORIENTED_EDGE ( 'NONE', *, *, #24177, .F. ) ;
#59796=PLANE ( 'NONE',  #30412 ) ;
#59803=DIRECTION ( 'NONE',  ( 1.000000000000000000, 0.000000000000000000, 0.000000000000000000 ) ) ;
#59805=ORIENTED_EDGE ( 'NONE', *, *, #35478, .T. ) ;
#59808=CARTESIAN_POINT ( 'NONE',  ( 0.000000000000000000, 8.250000000000001776, -17.00000000000000000 ) ) ;
#59810=DIRECTION ( 'NONE',  ( 0.000000000000000000, 1.000000000000000000, 0.000000000000000000 ) ) ;
#59811=CARTESIAN_POINT ( 'NONE',  ( -8.250000000000001776, 0.000000000000000000, -21.00000000000000000 ) ) ;
#59813=EDGE_CURVE ( 'NONE', #48587, #13221, #7026, .T. ) ;
#59818=EDGE_LOOP ( 'NONE', ( #11726, #56152, #14052, #7350 ) ) ;
#59820=PLANE ( 'NONE',  #38310 ) ;
#59823=LINE ( 'NONE', #11376, #29708 ) ;
#59825=VECTOR ( 'NONE', #23115, 1000.000000000000000 ) ;
#59827=FACE_OUTER_BOUND ( 'NONE', #45988, .T. ) ;
#59828=VERTEX_POINT ( 'NONE', #2079 ) ;
#59830=VERTEX_POINT ( 'NONE', #23635 ) ;
#59833=DIRECTION ( 'NONE',  ( 0.000000000000000000, 0.000000000000000000, 1.000000000000000000 ) ) ;
#59837=ORIENTED_EDGE ( 'NONE', *, *, #64493, .T. ) ;
#59838=EDGE_LOOP ( 'NONE', ( #38028, #62480, #13476, #36876 ) ) ;
#59841=LINE ( 'NONE', #11398, #23246 ) ;
#59856=EDGE_CURVE ( 'NONE', #32498, #52692, #18601, .T. ) ;
#59860=CARTESIAN_POINT ( 'NONE',  ( 8.250000000000005329, 8.250000000000001776, -26.00000000000001066 ) ) ;
#59868=LINE ( 'NONE', #10392, #25339 ) ;
#59881=CARTESIAN_POINT ( 'NONE',  ( -7.250000000000000000, -7.449999999999998401, -15.50000000000000000 ) ) ;
#59888=CARTESIAN_POINT ( 'NONE',  ( 0.000000000000000000, -8.249999999999998224, -23.50000000000000000 ) ) ;
#59898=PLANE ( 'NONE',  #23291 ) ;
#59904=CARTESIAN_POINT ( 'NONE',  ( 0.000000000000000000, 8.250000000000001776, -22.50000000000000000 ) ) ;
#59907=ORIENTED_EDGE ( 'NONE', *, *, #35254, .T. ) ;
#59915=CARTESIAN_POINT ( 'NONE',  ( -7.250000000000000888, -8.249999999999998224, -16.00000000000000000 ) ) ;
#59921=VECTOR ( 'NONE', #64544, 1000.000000000000000 ) ;
#59922=EDGE_LOOP ( 'NONE', ( #175, #36424, #29977, #66602 ) ) ;
#59926=LINE ( 'NONE', #33739, #38415 ) ;
#59928=CARTESIAN_POINT ( 'NONE',  ( -7.250000000000000888, 7.250000000000001776, -26.00000000000001066 ) ) ;
#59930=DIRECTION ( 'NONE',  ( -0.000000000000000000, -0.000000000000000000, 1.000000000000000000 ) ) ;
#59933=VERTEX_POINT ( 'NONE', #25398 ) ;
#59935=CIRCLE ( 'NONE', #24961, 1.000000000000000000 ) ;
#59937=PLANE ( 'NONE',  #51783 ) ;
#59950=DIRECTION ( 'NONE',  ( -1.000000000000000000, 0.000000000000000000, 0.000000000000000000 ) ) ;
#59959=CARTESIAN_POINT ( 'NONE',  ( 8.250000000000005329, 0.000000000000000000, -11.50000000000000000 ) ) ;
#59960=VECTOR ( 'NONE', #5946, 1000.000000000000000 ) ;
#59961=DIRECTION ( 'NONE',  ( 0.000000000000000000, 0.000000000000000000, -1.000000000000000000 ) ) ;
#59965=CARTESIAN_POINT ( 'NONE',  ( -7.250000000000000888, 7.450000000000003730, -19.50000000000000000 ) ) ;
#59967=CARTESIAN_POINT ( 'NONE',  ( -7.250000000000001776, -7.249999999999998224, -30.00000000000001066 ) ) ;
#59971=ORIENTED_EDGE ( 'NONE', *, *, #48565, .T. ) ;
#59974=CARTESIAN_POINT ( 'NONE',  ( 0.000000000000000000, 0.000000000000000000, -21.00000000000000000 ) ) ;
#59975=EDGE_LOOP ( 'NONE', ( #21273, #43906, #59546, #50378, #54046, #66045, #13558, #39973 ) ) ;
#59978=CARTESIAN_POINT ( 'NONE',  ( 7.250000000000005329, -7.249999999999998224, -11.00000000000000000 ) ) ;
#59990=ORIENTED_EDGE ( 'NONE', *, *, #54678, .F. ) ;
#60006=VERTEX_POINT ( 'NONE', #26805 ) ;
#60007=VECTOR ( 'NONE', #40734, 1000.000000000000000 ) ;
#60008=VERTEX_POINT ( 'NONE', #48014 ) ;
#60009=EDGE_CURVE ( 'NONE', #50215, #64072, #54029, .T. ) ;
#60015=FACE_OUTER_BOUND ( 'NONE', #59818, .T. ) ;
#60023=EDGE_CURVE ( 'NONE', #22866, #20587, #69501, .T. ) ;
#60024=DIRECTION ( 'NONE',  ( 0.000000000000000000, 0.000000000000000000, -1.000000000000000000 ) ) ;
#60026=EDGE_CURVE ( 'NONE', #16692, #26902, #10182, .T. ) ;
#60036=CARTESIAN_POINT ( 'NONE',  ( 8.250000000000005329, 0.000000000000000000, -15.50000000000000000 ) ) ;
#60051=CLOSED_SHELL ( 'NONE', ( #29780, #31332, #29021, #9702, #32197, #31505, #7415, #68303, #46439, #45056, #4803, #49291, #19876, #5084, #56726, #50963, #45762, #68277, #65329, #29726, #67234, #50867, #13247, #54602, #537, #40062, #50620, #808, #7511, #33321, #35508, #31018, #53895, #57748, #54388, #28516, #52697, #59317, #66411, #17209, #58137, #15110, #25433, #58790, #54667, #37230, #41022, #44763, #60354, #33433, #63212, #4722, #45906, #38744, #60671, #25906, #15409, #24762, #31086, #48271, #27364, #62029, #57880, #10087, #6212, #37883, #53975, #47908, #8619, #13823, #58720, #67813, #57563, #13334, #58867, #48805, #66800, #53060, #24714, #66449, #4336, #24511, #37398, #5102, #39610, #228, #57035, #63244, #48213, #9879, #51899, #34689, #65492, #54259, #8484, #47663, #9134, #41525, #14722, #15317, #61240, #19576, #58312, #34188, #44062, #15, #19557, #65212, #26397, #16295, #49537, #52215, #37266, #63092, #7750, #62753, #57517, #38277, #31460, #2291, #54452, #17113, #36249, #21176, #51991, #65446, #23124, #27369, #66516, #36348, #56797, #67778, #66794, #13309, #61294, #43530, #23343, #5696, #60916, #26437, #66973, #26926, #60199, #65955, #14229, #19567, #13601, #23219, #10916, #31550, #6084, #34507, #26091, #7295, #2367, #69885, #35204, #46472, #60318, #1216, #44439, #2091, #7288, #14079, #37556, #63835, #25006, #37187, #61876, #42818, #19515, #42886, #49741, #21353, #18529, #52340, #18881, #46658, #68689, #69872, #29922, #64974, #36014, #1273, #62885, #28181, #23309, #17966, #31162, #65260, #42618, #45023, #3829, #55862, #39857, #45292, #15847, #40068, #61373, #56528, #46473, #66829, #45952, #19436, #1358, #39606, #16383, #41053, #11659, #51984, #58633, #27892, #59595, #46478, #19725, #22840, #38500, #53363, #36604, #50450, #33342, #1168, #47208, #18757, #32032, #25160, #36117, #54991, #28272, #8162, #14691, #31481, #68690, #68716, #61303, #33000, #21585, #14390, #63983, #6339, #25462, #30789, #1306, #36656, #28443, #29231, #52845, #19017, #59730, #71, #57833, #61103, #53370, #50346, #4421, #16701, #38198, #26161, #28270, #18537, #30683, #31732, #47010, #48769, #55843, #4999, #10712, #10417, #27671, #35473, #4945, #63952, #22774, #63289, #53555, #21106, #12380, #49575, #69140, #27569, #57903, #44837, #22697, #64067, #435, #7429, #68816, #1684, #28023, #36002, #18993, #57173, #51259, #39530, #9349, #48566, #63521, #50404, #9869, #9240, #36834, #69979, #15599, #61143, #51920, #41854, #18446, #30400, #67718, #62529, #22834, #40955, #51455, #2027, #45346, #45599, #44570, #48413, #10753, #66018, #67750, #403, #63647, #20602, #65450, #55293, #57612, #17659, #1453, #49585, #57159, #69969, #29078, #65647, #27242, #12069, #56898, #1886, #66892, #45090, #67329, #59681, #3577, #49674, #11068, #69420, #33073, #2239, #54546, #58798, #54557, #42133, #22859, #12786, #43572, #52814, #5772, #47556, #43265, #61863, #2908, #58225, #17411, #38063, #272, #1774, #31342, #48652, #10650, #25975, #52206, #32692, #40127, #21516, #65632, #22567, #2292, #58184, #56330, #63968, #24213, #22994, #65202, #68072, #25877, #41361, #7897, #68270, #25840, #43056, #13937, #23042, #1754, #21345, #63985, #556, #10787, #42756, #27625 ) ) ;
#60052=CARTESIAN_POINT ( 'NONE',  ( 7.450000000000004619, -1.336933437520057563E-15, -15.50000000000000000 ) ) ;
#60053=DIRECTION ( 'NONE',  ( -1.000000000000000000, 0.000000000000000000, 0.000000000000000000 ) ) ;
#60060=DIRECTION ( 'NONE',  ( 0.000000000000000000, -1.000000000000000000, 0.000000000000000000 ) ) ;
#60072=EDGE_CURVE ( 'NONE', #65035, #55322, #69232, .T. ) ;
#60090=ORIENTED_EDGE ( 'NONE', *, *, #501, .F. ) ;
#60092=AXIS2_PLACEMENT_3D ( 'NONE', #24432, #66507, #13812 ) ;
#60099=DIRECTION ( 'NONE',  ( -1.000000000000000000, 0.000000000000000000, 0.000000000000000000 ) ) ;
#60104=LINE ( 'NONE', #61849, #15995 ) ;
#60109=VECTOR ( 'NONE', #43790, 1000.000000000000000 ) ;
#60121=ORIENTED_EDGE ( 'NONE', *, *, #60590, .T. ) ;
#60123=VERTEX_POINT ( 'NONE', #65662 ) ;
#60124=CARTESIAN_POINT ( 'NONE',  ( -7.250000000000000888, -8.249999999999998224, -25.00000000000000000 ) ) ;
#60127=CARTESIAN_POINT ( 'NONE',  ( 0.000000000000000000, 8.750000000000001776, -30.00000000000001066 ) ) ;
#60139=LINE ( 'NONE', #38250, #29355 ) ;
#60155=CARTESIAN_POINT ( 'NONE',  ( -8.250000000000001776, -8.249999999999998224, -26.00000000000001066 ) ) ;
#60158=VECTOR ( 'NONE', #62036, 1000.000000000000000 ) ;
#60159=FACE_OUTER_BOUND ( 'NONE', #65590, .T. ) ;
#60160=PLANE ( 'NONE',  #16271 ) ;
#60162=CIRCLE ( 'NONE', #52245, 1.000000000000000000 ) ;
#60163=VERTEX_POINT ( 'NONE', #22870 ) ;
#60166=EDGE_LOOP ( 'NONE', ( #52113, #22444, #12107, #13919, #21467, #61113, #5201, #15329 ) ) ;
#60186=CARTESIAN_POINT ( 'NONE',  ( 0.000000000000000000, 8.250000000000001776, -12.50000000000000000 ) ) ;
#60187=AXIS2_PLACEMENT_3D ( 'NONE', #19717, #18207, #66996 ) ;
#60188=DIRECTION ( 'NONE',  ( 0.000000000000000000, 0.000000000000000000, -1.000000000000000000 ) ) ;
#60199=ADVANCED_FACE ( 'NONE', ( #16880 ), #27482, .F. ) ;
#60212=ORIENTED_EDGE ( 'NONE', *, *, #50214, .F. ) ;
#60216=VECTOR ( 'NONE', #10817, 1000.000000000000000 ) ;
#60224=VERTEX_POINT ( 'NONE', #45730 ) ;
#60231=ORIENTED_EDGE ( 'NONE', *, *, #39904, .F. ) ;
#60233=ORIENTED_EDGE ( 'NONE', *, *, #33851, .T. ) ;
#60236=PLANE ( 'NONE',  #4805 ) ;
#60246=EDGE_LOOP ( 'NONE', ( #13774, #61011, #14956, #52967 ) ) ;
#60247=CARTESIAN_POINT ( 'NONE',  ( -7.250000000000000888, 7.250000000000001776, -16.00000000000000000 ) ) ;
#60249=DIRECTION ( 'NONE',  ( 1.000000000000000000, 0.000000000000000000, 0.000000000000000000 ) ) ;
#60252=VERTEX_POINT ( 'NONE', #14973 ) ;
#60256=ORIENTED_EDGE ( 'NONE', *, *, #30709, .F. ) ;
#60259=ORIENTED_EDGE ( 'NONE', *, *, #19215, .F. ) ;
#60287=DIRECTION ( 'NONE',  ( 1.000000000000000000, -0.000000000000000000, 0.000000000000000000 ) ) ;
#60296=LINE ( 'NONE', #38402, #25860 ) ;
#60300=AXIS2_PLACEMENT_3D ( 'NONE', #37836, #54100, #64029 ) ;
#60302=VERTEX_POINT ( 'NONE', #19562 ) ;
#60316=DIRECTION ( 'NONE',  ( 0.000000000000000000, 0.000000000000000000, -1.000000000000000000 ) ) ;
#60317=ORIENTED_EDGE ( 'NONE', *, *, #52267, .T. ) ;
#60318=ADVANCED_FACE ( 'NONE', ( #9674 ), #20966, .F. ) ;
#60327=ORIENTED_EDGE ( 'NONE', *, *, #49266, .T. ) ;
#60328=ORIENTED_EDGE ( 'NONE', *, *, #57807, .T. ) ;
#60330=CARTESIAN_POINT ( 'NONE',  ( -7.250000000000001776, -7.249999999999998224, -12.50000000000000000 ) ) ;
#60334=EDGE_LOOP ( 'NONE', ( #6922, #39701, #8003, #46664, #42778, #35179, #68310, #15566 ) ) ;
#60336=EDGE_CURVE ( 'NONE', #2927, #44960, #53172, .T. ) ;
#60341=VECTOR ( 'NONE', #34818, 1000.000000000000000 ) ;
#60350=EDGE_CURVE ( 'NONE', #46964, #42683, #69058, .T. ) ;
#60354=ADVANCED_FACE ( 'NONE', ( #42537 ), #20611, .F. ) ;
#60358=EDGE_LOOP ( 'NONE', ( #2047, #24898, #36148, #54247 ) ) ;
#60359=VECTOR ( 'NONE', #60416, 1000.000000000000000 ) ;
#60360=DIRECTION ( 'NONE',  ( -5.981805089575196197E-17, -1.000000000000000000, 0.000000000000000000 ) ) ;
#60368=DIRECTION ( 'NONE',  ( 1.000000000000000000, -5.981805089575196197E-17, 0.000000000000000000 ) ) ;
#60380=EDGE_CURVE ( 'NONE', #17866, #9016, #14613, .T. ) ;
#60388=LINE ( 'NONE', #16930, #43307 ) ;
#60395=ORIENTED_EDGE ( 'NONE', *, *, #22383, .F. ) ;
#60406=VERTEX_POINT ( 'NONE', #65835 ) ;
#60409=DIRECTION ( 'NONE',  ( 0.000000000000000000, -0.000000000000000000, 1.000000000000000000 ) ) ;
#60413=ORIENTED_EDGE ( 'NONE', *, *, #2413, .F. ) ;
#60416=DIRECTION ( 'NONE',  ( 0.000000000000000000, 0.000000000000000000, 1.000000000000000000 ) ) ;
#60433=VECTOR ( 'NONE', #5809, 1000.000000000000000 ) ;
#60434=EDGE_CURVE ( 'NONE', #25825, #35692, #59841, .T. ) ;
#60437=CARTESIAN_POINT ( 'NONE',  ( 7.250000000000004441, 7.450000000000001954, -13.50000000000000178 ) ) ;
#60439=CIRCLE ( 'NONE', #31264, 1.000000000000000000 ) ;
#60445=VECTOR ( 'NONE', #4536, 1000.000000000000000 ) ;
#60456=DIRECTION ( 'NONE',  ( -1.000000000000000000, 0.000000000000000000, 0.000000000000000000 ) ) ;
#60480=FACE_OUTER_BOUND ( 'NONE', #16368, .T. ) ;
#60490=EDGE_CURVE ( 'NONE', #28651, #36435, #6301, .T. ) ;
#60514=ORIENTED_EDGE ( 'NONE', *, *, #1288, .F. ) ;
#60518=EDGE_CURVE ( 'NONE', #39018, #66073, #55574, .T. ) ;
#60537=ORIENTED_EDGE ( 'NONE', *, *, #57617, .T. ) ;
#60538=VERTEX_POINT ( 'NONE', #12082 ) ;
#60549=CARTESIAN_POINT ( 'NONE',  ( 10.50000000000000178, 9.690000000000001279, 0.000000000000000000 ) ) ;
#60573=DIRECTION ( 'NONE',  ( 0.000000000000000000, 1.000000000000000000, 0.000000000000000000 ) ) ;
#60574=LINE ( 'NONE', #66233, #16178 ) ;
#60581=FACE_OUTER_BOUND ( 'NONE', #34683, .T. ) ;
#60590=EDGE_CURVE ( 'NONE', #54499, #63139, #15348, .T. ) ;
#60593=AXIS2_PLACEMENT_3D ( 'NONE', #63037, #30859, #14592 ) ;
#60610=ORIENTED_EDGE ( 'NONE', *, *, #23485, .F. ) ;
#60614=AXIS2_PLACEMENT_3D ( 'NONE', #3048, #31335, #52902 ) ;
#60631=ORIENTED_EDGE ( 'NONE', *, *, #58515, .T. ) ;
#60636=VECTOR ( 'NONE', #25090, 1000.000000000000000 ) ;
#60640=EDGE_CURVE ( 'NONE', #47184, #55467, #26656, .T. ) ;
#60647=AXIS2_PLACEMENT_3D ( 'NONE', #12604, #18613, #34521 ) ;
#60656=DIRECTION ( 'NONE',  ( 0.000000000000000000, 0.000000000000000000, -1.000000000000000000 ) ) ;
#60660=CARTESIAN_POINT ( 'NONE',  ( 9.689999999999999503, -10.50000000000000178, 0.000000000000000000 ) ) ;
#60664=CARTESIAN_POINT ( 'NONE',  ( -8.250000000000001776, 0.000000000000000000, -15.50000000000000000 ) ) ;
#60668=CARTESIAN_POINT ( 'NONE',  ( 9.690000000000001279, 9.750000000000000000, -4.250000000000000000 ) ) ;
#60670=VECTOR ( 'NONE', #1082, 1000.000000000000000 ) ;
#60671=ADVANCED_FACE ( 'NONE', ( #29733 ), #30448, .T. ) ;
#60673=CARTESIAN_POINT ( 'NONE',  ( -7.250000000000001776, -7.249999999999998224, -16.00000000000000000 ) ) ;
#60674=ORIENTED_EDGE ( 'NONE', *, *, #52524, .T. ) ;
#60690=DIRECTION ( 'NONE',  ( 1.000000000000000000, 0.000000000000000000, 0.000000000000000000 ) ) ;
#60691=VERTEX_POINT ( 'NONE', #9580 ) ;
#60694=AXIS2_PLACEMENT_3D ( 'NONE', #20109, #4211, #14459 ) ;
#60699=LINE ( 'NONE', #13298, #65407 ) ;
#60711=AXIS2_PLACEMENT_3D ( 'NONE', #44794, #12610, #12262 ) ;
#60737=DIRECTION ( 'NONE',  ( -1.000000000000000000, 0.000000000000000000, 0.000000000000000000 ) ) ;
#60738=DIRECTION ( 'NONE',  ( 1.334402673828312846E-16, 1.000000000000000000, 0.000000000000000000 ) ) ;
#60740=CARTESIAN_POINT ( 'NONE',  ( 7.450000000000004619, -1.336933437520057563E-15, -11.00000000000000000 ) ) ;
#60741=CARTESIAN_POINT ( 'NONE',  ( 9.690000000000001279, 8.750000000000000000, -7.000000000000000000 ) ) ;
#60742=ORIENTED_EDGE ( 'NONE', *, *, #12930, .T. ) ;
#60745=VERTEX_POINT ( 'NONE', #19828 ) ;
#60769=CARTESIAN_POINT ( 'NONE',  ( 0.000000000000000000, 0.000000000000000000, -19.00000000000000000 ) ) ;
#60770=ORIENTED_EDGE ( 'NONE', *, *, #6103, .T. ) ;
#60777=EDGE_CURVE ( 'NONE', #16435, #28094, #32309, .T. ) ;
#60783=ORIENTED_EDGE ( 'NONE', *, *, #41904, .T. ) ;
#60791=CIRCLE ( 'NONE', #40504, 0.2000000000000005107 ) ;
#60797=ORIENTED_EDGE ( 'NONE', *, *, #6885, .T. ) ;
#60799=CIRCLE ( 'NONE', #44997, 0.9999999999999991118 ) ;
#60809=DIRECTION ( 'NONE',  ( 0.000000000000000000, 1.000000000000000000, 0.000000000000000000 ) ) ;
#60811=CARTESIAN_POINT ( 'NONE',  ( 6.749999999999996447, -7.348062532928000934, 0.000000000000000000 ) ) ;
#60813=EDGE_CURVE ( 'NONE', #7192, #33956, #68388, .T. ) ;
#60815=DIRECTION ( 'NONE',  ( 0.000000000000000000, 0.000000000000000000, 1.000000000000000000 ) ) ;
#60816=DIRECTION ( 'NONE',  ( 0.000000000000000000, -1.000000000000000000, 0.000000000000000000 ) ) ;
#60821=EDGE_CURVE ( 'NONE', #10719, #50834, #31163, .T. ) ;
#60844=AXIS2_PLACEMENT_3D ( 'NONE', #32995, #4402, #48226 ) ;
#60849=CARTESIAN_POINT ( 'NONE',  ( 9.690000000000001279, -9.750000000000001776, -7.000000000000000000 ) ) ;
#60851=ORIENTED_EDGE ( 'NONE', *, *, #66650, .F. ) ;
#60853=CIRCLE ( 'NONE', #26012, 0.1999999999999996503 ) ;
#60862=ORIENTED_EDGE ( 'NONE', *, *, #5396, .F. ) ;
#60864=DIRECTION ( 'NONE',  ( -0.000000000000000000, -0.000000000000000000, 1.000000000000000000 ) ) ;
#60867=EDGE_LOOP ( 'NONE', ( #25661, #22013, #57286, #1698, #41634, #67632, #42964, #14700 ) ) ;
#60868=ORIENTED_EDGE ( 'NONE', *, *, #8705, .F. ) ;
#60869=FACE_OUTER_BOUND ( 'NONE', #66866, .T. ) ;
#60872=CARTESIAN_POINT ( 'NONE',  ( 8.250000000000005329, -7.249999999999998224, -26.00000000000001066 ) ) ;
#60873=ORIENTED_EDGE ( 'NONE', *, *, #50905, .T. ) ;
#60879=DIRECTION ( 'NONE',  ( 0.000000000000000000, 0.000000000000000000, -1.000000000000000000 ) ) ;
#60882=CARTESIAN_POINT ( 'NONE',  ( 7.450000000000004619, -1.336933437520057563E-15, -8.500000000000000000 ) ) ;
#60902=DIRECTION ( 'NONE',  ( -1.000000000000000000, 0.000000000000000000, 0.000000000000000000 ) ) ;
#60903=VECTOR ( 'NONE', #54245, 1000.000000000000000 ) ;
#60910=EDGE_CURVE ( 'NONE', #42070, #34855, #723, .T. ) ;
#60912=AXIS2_PLACEMENT_3D ( 'NONE', #4874, #15825, #69917 ) ;
#60916=ADVANCED_FACE ( 'NONE', ( #48455 ), #48807, .F. ) ;
#60919=ORIENTED_EDGE ( 'NONE', *, *, #53131, .F. ) ;
#60920=CARTESIAN_POINT ( 'NONE',  ( 7.450000000000004619, -1.336933437520057563E-15, -14.00000000000000000 ) ) ;
#60939=DIRECTION ( 'NONE',  ( -1.000000000000000000, 0.000000000000000000, 0.000000000000000000 ) ) ;
#60941=VECTOR ( 'NONE', #55781, 1000.000000000000000 ) ;
#60950=ORIENTED_EDGE ( 'NONE', *, *, #2596, .F. ) ;
#60957=FACE_OUTER_BOUND ( 'NONE', #11807, .T. ) ;
#60959=VECTOR ( 'NONE', #26649, 1000.000000000000000 ) ;
#60961=DIRECTION ( 'NONE',  ( 1.000000000000000000, 0.000000000000000000, 0.000000000000000000 ) ) ;
#60963=CARTESIAN_POINT ( 'NONE',  ( -8.250000000000001776, -7.249999999999998224, -22.50000000000000000 ) ) ;
#60967=CARTESIAN_POINT ( 'NONE',  ( 0.000000000000000000, 8.250000000000001776, -24.00000000000000000 ) ) ;
#60983=CARTESIAN_POINT ( 'NONE',  ( 7.250000000000005329, -7.249999999999998224, -26.00000000000001066 ) ) ;
#60986=CARTESIAN_POINT ( 'NONE',  ( -7.250000000000000888, 8.250000000000001776, -17.00000000000000000 ) ) ;
#60991=DIRECTION ( 'NONE',  ( 1.000000000000000000, 0.000000000000000000, 0.000000000000000000 ) ) ;
#61000=ORIENTED_EDGE ( 'NONE', *, *, #45672, .F. ) ;
#61002=CARTESIAN_POINT ( 'NONE',  ( 4.456444791733522252E-16, 7.450000000000002842, -22.00000000000000000 ) ) ;
#61011=ORIENTED_EDGE ( 'NONE', *, *, #10184, .F. ) ;
#61013=PLANE ( 'NONE',  #18444 ) ;
#61023=VERTEX_POINT ( 'NONE', #22960 ) ;
#61024=ORIENTED_EDGE ( 'NONE', *, *, #39260, .T. ) ;
#61038=CARTESIAN_POINT ( 'NONE',  ( 7.250000000000005329, -8.249999999999998224, -9.500000000000001776 ) ) ;
#61044=CYLINDRICAL_SURFACE ( 'NONE', #58457, 1.000000000000000000 ) ;
#61047=VERTEX_POINT ( 'NONE', #28958 ) ;
#61050=PLANE ( 'NONE',  #69783 ) ;
#61052=EDGE_CURVE ( 'NONE', #50228, #31960, #22625, .T. ) ;
#61058=EDGE_CURVE ( 'NONE', #33875, #6182, #58298, .T. ) ;
#61060=LINE ( 'NONE', #34183, #31175 ) ;
#61070=ORIENTED_EDGE ( 'NONE', *, *, #35697, .F. ) ;
#61072=DIRECTION ( 'NONE',  ( -1.794541526872559352E-16, -1.000000000000000000, 0.000000000000000000 ) ) ;
#61073=DIRECTION ( 'NONE',  ( -0.000000000000000000, -0.000000000000000000, 1.000000000000000000 ) ) ;
#61077=ORIENTED_EDGE ( 'NONE', *, *, #41158, .T. ) ;
#61078=CARTESIAN_POINT ( 'NONE',  ( -8.250000000000001776, 0.000000000000000000, -8.000000000000000000 ) ) ;
#61083=AXIS2_PLACEMENT_3D ( 'NONE', #68929, #15192, #36762 ) ;
#61084=DIRECTION ( 'NONE',  ( 1.000000000000000000, 0.000000000000000000, 0.000000000000000000 ) ) ;
#61090=ORIENTED_EDGE ( 'NONE', *, *, #21737, .T. ) ;
#61096=CARTESIAN_POINT ( 'NONE',  ( 0.000000000000000000, -7.449999999999998401, -25.00000000000000000 ) ) ;
#61099=EDGE_LOOP ( 'NONE', ( #41211, #11470, #39439, #26108 ) ) ;
#61103=ADVANCED_FACE ( 'NONE', ( #23996, #35287 ), #30362, .F. ) ;
#61113=ORIENTED_EDGE ( 'NONE', *, *, #11588, .T. ) ;
#61119=DIRECTION ( 'NONE',  ( 0.000000000000000000, 0.000000000000000000, 1.000000000000000000 ) ) ;
#61121=CARTESIAN_POINT ( 'NONE',  ( 8.250000000000005329, -7.249999999999998224, -12.00000000000000000 ) ) ;
#61122=DIRECTION ( 'NONE',  ( 0.000000000000000000, 0.000000000000000000, -1.000000000000000000 ) ) ;
#61125=ORIENTED_EDGE ( 'NONE', *, *, #48561, .F. ) ;
#61133=CARTESIAN_POINT ( 'NONE',  ( -7.250000000000001776, -7.249999999999998224, -9.000000000000001776 ) ) ;
#61138=DIRECTION ( 'NONE',  ( 0.000000000000000000, 0.000000000000000000, 1.000000000000000000 ) ) ;
#61141=CARTESIAN_POINT ( 'NONE',  ( 7.450000000000004619, -1.336933437520057563E-15, -9.500000000000001776 ) ) ;
#61142=AXIS2_PLACEMENT_3D ( 'NONE', #68246, #36065, #57637 ) ;
#61143=ADVANCED_FACE ( 'NONE', ( #29648 ), #2780, .T. ) ;
#61152=EDGE_CURVE ( 'NONE', #49332, #21330, #45924, .T. ) ;
#61153=ORIENTED_EDGE ( 'NONE', *, *, #63559, .T. ) ;
#61156=VERTEX_POINT ( 'NONE', #24705 ) ;
#61162=LINE ( 'NONE', #16681, #47396 ) ;
#61168=ORIENTED_EDGE ( 'NONE', *, *, #21922, .T. ) ;
#61180=CARTESIAN_POINT ( 'NONE',  ( -7.250000000000000888, 7.250000000000001776, -14.50000000000000000 ) ) ;
#61185=EDGE_LOOP ( 'NONE', ( #33019, #20485, #22350, #37890 ) ) ;
#61186=LINE ( 'NONE', #60849, #2497 ) ;
#61200=EDGE_CURVE ( 'NONE', #31506, #20448, #3496, .T. ) ;
#61203=ORIENTED_EDGE ( 'NONE', *, *, #18107, .F. ) ;
#61214=CARTESIAN_POINT ( 'NONE',  ( 7.250000000000005329, 7.250000000000000888, -14.00000000000000000 ) ) ;
#61217=CARTESIAN_POINT ( 'NONE',  ( -7.250000000000000888, 7.250000000000001776, -12.00000000000000000 ) ) ;
#61219=CARTESIAN_POINT ( 'NONE',  ( -7.450000000000001954, 7.250000000000000000, -7.500000000000000000 ) ) ;
#61225=DIRECTION ( 'NONE',  ( 0.000000000000000000, 0.000000000000000000, 1.000000000000000000 ) ) ;
#61230=CARTESIAN_POINT ( 'NONE',  ( 0.000000000000000000, 8.250000000000001776, -9.000000000000001776 ) ) ;
#61240=ADVANCED_FACE ( 'NONE', ( #48023 ), #21841, .F. ) ;
#61245=ORIENTED_EDGE ( 'NONE', *, *, #40947, .F. ) ;
#61258=ORIENTED_EDGE ( 'NONE', *, *, #19390, .T. ) ;
#61264=PLANE ( 'NONE',  #11584 ) ;
#61275=CARTESIAN_POINT ( 'NONE',  ( 0.000000000000000000, 8.250000000000001776, -15.00000000000000000 ) ) ;
#61277=VERTEX_POINT ( 'NONE', #37079 ) ;
#61281=ORIENTED_EDGE ( 'NONE', *, *, #2982, .F. ) ;
#61286=DIRECTION ( 'NONE',  ( -1.000000000000000000, 0.000000000000000000, 0.000000000000000000 ) ) ;
#61294=ADVANCED_FACE ( 'NONE', ( #59677 ), #11226, .T. ) ;
#61300=AXIS2_PLACEMENT_3D ( 'NONE', #51537, #3100, #46217 ) ;
#61303=ADVANCED_FACE ( 'NONE', ( #48719, #279 ), #64291, .T. ) ;
#61308=VECTOR ( 'NONE', #23238, 1000.000000000000000 ) ;
#61312=CARTESIAN_POINT ( 'NONE',  ( 0.000000000000000000, -7.449999999999998401, -16.50000000000000000 ) ) ;
#61313=VECTOR ( 'NONE', #1397, 1000.000000000000000 ) ;
#61318=EDGE_CURVE ( 'NONE', #17506, #64534, #64376, .T. ) ;
#61320=LINE ( 'NONE', #12875, #41588 ) ;
#61324=CIRCLE ( 'NONE', #57971, 0.1999999999999996503 ) ;
#61325=EDGE_CURVE ( 'NONE', #22300, #56770, #21583, .T. ) ;
#61338=CARTESIAN_POINT ( 'NONE',  ( 7.250000000000005329, -7.249999999999998224, -17.50000000000000000 ) ) ;
#61340=FACE_OUTER_BOUND ( 'NONE', #42965, .T. ) ;
#61341=ORIENTED_EDGE ( 'NONE', *, *, #24085, .T. ) ;
#61346=LINE ( 'NONE', #61002, #50743 ) ;
#61369=EDGE_CURVE ( 'NONE', #34713, #17836, #38542, .T. ) ;
#61372=DIRECTION ( 'NONE',  ( 0.000000000000000000, 1.000000000000000000, 0.000000000000000000 ) ) ;
#61373=ADVANCED_FACE ( 'NONE', ( #11309, #37847 ), #69322, .T. ) ;
#61374=DIRECTION ( 'NONE',  ( 0.000000000000000000, 0.000000000000000000, 1.000000000000000000 ) ) ;
#61377=CARTESIAN_POINT ( 'NONE',  ( -7.250000000000000000, -7.449999999999998401, -8.500000000000000000 ) ) ;
#61401=FACE_OUTER_BOUND ( 'NONE', #63427, .T. ) ;
#61409=CIRCLE ( 'NONE', #46746, 0.9999999999999991118 ) ;
#61415=DIRECTION ( 'NONE',  ( 0.000000000000000000, 0.000000000000000000, 1.000000000000000000 ) ) ;
#61416=FACE_OUTER_BOUND ( 'NONE', #16931, .T. ) ;
#61419=DIRECTION ( 'NONE',  ( -1.000000000000000000, 0.000000000000000000, 0.000000000000000000 ) ) ;
#61433=EDGE_LOOP ( 'NONE', ( #43692, #48141, #52901, #43233 ) ) ;
#61434=EDGE_LOOP ( 'NONE', ( #4558, #13964, #38936, #47424 ) ) ;
#61435=EDGE_CURVE ( 'NONE', #48126, #42371, #36912, .T. ) ;
#61437=CYLINDRICAL_SURFACE ( 'NONE', #20086, 1.000000000000000000 ) ;
#61443=FACE_OUTER_BOUND ( 'NONE', #67287, .T. ) ;
#61449=ORIENTED_EDGE ( 'NONE', *, *, #12636, .T. ) ;
#61452=EDGE_CURVE ( 'NONE', #13815, #25255, #33228, .T. ) ;
#61464=VERTEX_POINT ( 'NONE', #44866 ) ;
#61470=FACE_OUTER_BOUND ( 'NONE', #51377, .T. ) ;
#61474=CARTESIAN_POINT ( 'NONE',  ( -7.250000000000000000, -7.449999999999998401, -10.50000000000000000 ) ) ;
#61477=ORIENTED_EDGE ( 'NONE', *, *, #21421, .F. ) ;
#61479=ORIENTED_EDGE ( 'NONE', *, *, #5361, .T. ) ;
#61508=CARTESIAN_POINT ( 'NONE',  ( -7.450000000000001954, -7.249999999999998224, -23.50000000000000000 ) ) ;
#61537=ORIENTED_EDGE ( 'NONE', *, *, #34771, .T. ) ;
#61538=AXIS2_PLACEMENT_3D ( 'NONE', #53380, #53033, #43437 ) ;
#61545=EDGE_CURVE ( 'NONE', #42371, #50215, #2435, .T. ) ;
#61552=DIRECTION ( 'NONE',  ( 0.000000000000000000, 0.000000000000000000, -1.000000000000000000 ) ) ;
#61555=DIRECTION ( 'NONE',  ( -1.000000000000000000, 0.000000000000000000, 0.000000000000000000 ) ) ;
#61584=VERTEX_POINT ( 'NONE', #23995 ) ;
#61585=EDGE_CURVE ( 'NONE', #29173, #36079, #61840, .T. ) ;
#61586=ORIENTED_EDGE ( 'NONE', *, *, #17394, .F. ) ;
#61595=CARTESIAN_POINT ( 'NONE',  ( -7.450000000000001954, -7.249999999999998224, -25.00000000000000000 ) ) ;
#61600=DIRECTION ( 'NONE',  ( -0.000000000000000000, 0.000000000000000000, 1.000000000000000000 ) ) ;
#61601=VECTOR ( 'NONE', #66414, 1000.000000000000000 ) ;
#61602=AXIS2_PLACEMENT_3D ( 'NONE', #56250, #34671, #7794 ) ;
#61609=DIRECTION ( 'NONE',  ( 0.000000000000000000, 0.000000000000000000, -1.000000000000000000 ) ) ;
#61610=ORIENTED_EDGE ( 'NONE', *, *, #62648, .F. ) ;
#61614=EDGE_LOOP ( 'NONE', ( #53204, #67724, #898, #8650 ) ) ;
#61617=DIRECTION ( 'NONE',  ( 0.000000000000000000, 1.000000000000000000, 0.000000000000000000 ) ) ;
#61619=DIRECTION ( 'NONE',  ( 0.000000000000000000, 0.000000000000000000, 1.000000000000000000 ) ) ;
#61624=EDGE_LOOP ( 'NONE', ( #45793, #12784, #58434, #62169 ) ) ;
#61627=ORIENTED_EDGE ( 'NONE', *, *, #8385, .T. ) ;
#61630=CARTESIAN_POINT ( 'NONE',  ( -9.690000000000001279, -9.690000000000001279, 0.000000000000000000 ) ) ;
#61632=DIRECTION ( 'NONE',  ( 0.000000000000000000, 0.000000000000000000, -1.000000000000000000 ) ) ;
#61646=ORIENTED_EDGE ( 'NONE', *, *, #34820, .T. ) ;
#61648=CARTESIAN_POINT ( 'NONE',  ( 7.450000000000003730, -7.249999999999997335, -22.00000000000000000 ) ) ;
#61649=EDGE_CURVE ( 'NONE', #47806, #34716, #65173, .T. ) ;
#61652=EDGE_CURVE ( 'NONE', #25093, #58003, #56106, .T. ) ;
#61655=CIRCLE ( 'NONE', #58296, 0.2000000000000005107 ) ;
#61657=AXIS2_PLACEMENT_3D ( 'NONE', #11310, #27, #37161 ) ;
#61663=CIRCLE ( 'NONE', #9754, 0.2000000000000005107 ) ;
#61669=VECTOR ( 'NONE', #26368, 1000.000000000000000 ) ;
#61671=LINE ( 'NONE', #34795, #38267 ) ;
#61673=CARTESIAN_POINT ( 'NONE',  ( 7.450000000000003730, -7.249999999999997335, -16.50000000000000000 ) ) ;
#61674=EDGE_CURVE ( 'NONE', #32938, #42459, #63513, .T. ) ;
#61680=ORIENTED_EDGE ( 'NONE', *, *, #49001, .T. ) ;
#61682=LINE ( 'NONE', #13248, #55925 ) ;
#61688=CARTESIAN_POINT ( 'NONE',  ( -8.250000000000001776, -8.249999999999998224, -26.00000000000001066 ) ) ;
#61689=LINE ( 'NONE', #2304, #39148 ) ;
#61690=LINE ( 'NONE', #19264, #13844 ) ;
#61701=CARTESIAN_POINT ( 'NONE',  ( 8.750000000000005329, 7.250000000000000888, -26.00000000000001066 ) ) ;
#61703=AXIS2_PLACEMENT_3D ( 'NONE', #52944, #59961, #55028 ) ;
#61707=CYLINDRICAL_SURFACE ( 'NONE', #50344, 1.000000000000000000 ) ;
#61726=VECTOR ( 'NONE', #46027, 1000.000000000000000 ) ;
#61729=ORIENTED_EDGE ( 'NONE', *, *, #6006, .T. ) ;
#61731=EDGE_CURVE ( 'NONE', #24148, #68045, #69851, .T. ) ;
#61741=FACE_OUTER_BOUND ( 'NONE', #7231, .T. ) ;
#61743=CIRCLE ( 'NONE', #19960, 0.1999999999999987899 ) ;
#61746=CIRCLE ( 'NONE', #34634, 0.9999999999999991118 ) ;
#61758=CARTESIAN_POINT ( 'NONE',  ( 7.250000000000005329, 8.250000000000001776, -16.00000000000000000 ) ) ;
#61762=DIRECTION ( 'NONE',  ( 1.000000000000000000, 0.000000000000000000, -0.000000000000000000 ) ) ;
#61766=FACE_OUTER_BOUND ( 'NONE', #30965, .T. ) ;
#61769=DIRECTION ( 'NONE',  ( -0.000000000000000000, -0.000000000000000000, 1.000000000000000000 ) ) ;
#61773=CARTESIAN_POINT ( 'NONE',  ( 8.250000000000005329, 0.000000000000000000, -12.00000000000000000 ) ) ;
#61779=EDGE_CURVE ( 'NONE', #47728, #10391, #6461, .T. ) ;
#61780=CARTESIAN_POINT ( 'NONE',  ( -7.250000000000001776, -7.249999999999998224, -26.00000000000001066 ) ) ;
#61784=DIRECTION ( 'NONE',  ( 0.000000000000000000, -0.000000000000000000, 1.000000000000000000 ) ) ;
#61787=CARTESIAN_POINT ( 'NONE',  ( -7.250000000000000888, 8.250000000000001776, -23.50000000000000000 ) ) ;
#61794=ORIENTED_EDGE ( 'NONE', *, *, #67992, .F. ) ;
#61799=CARTESIAN_POINT ( 'NONE',  ( -7.450000000000001954, -7.249999999999998224, -23.50000000000000000 ) ) ;
#61810=DIRECTION ( 'NONE',  ( 0.000000000000000000, 0.000000000000000000, 1.000000000000000000 ) ) ;
#61818=CARTESIAN_POINT ( 'NONE',  ( 7.250000000000005329, -7.249999999999998224, -17.00000000000000000 ) ) ;
#61821=DIRECTION ( 'NONE',  ( 1.000000000000000000, 0.000000000000000000, 0.000000000000000000 ) ) ;
#61826=ORIENTED_EDGE ( 'NONE', *, *, #34497, .T. ) ;
#61837=FACE_OUTER_BOUND ( 'NONE', #19108, .T. ) ;
#61840=LINE ( 'NONE', #17301, #1907 ) ;
#61844=DIRECTION ( 'NONE',  ( 1.000000000000000000, 0.000000000000000000, 0.000000000000000000 ) ) ;
#61847=PLANE ( 'NONE',  #25642 ) ;
#61849=CARTESIAN_POINT ( 'NONE',  ( 0.000000000000000000, -8.249999999999998224, -14.50000000000000000 ) ) ;
#61854=CARTESIAN_POINT ( 'NONE',  ( 8.250000000000005329, 0.000000000000000000, -22.00000000000000000 ) ) ;
#61859=DIRECTION ( 'NONE',  ( 1.000000000000000000, 0.000000000000000000, 0.000000000000000000 ) ) ;
#61863=ADVANCED_FACE ( 'NONE', ( #65258, #543 ), #49666, .F. ) ;
#61870=VECTOR ( 'NONE', #40506, 1000.000000000000000 ) ;
#61872=EDGE_LOOP ( 'NONE', ( #67177, #12491, #32339, #47740 ) ) ;
#61876=ADVANCED_FACE ( 'NONE', ( #17483 ), #23132, .F. ) ;
#61881=DIRECTION ( 'NONE',  ( 0.000000000000000000, 0.000000000000000000, -1.000000000000000000 ) ) ;
#61882=CIRCLE ( 'NONE', #15625, 0.2000000000000005107 ) ;
#61896=DIRECTION ( 'NONE',  ( -1.000000000000000000, 2.602085213965213008E-15, 0.000000000000000000 ) ) ;
#61897=DIRECTION ( 'NONE',  ( -1.794541526872559352E-16, -1.000000000000000000, 0.000000000000000000 ) ) ;
#61900=CARTESIAN_POINT ( 'NONE',  ( 0.000000000000000000, -7.449999999999998401, -20.50000000000000000 ) ) ;
#61911=CYLINDRICAL_SURFACE ( 'NONE', #62032, 1.000000000000000000 ) ;
#61914=EDGE_CURVE ( 'NONE', #2063, #14714, #62932, .T. ) ;
#61920=CARTESIAN_POINT ( 'NONE',  ( -7.250000000000000888, 7.250000000000001776, -9.500000000000001776 ) ) ;
#61927=ORIENTED_EDGE ( 'NONE', *, *, #49921, .F. ) ;
#61930=CARTESIAN_POINT ( 'NONE',  ( 8.250000000000005329, -7.249999999999998224, -17.50000000000000000 ) ) ;
#61932=CARTESIAN_POINT ( 'NONE',  ( -8.250000000000001776, -7.249999999999998224, -18.00000000000000000 ) ) ;
#61937=CARTESIAN_POINT ( 'NONE',  ( -7.250000000000000888, 7.450000000000003730, -22.00000000000000000 ) ) ;
#61950=EDGE_CURVE ( 'NONE', #55879, #29528, #35132, .T. ) ;
#61954=DIRECTION ( 'NONE',  ( 0.000000000000000000, 0.000000000000000000, -1.000000000000000000 ) ) ;
#61957=CARTESIAN_POINT ( 'NONE',  ( 7.450000000000006395, 7.250000000000000888, -21.00000000000000000 ) ) ;
#61969=VERTEX_POINT ( 'NONE', #56710 ) ;
#61974=PLANE ( 'NONE',  #27002 ) ;
#61977=DIRECTION ( 'NONE',  ( 0.000000000000000000, 0.000000000000000000, -1.000000000000000000 ) ) ;
#61989=ORIENTED_EDGE ( 'NONE', *, *, #35801, .T. ) ;
#61991=EDGE_CURVE ( 'NONE', #39877, #8834, #34786, .T. ) ;
#61997=EDGE_CURVE ( 'NONE', #40124, #15934, #23492, .T. ) ;
#61999=VERTEX_POINT ( 'NONE', #24187 ) ;
#62005=DIRECTION ( 'NONE',  ( -1.794541526872559352E-16, -1.000000000000000000, 0.000000000000000000 ) ) ;
#62029=ADVANCED_FACE ( 'NONE', ( #24546 ), #1927, .F. ) ;
#62032=AXIS2_PLACEMENT_3D ( 'NONE', #67214, #18410, #34320 ) ;
#62036=DIRECTION ( 'NONE',  ( 0.000000000000000000, 0.000000000000000000, 1.000000000000000000 ) ) ;
#62042=DIRECTION ( 'NONE',  ( 1.000000000000000000, -0.000000000000000000, 0.000000000000000000 ) ) ;
#62047=ORIENTED_EDGE ( 'NONE', *, *, #67992, .T. ) ;
#62063=DIRECTION ( 'NONE',  ( -1.000000000000000000, 1.794541526872559352E-16, 0.000000000000000000 ) ) ;
#62064=CIRCLE ( 'NONE', #63247, 0.1999999999999987899 ) ;
#62065=DIRECTION ( 'NONE',  ( 0.000000000000000000, 0.000000000000000000, 1.000000000000000000 ) ) ;
#62066=DIRECTION ( 'NONE',  ( 1.000000000000000000, 0.000000000000000000, 0.000000000000000000 ) ) ;
#62072=ORIENTED_EDGE ( 'NONE', *, *, #24016, .T. ) ;
#62074=ORIENTED_EDGE ( 'NONE', *, *, #6885, .F. ) ;
#62091=CARTESIAN_POINT ( 'NONE',  ( 7.250000000000005329, 8.250000000000001776, -17.50000000000000000 ) ) ;
#62099=CARTESIAN_POINT ( 'NONE',  ( 0.000000000000000000, -7.449999999999998401, -25.50000000000000355 ) ) ;
#62101=EDGE_CURVE ( 'NONE', #9455, #20433, #47190, .T. ) ;
#62103=CARTESIAN_POINT ( 'NONE',  ( 0.000000000000000000, -7.449999999999998401, -10.00000000000000000 ) ) ;
#62115=CIRCLE ( 'NONE', #24893, 1.000000000000002665 ) ;
#62119=CARTESIAN_POINT ( 'NONE',  ( -7.250000000000000888, -8.249999999999998224, -16.50000000000000000 ) ) ;
#62121=DIRECTION ( 'NONE',  ( 0.000000000000000000, 0.000000000000000000, 1.000000000000000000 ) ) ;
#62127=VERTEX_POINT ( 'NONE', #30544 ) ;
#62128=EDGE_CURVE ( 'NONE', #23277, #28299, #40359, .T. ) ;
#62139=DIRECTION ( 'NONE',  ( -1.794541526872559352E-16, -1.000000000000000000, 0.000000000000000000 ) ) ;
#62151=ORIENTED_EDGE ( 'NONE', *, *, #62128, .T. ) ;
#62155=DIRECTION ( 'NONE',  ( 0.000000000000000000, 0.000000000000000000, 1.000000000000000000 ) ) ;
#62169=ORIENTED_EDGE ( 'NONE', *, *, #63697, .T. ) ;
#62190=CARTESIAN_POINT ( 'NONE',  ( 9.690000000000001279, -9.750000000000001776, -7.000000000000000000 ) ) ;
#62191=CARTESIAN_POINT ( 'NONE',  ( 7.250000000000005329, -7.249999999999998224, -18.50000000000000000 ) ) ;
#62194=EDGE_CURVE ( 'NONE', #51208, #29528, #67478, .T. ) ;
#62197=CARTESIAN_POINT ( 'NONE',  ( -7.250000000000000000, -7.449999999999998401, -14.00000000000000000 ) ) ;
#62201=VECTOR ( 'NONE', #8800, 1000.000000000000000 ) ;
#62210=VECTOR ( 'NONE', #28992, 1000.000000000000000 ) ;
#62212=ORIENTED_EDGE ( 'NONE', *, *, #36838, .F. ) ;
#62216=AXIS2_PLACEMENT_3D ( 'NONE', #43375, #4522, #47995 ) ;
#62217=DIRECTION ( 'NONE',  ( -8.951101527228104953E-17, 1.000000000000000000, -0.000000000000000000 ) ) ;
#62218=CARTESIAN_POINT ( 'NONE',  ( -7.250000000000000000, -7.449999999999998401, -21.00000000000000000 ) ) ;
#62224=LINE ( 'NONE', #36405, #53124 ) ;
#62226=ORIENTED_EDGE ( 'NONE', *, *, #68093, .T. ) ;
#62227=CARTESIAN_POINT ( 'NONE',  ( -7.250000000000000888, 7.250000000000001776, -13.00000000000000178 ) ) ;
#62234=ORIENTED_EDGE ( 'NONE', *, *, #7806, .T. ) ;
#62242=LINE ( 'NONE', #2844, #51479 ) ;
#62247=ORIENTED_EDGE ( 'NONE', *, *, #65686, .T. ) ;
#62250=CARTESIAN_POINT ( 'NONE',  ( -8.250000000000001776, 7.250000000000000888, -12.50000000000000000 ) ) ;
#62257=EDGE_CURVE ( 'NONE', #53573, #59150, #6110, .T. ) ;
#62275=DIRECTION ( 'NONE',  ( 0.000000000000000000, 1.000000000000000000, -0.000000000000000000 ) ) ;
#62279=DIRECTION ( 'NONE',  ( 0.000000000000000000, 0.000000000000000000, 1.000000000000000000 ) ) ;
#62283=ORIENTED_EDGE ( 'NONE', *, *, #36142, .T. ) ;
#62300=AXIS2_PLACEMENT_3D ( 'NONE', #40276, #34957, #27938 ) ;
#62301=DIRECTION ( 'NONE',  ( 0.000000000000000000, 0.000000000000000000, -1.000000000000000000 ) ) ;
#62305=EDGE_CURVE ( 'NONE', #63139, #38943, #38635, .T. ) ;
#62306=VERTEX_POINT ( 'NONE', #65175 ) ;
#62311=AXIS2_PLACEMENT_3D ( 'NONE', #2314, #29529, #23881 ) ;
#62323=CARTESIAN_POINT ( 'NONE',  ( 4.456444791733522252E-16, 7.450000000000002842, -9.500000000000001776 ) ) ;
#62335=ORIENTED_EDGE ( 'NONE', *, *, #40222, .F. ) ;
#62344=EDGE_CURVE ( 'NONE', #11392, #52946, #17802, .T. ) ;
#62355=EDGE_CURVE ( 'NONE', #6680, #62579, #50561, .T. ) ;
#62365=EDGE_LOOP ( 'NONE', ( #664, #48244 ) ) ;
#62374=DIRECTION ( 'NONE',  ( 0.000000000000000000, -1.000000000000000000, 0.000000000000000000 ) ) ;
#62382=EDGE_CURVE ( 'NONE', #35045, #46508, #39249, .T. ) ;
#62385=CARTESIAN_POINT ( 'NONE',  ( -7.250000000000000888, 7.250000000000001776, -24.50000000000000000 ) ) ;
#62401=EDGE_LOOP ( 'NONE', ( #43381, #4633, #32246, #56848, #25629, #45443, #17118, #49147 ) ) ;
#62406=DIRECTION ( 'NONE',  ( 0.000000000000000000, 0.000000000000000000, -1.000000000000000000 ) ) ;
#62409=CARTESIAN_POINT ( 'NONE',  ( 7.250000000000005329, 8.250000000000001776, -20.50000000000000000 ) ) ;
#62411=ORIENTED_EDGE ( 'NONE', *, *, #36591, .F. ) ;
#62412=ORIENTED_EDGE ( 'NONE', *, *, #20407, .T. ) ;
#62413=FACE_OUTER_BOUND ( 'NONE', #9559, .T. ) ;
#62422=EDGE_CURVE ( 'NONE', #24533, #21671, #53960, .T. ) ;
#62432=AXIS2_PLACEMENT_3D ( 'NONE', #33363, #16066, #10749 ) ;
#62446=DIRECTION ( 'NONE',  ( 1.000000000000000000, 0.000000000000000000, 0.000000000000000000 ) ) ;
#62457=DIRECTION ( 'NONE',  ( -0.000000000000000000, -0.000000000000000000, 1.000000000000000000 ) ) ;
#62460=VECTOR ( 'NONE', #49908, 1000.000000000000000 ) ;
#62463=ORIENTED_EDGE ( 'NONE', *, *, #27802, .T. ) ;
#62466=EDGE_CURVE ( 'NONE', #6379, #43564, #45649, .T. ) ;
#62478=EDGE_CURVE ( 'NONE', #67217, #44960, #50401, .T. ) ;
#62480=ORIENTED_EDGE ( 'NONE', *, *, #6976, .F. ) ;
#62483=CARTESIAN_POINT ( 'NONE',  ( 7.450000000000004619, -1.336933437520057563E-15, -15.50000000000000000 ) ) ;
#62492=VERTEX_POINT ( 'NONE', #7821 ) ;
#62493=CIRCLE ( 'NONE', #69289, 0.9999999999999991118 ) ;
#62496=CYLINDRICAL_SURFACE ( 'NONE', #23150, 0.1999999999999987899 ) ;
#62510=DIRECTION ( 'NONE',  ( -1.000000000000000000, 0.000000000000000000, 0.000000000000000000 ) ) ;
#62525=AXIS2_PLACEMENT_3D ( 'NONE', #66526, #33988, #66862 ) ;
#62529=ADVANCED_FACE ( 'NONE', ( #25512 ), #68286, .T. ) ;
#62538=DIRECTION ( 'NONE',  ( -1.000000000000000000, 0.000000000000000000, 0.000000000000000000 ) ) ;
#62557=PLANE ( 'NONE',  #42279 ) ;
#62570=CIRCLE ( 'NONE', #20848, 1.000000000000000000 ) ;
#62571=CARTESIAN_POINT ( 'NONE',  ( 7.250000000000004441, 7.450000000000001954, -19.50000000000000000 ) ) ;
#62572=AXIS2_PLACEMENT_3D ( 'NONE', #61818, #39536, #28584 ) ;
#62574=CARTESIAN_POINT ( 'NONE',  ( -7.250000000000000888, 7.250000000000001776, -19.00000000000000000 ) ) ;
#62575=ORIENTED_EDGE ( 'NONE', *, *, #57053, .T. ) ;
#62579=VERTEX_POINT ( 'NONE', #63332 ) ;
#62581=CARTESIAN_POINT ( 'NONE',  ( -7.250000000000001776, -7.249999999999998224, -16.50000000000000000 ) ) ;
#62586=CIRCLE ( 'NONE', #27576, 1.000000000000000000 ) ;
#62588=LINE ( 'NONE', #10264, #35666 ) ;
#62596=ORIENTED_EDGE ( 'NONE', *, *, #33220, .F. ) ;
#62597=EDGE_CURVE ( 'NONE', #24588, #33736, #57324, .T. ) ;
#62604=ORIENTED_EDGE ( 'NONE', *, *, #38282, .T. ) ;
#62613=CARTESIAN_POINT ( 'NONE',  ( -7.250000000000001776, -7.249999999999998224, -20.50000000000000000 ) ) ;
#62614=ORIENTED_EDGE ( 'NONE', *, *, #55267, .F. ) ;
#62623=FACE_OUTER_BOUND ( 'NONE', #22173, .T. ) ;
#62625=VECTOR ( 'NONE', #41716, 1000.000000000000000 ) ;
#62631=AXIS2_PLACEMENT_3D ( 'NONE', #60247, #16784, #54973 ) ;
#62634=DIRECTION ( 'NONE',  ( -1.000000000000000000, 0.000000000000000000, 0.000000000000000000 ) ) ;
#62648=EDGE_CURVE ( 'NONE', #61023, #17140, #65424, .T. ) ;
#62649=EDGE_CURVE ( 'NONE', #58319, #57460, #43654, .T. ) ;
#62652=DIRECTION ( 'NONE',  ( -1.000000000000000000, 0.000000000000000000, 0.000000000000000000 ) ) ;
#62655=VERTEX_POINT ( 'NONE', #15943 ) ;
#62658=DIRECTION ( 'NONE',  ( 1.000000000000000000, 0.000000000000000000, 0.000000000000000000 ) ) ;
#62669=VECTOR ( 'NONE', #60809, 1000.000000000000000 ) ;
#62671=LINE ( 'NONE', #40762, #38263 ) ;
#62675=DIRECTION ( 'NONE',  ( -1.000000000000000000, 0.000000000000000000, -0.000000000000000000 ) ) ;
#62682=ORIENTED_EDGE ( 'NONE', *, *, #50020, .F. ) ;
#62686=DIRECTION ( 'NONE',  ( -1.000000000000000000, 0.000000000000000000, 0.000000000000000000 ) ) ;
#62689=FACE_OUTER_BOUND ( 'NONE', #24349, .T. ) ;
#62696=ORIENTED_EDGE ( 'NONE', *, *, #7658, .T. ) ;
#62699=ORIENTED_EDGE ( 'NONE', *, *, #725, .T. ) ;
#62704=VERTEX_POINT ( 'NONE', #1073 ) ;
#62709=DIRECTION ( 'NONE',  ( -0.000000000000000000, -0.000000000000000000, 1.000000000000000000 ) ) ;
#62716=DIRECTION ( 'NONE',  ( -1.000000000000000000, 0.000000000000000000, 0.000000000000000000 ) ) ;
#62717=VECTOR ( 'NONE', #16144, 1000.000000000000000 ) ;
#62722=VECTOR ( 'NONE', #41833, 1000.000000000000000 ) ;
#62724=LINE ( 'NONE', #58127, #54909 ) ;
#62729=AXIS2_PLACEMENT_3D ( 'NONE', #38607, #33298, #33641 ) ;
#62730=LINE ( 'NONE', #14650, #63050 ) ;
#62735=EDGE_CURVE ( 'NONE', #64072, #41205, #51571, .T. ) ;
#62738=ORIENTED_EDGE ( 'NONE', *, *, #55795, .T. ) ;
#62753=ADVANCED_FACE ( 'NONE', ( #12686 ), #50183, .T. ) ;
#62754=DIRECTION ( 'NONE',  ( 0.000000000000000000, 0.000000000000000000, 1.000000000000000000 ) ) ;
#62759=EDGE_CURVE ( 'NONE', #5045, #21232, #35762, .T. ) ;
#62768=AXIS2_PLACEMENT_3D ( 'NONE', #59967, #38745, #65295 ) ;
#62772=FACE_OUTER_BOUND ( 'NONE', #50146, .T. ) ;
#62785=ORIENTED_EDGE ( 'NONE', *, *, #7320, .T. ) ;
#62786=VERTEX_POINT ( 'NONE', #67511 ) ;
#62803=EDGE_CURVE ( 'NONE', #49333, #27966, #7738, .T. ) ;
#62805=DIRECTION ( 'NONE',  ( -1.000000000000000000, 0.000000000000000000, 0.000000000000000000 ) ) ;
#62806=CARTESIAN_POINT ( 'NONE',  ( -7.250000000000001776, -7.249999999999998224, -26.00000000000001066 ) ) ;
#62812=LINE ( 'NONE', #13322, #22271 ) ;
#62817=AXIS2_PLACEMENT_3D ( 'NONE', #1480, #17755, #23050 ) ;
#62818=CARTESIAN_POINT ( 'NONE',  ( -6.500000000000002665, 6.500000000000002665, 0.000000000000000000 ) ) ;
#62821=DIRECTION ( 'NONE',  ( -1.000000000000000000, 0.000000000000000000, 0.000000000000000000 ) ) ;
#62834=CYLINDRICAL_SURFACE ( 'NONE', #18551, 0.2000000000000005107 ) ;
#62842=DIRECTION ( 'NONE',  ( 1.000000000000000000, -0.000000000000000000, 0.000000000000000000 ) ) ;
#62854=ORIENTED_EDGE ( 'NONE', *, *, #40719, .T. ) ;
#62885=ADVANCED_FACE ( 'NONE', ( #18702 ), #61847, .F. ) ;
#62904=ORIENTED_EDGE ( 'NONE', *, *, #35168, .T. ) ;
#62908=DIRECTION ( 'NONE',  ( 0.000000000000000000, -0.000000000000000000, 1.000000000000000000 ) ) ;
#62917=CARTESIAN_POINT ( 'NONE',  ( 8.250000000000005329, -7.249999999999998224, -26.00000000000001066 ) ) ;
#62920=ORIENTED_EDGE ( 'NONE', *, *, #38536, .T. ) ;
#62921=CYLINDRICAL_SURFACE ( 'NONE', #37705, 1.000000000000000000 ) ;
#62931=AXIS2_PLACEMENT_3D ( 'NONE', #31638, #32329, #53215 ) ;
#62932=CIRCLE ( 'NONE', #41484, 1.000000000000000000 ) ;
#62953=ORIENTED_EDGE ( 'NONE', *, *, #13399, .T. ) ;
#62960=ORIENTED_EDGE ( 'NONE', *, *, #32290, .T. ) ;
#62965=DIRECTION ( 'NONE',  ( 0.000000000000000000, 0.000000000000000000, 1.000000000000000000 ) ) ;
#62966=ORIENTED_EDGE ( 'NONE', *, *, #36187, .F. ) ;
#62971=VECTOR ( 'NONE', #36940, 1000.000000000000000 ) ;
#62975=ORIENTED_EDGE ( 'NONE', *, *, #63997, .F. ) ;
#62979=CYLINDRICAL_SURFACE ( 'NONE', #14720, 0.1999999999999996503 ) ;
#62982=AXIS2_PLACEMENT_3D ( 'NONE', #69424, #68374, #31268 ) ;
#62989=DIRECTION ( 'NONE',  ( 0.000000000000000000, 0.000000000000000000, 1.000000000000000000 ) ) ;
#62997=CARTESIAN_POINT ( 'NONE',  ( -8.750000000000001776, -7.249999999999998224, -30.00000000000001066 ) ) ;
#63005=CARTESIAN_POINT ( 'NONE',  ( 7.450000000000006395, 7.250000000000000888, -8.500000000000000000 ) ) ;
#63012=ORIENTED_EDGE ( 'NONE', *, *, #52574, .F. ) ;
#63033=ORIENTED_EDGE ( 'NONE', *, *, #23734, .T. ) ;
#63037=CARTESIAN_POINT ( 'NONE',  ( 7.250000000000005329, 7.250000000000000888, -24.50000000000000000 ) ) ;
#63038=CARTESIAN_POINT ( 'NONE',  ( 0.000000000000000000, 0.000000000000000000, -7.500000000000000000 ) ) ;
#63039=VECTOR ( 'NONE', #39217, 1000.000000000000000 ) ;
#63050=VECTOR ( 'NONE', #20645, 1000.000000000000000 ) ;
#63051=CARTESIAN_POINT ( 'NONE',  ( -8.689999999999999503, -9.750000000000001776, -5.000000000000000000 ) ) ;
#63058=DIRECTION ( 'NONE',  ( 0.000000000000000000, 0.000000000000000000, 1.000000000000000000 ) ) ;
#63059=VERTEX_POINT ( 'NONE', #37429 ) ;
#63064=ORIENTED_EDGE ( 'NONE', *, *, #62257, .T. ) ;
#63069=EDGE_CURVE ( 'NONE', #23322, #48765, #58989, .T. ) ;
#63074=EDGE_CURVE ( 'NONE', #55865, #1150, #43772, .T. ) ;
#63089=VECTOR ( 'NONE', #51775, 1000.000000000000000 ) ;
#63090=PLANE ( 'NONE',  #46082 ) ;
#63092=ADVANCED_FACE ( 'NONE', ( #60015 ), #21170, .T. ) ;
#63098=DIRECTION ( 'NONE',  ( 0.000000000000000000, -1.000000000000000000, -0.000000000000000000 ) ) ;
#63099=ORIENTED_EDGE ( 'NONE', *, *, #37390, .F. ) ;
#63103=PLANE ( 'NONE',  #23356 ) ;
#63121=DIRECTION ( 'NONE',  ( 0.000000000000000000, 1.000000000000000000, -0.000000000000000000 ) ) ;
#63125=ORIENTED_EDGE ( 'NONE', *, *, #29026, .T. ) ;
#63126=CARTESIAN_POINT ( 'NONE',  ( -8.250000000000001776, -7.249999999999998224, -10.00000000000000178 ) ) ;
#63139=VERTEX_POINT ( 'NONE', #16559 ) ;
#63141=DIRECTION ( 'NONE',  ( -1.000000000000000000, 0.000000000000000000, 0.000000000000000000 ) ) ;
#63142=ORIENTED_EDGE ( 'NONE', *, *, #63819, .T. ) ;
#63151=VECTOR ( 'NONE', #36468, 1000.000000000000000 ) ;
#63160=VECTOR ( 'NONE', #42092, 1000.000000000000000 ) ;
#63165=CARTESIAN_POINT ( 'NONE',  ( 0.000000000000000000, -7.449999999999998401, -7.500000000000000000 ) ) ;
#63166=VECTOR ( 'NONE', #6060, 1000.000000000000000 ) ;
#63168=ORIENTED_EDGE ( 'NONE', *, *, #44102, .T. ) ;
#63177=AXIS2_PLACEMENT_3D ( 'NONE', #61141, #11671, #6715 ) ;
#63179=CARTESIAN_POINT ( 'NONE',  ( 7.250000000000005329, -7.249999999999998224, -26.00000000000001066 ) ) ;
#63180=VERTEX_POINT ( 'NONE', #29569 ) ;
#63182=CARTESIAN_POINT ( 'NONE',  ( 8.750000000000005329, 0.000000000000000000, -30.00000000000001066 ) ) ;
#63193=ORIENTED_EDGE ( 'NONE', *, *, #43642, .T. ) ;
#63209=DIRECTION ( 'NONE',  ( -1.000000000000000000, 0.000000000000000000, 0.000000000000000000 ) ) ;
#63212=ADVANCED_FACE ( 'NONE', ( #2015 ), #34169, .T. ) ;
#63214=DIRECTION ( 'NONE',  ( -0.000000000000000000, 0.000000000000000000, -1.000000000000000000 ) ) ;
#63220=ORIENTED_EDGE ( 'NONE', *, *, #5594, .T. ) ;
#63234=AXIS2_PLACEMENT_3D ( 'NONE', #25794, #6296, #12268 ) ;
#63244=ADVANCED_FACE ( 'NONE', ( #11912 ), #17917, .T. ) ;
#63245=AXIS2_PLACEMENT_3D ( 'NONE', #14278, #45733, #35471 ) ;
#63247=AXIS2_PLACEMENT_3D ( 'NONE', #25896, #36863, #69019 ) ;
#63248=EDGE_CURVE ( 'NONE', #10391, #68282, #66374, .T. ) ;
#63263=CARTESIAN_POINT ( 'NONE',  ( 0.000000000000000000, -7.449999999999998401, -16.00000000000000000 ) ) ;
#63280=VECTOR ( 'NONE', #6025, 1000.000000000000000 ) ;
#63281=DIRECTION ( 'NONE',  ( 1.000000000000000000, -0.000000000000000000, 0.000000000000000000 ) ) ;
#63285=ORIENTED_EDGE ( 'NONE', *, *, #34592, .T. ) ;
#63288=ORIENTED_EDGE ( 'NONE', *, *, #55636, .F. ) ;
#63289=ADVANCED_FACE ( 'NONE', ( #7302 ), #61044, .T. ) ;
#63295=DIRECTION ( 'NONE',  ( -0.000000000000000000, -0.000000000000000000, 1.000000000000000000 ) ) ;
#63300=CARTESIAN_POINT ( 'NONE',  ( 7.250000000000005329, -7.449999999999998401, -12.00000000000000000 ) ) ;
#63306=ORIENTED_EDGE ( 'NONE', *, *, #37136, .F. ) ;
#63316=PLANE ( 'NONE',  #55860 ) ;
#63324=ORIENTED_EDGE ( 'NONE', *, *, #55487, .F. ) ;
#63325=DIRECTION ( 'NONE',  ( 1.000000000000000000, -5.981805089575194965E-17, 0.000000000000000000 ) ) ;
#63328=ORIENTED_EDGE ( 'NONE', *, *, #38792, .F. ) ;
#63332=CARTESIAN_POINT ( 'NONE',  ( 8.250000000000005329, -7.249999999999998224, -23.50000000000000000 ) ) ;
#63333=DIRECTION ( 'NONE',  ( 0.000000000000000000, 0.000000000000000000, 1.000000000000000000 ) ) ;
#63343=FACE_BOUND ( 'NONE', #69371, .T. ) ;
#63346=VECTOR ( 'NONE', #43360, 1000.000000000000000 ) ;
#63349=EDGE_CURVE ( 'NONE', #50861, #47806, #18975, .T. ) ;
#63352=DIRECTION ( 'NONE',  ( -0.000000000000000000, -0.000000000000000000, -1.000000000000000000 ) ) ;
#63359=CARTESIAN_POINT ( 'NONE',  ( 9.190000000000001279, -9.750000000000001776, -5.000000000000000000 ) ) ;
#63361=AXIS2_PLACEMENT_3D ( 'NONE', #31087, #58316, #9877 ) ;
#63369=ORIENTED_EDGE ( 'NONE', *, *, #44226, .T. ) ;
#63385=VERTEX_POINT ( 'NONE', #62091 ) ;
#63393=DIRECTION ( 'NONE',  ( -1.000000000000000000, 0.000000000000000000, 0.000000000000000000 ) ) ;
#63395=EDGE_LOOP ( 'NONE', ( #19914, #31595, #30853, #47890 ) ) ;
#63397=ORIENTED_EDGE ( 'NONE', *, *, #64350, .T. ) ;
#63398=AXIS2_PLACEMENT_3D ( 'NONE', #31647, #47889, #58527 ) ;
#63408=EDGE_LOOP ( 'NONE', ( #8010, #6066 ) ) ;
#63409=AXIS2_PLACEMENT_3D ( 'NONE', #52400, #46729, #41432 ) ;
#63421=CYLINDRICAL_SURFACE ( 'NONE', #22776, 0.1999999999999996503 ) ;
#63427=EDGE_LOOP ( 'NONE', ( #55350, #26290, #7287, #66853 ) ) ;
#63430=FACE_OUTER_BOUND ( 'NONE', #54993, .T. ) ;
#63436=LINE ( 'NONE', #14641, #63089 ) ;
#63438=DIRECTION ( 'NONE',  ( 0.000000000000000000, -1.000000000000000000, 0.000000000000000000 ) ) ;
#63441=DIRECTION ( 'NONE',  ( -0.000000000000000000, -0.000000000000000000, 1.000000000000000000 ) ) ;
#63443=EDGE_CURVE ( 'NONE', #17140, #17991, #24568, .T. ) ;
#63451=CARTESIAN_POINT ( 'NONE',  ( 8.250000000000005329, 0.000000000000000000, -16.50000000000000000 ) ) ;
#63460=DIRECTION ( 'NONE',  ( 0.000000000000000000, 0.000000000000000000, -1.000000000000000000 ) ) ;
#63472=DIRECTION ( 'NONE',  ( -0.000000000000000000, 0.000000000000000000, 1.000000000000000000 ) ) ;
#63473=ORIENTED_EDGE ( 'NONE', *, *, #50092, .T. ) ;
#63476=CARTESIAN_POINT ( 'NONE',  ( 0.000000000000000000, -7.449999999999998401, -25.50000000000000355 ) ) ;
#63481=ORIENTED_EDGE ( 'NONE', *, *, #11898, .T. ) ;
#63486=DIRECTION ( 'NONE',  ( 1.000000000000000000, 0.000000000000000000, 0.000000000000000000 ) ) ;
#63489=ORIENTED_EDGE ( 'NONE', *, *, #51013, .F. ) ;
#63502=CYLINDRICAL_SURFACE ( 'NONE', #16933, 1.500000000000000444 ) ;
#63511=LINE ( 'NONE', #4806, #26127 ) ;
#63513=LINE ( 'NONE', #69503, #58413 ) ;
#63521=ADVANCED_FACE ( 'NONE', ( #4476 ), #26041, .T. ) ;
#63522=FACE_OUTER_BOUND ( 'NONE', #34135, .T. ) ;
#63525=VERTEX_POINT ( 'NONE', #32723 ) ;
#63526=CARTESIAN_POINT ( 'NONE',  ( 7.250000000000005329, -8.249999999999998224, -26.00000000000001066 ) ) ;
#63530=VECTOR ( 'NONE', #27446, 1000.000000000000000 ) ;
#63531=EDGE_CURVE ( 'NONE', #64467, #55374, #12134, .T. ) ;
#63540=LINE ( 'NONE', #53290, #13872 ) ;
#63542=FACE_BOUND ( 'NONE', #3084, .T. ) ;
#63547=LINE ( 'NONE', #8376, #25564 ) ;
#63553=EDGE_CURVE ( 'NONE', #14970, #21232, #48997, .T. ) ;
#63554=VECTOR ( 'NONE', #23460, 1000.000000000000000 ) ;
#63557=CARTESIAN_POINT ( 'NONE',  ( -8.689999999999999503, 9.750000000000000000, -5.000000000000000000 ) ) ;
#63559=EDGE_CURVE ( 'NONE', #33326, #57065, #14422, .T. ) ;
#63561=AXIS2_PLACEMENT_3D ( 'NONE', #21098, #15788, #55360 ) ;
#63563=EDGE_CURVE ( 'NONE', #20828, #64072, #214, .T. ) ;
#63565=DIRECTION ( 'NONE',  ( -0.000000000000000000, -0.000000000000000000, -1.000000000000000000 ) ) ;
#63575=AXIS2_PLACEMENT_3D ( 'NONE', #38632, #18079, #33323 ) ;
#63578=DIRECTION ( 'NONE',  ( 0.000000000000000000, 0.000000000000000000, -1.000000000000000000 ) ) ;
#63583=ORIENTED_EDGE ( 'NONE', *, *, #6570, .F. ) ;
#63589=CARTESIAN_POINT ( 'NONE',  ( 4.456444791733522252E-16, 7.450000000000002842, -25.00000000000000000 ) ) ;
#63598=CYLINDRICAL_SURFACE ( 'NONE', #56205, 0.1999999999999987899 ) ;
#63604=AXIS2_PLACEMENT_3D ( 'NONE', #6756, #28325, #49895 ) ;
#63622=LINE ( 'NONE', #25430, #41419 ) ;
#63636=DIRECTION ( 'NONE',  ( 0.000000000000000000, -1.000000000000000000, -0.000000000000000000 ) ) ;
#63638=CARTESIAN_POINT ( 'NONE',  ( 8.250000000000005329, -8.249999999999998224, -26.00000000000001066 ) ) ;
#63640=FACE_OUTER_BOUND ( 'NONE', #11902, .T. ) ;
#63641=ORIENTED_EDGE ( 'NONE', *, *, #33208, .F. ) ;
#63647=ADVANCED_FACE ( 'NONE', ( #54652 ), #23762, .F. ) ;
#63649=EDGE_CURVE ( 'NONE', #30178, #34012, #16873, .T. ) ;
#63657=FACE_OUTER_BOUND ( 'NONE', #25457, .T. ) ;
#63661=DIRECTION ( 'NONE',  ( 1.000000000000000000, 0.000000000000000000, 0.000000000000000000 ) ) ;
#63662=AXIS2_PLACEMENT_3D ( 'NONE', #25536, #47438, #14561 ) ;
#63668=DIRECTION ( 'NONE',  ( -1.000000000000000000, 0.000000000000000000, -0.000000000000000000 ) ) ;
#63672=VECTOR ( 'NONE', #26975, 1000.000000000000000 ) ;
#63680=DIRECTION ( 'NONE',  ( 0.000000000000000000, 0.000000000000000000, 1.000000000000000000 ) ) ;
#63681=ORIENTED_EDGE ( 'NONE', *, *, #68032, .F. ) ;
#63684=ORIENTED_EDGE ( 'NONE', *, *, #41234, .F. ) ;
#63685=VERTEX_POINT ( 'NONE', #23422 ) ;
#63695=DIRECTION ( 'NONE',  ( -0.000000000000000000, -0.000000000000000000, 1.000000000000000000 ) ) ;
#63697=EDGE_CURVE ( 'NONE', #10069, #65486, #68812, .T. ) ;
#63699=CARTESIAN_POINT ( 'NONE',  ( 7.250000000000005329, 8.250000000000001776, -14.50000000000000000 ) ) ;
#63706=LINE ( 'NONE', #25876, #23644 ) ;
#63707=DIRECTION ( 'NONE',  ( -0.000000000000000000, -0.000000000000000000, -1.000000000000000000 ) ) ;
#63709=FACE_OUTER_BOUND ( 'NONE', #32883, .T. ) ;
#63713=LINE ( 'NONE', #50720, #3755 ) ;
#63724=EDGE_CURVE ( 'NONE', #18134, #61969, #10304, .T. ) ;
#63725=PLANE ( 'NONE',  #69204 ) ;
#63735=EDGE_LOOP ( 'NONE', ( #58768, #50941, #41439, #19927 ) ) ;
#63736=ORIENTED_EDGE ( 'NONE', *, *, #16461, .T. ) ;
#63742=CARTESIAN_POINT ( 'NONE',  ( -8.250000000000001776, 0.000000000000000000, -14.50000000000000000 ) ) ;
#63746=DIRECTION ( 'NONE',  ( 1.000000000000000000, -5.981805089575194965E-17, 0.000000000000000000 ) ) ;
#63748=CARTESIAN_POINT ( 'NONE',  ( 7.250000000000005329, 8.250000000000001776, -26.00000000000001066 ) ) ;
#63761=ORIENTED_EDGE ( 'NONE', *, *, #1288, .T. ) ;
#63771=VECTOR ( 'NONE', #25040, 1000.000000000000000 ) ;
#63785=LINE ( 'NONE', #15340, #33459 ) ;
#63788=VERTEX_POINT ( 'NONE', #62997 ) ;
#63791=DIRECTION ( 'NONE',  ( 0.000000000000000000, 1.000000000000000000, 0.000000000000000000 ) ) ;
#63793=LINE ( 'NONE', #9703, #56219 ) ;
#63796=AXIS2_PLACEMENT_3D ( 'NONE', #12977, #61073, #34555 ) ;
#63802=CARTESIAN_POINT ( 'NONE',  ( 7.250000000000005329, 7.250000000000000888, -26.00000000000001066 ) ) ;
#63815=CARTESIAN_POINT ( 'NONE',  ( -9.690000000000001279, 9.690000000000001279, -5.000000000000000000 ) ) ;
#63817=LINE ( 'NONE', #37297, #31766 ) ;
#63819=EDGE_CURVE ( 'NONE', #997, #28252, #4996, .T. ) ;
#63835=ADVANCED_FACE ( 'NONE', ( #52041 ), #68658, .T. ) ;
#63839=ORIENTED_EDGE ( 'NONE', *, *, #53507, .F. ) ;
#63854=LINE ( 'NONE', #58194, #23885 ) ;
#63859=AXIS2_PLACEMENT_3D ( 'NONE', #60330, #33123, #39123 ) ;
#63863=DIRECTION ( 'NONE',  ( -1.000000000000000000, 0.000000000000000000, 0.000000000000000000 ) ) ;
#63869=VECTOR ( 'NONE', #32221, 1000.000000000000000 ) ;
#63873=CYLINDRICAL_SURFACE ( 'NONE', #59575, 0.2000000000000005107 ) ;
#63876=ORIENTED_EDGE ( 'NONE', *, *, #14701, .F. ) ;
#63877=LINE ( 'NONE', #15441, #64115 ) ;
#63881=ORIENTED_EDGE ( 'NONE', *, *, #32797, .T. ) ;
#63884=FACE_OUTER_BOUND ( 'NONE', #43903, .T. ) ;
#63889=DIRECTION ( 'NONE',  ( 0.000000000000000000, 0.000000000000000000, -1.000000000000000000 ) ) ;
#63892=EDGE_CURVE ( 'NONE', #15537, #29056, #57493, .T. ) ;
#63900=VECTOR ( 'NONE', #48664, 1000.000000000000000 ) ;
#63908=AXIS2_PLACEMENT_3D ( 'NONE', #40805, #45398, #2621 ) ;
#63912=VECTOR ( 'NONE', #46870, 1000.000000000000000 ) ;
#63913=CARTESIAN_POINT ( 'NONE',  ( -7.450000000000001954, 0.000000000000000000, -12.50000000000000000 ) ) ;
#63922=VECTOR ( 'NONE', #62121, 1000.000000000000000 ) ;
#63923=CARTESIAN_POINT ( 'NONE',  ( 7.450000000000003730, -7.249999999999997335, -11.50000000000000000 ) ) ;
#63924=ORIENTED_EDGE ( 'NONE', *, *, #60380, .F. ) ;
#63930=VERTEX_POINT ( 'NONE', #42820 ) ;
#63937=VERTEX_POINT ( 'NONE', #26920 ) ;
#63938=CARTESIAN_POINT ( 'NONE',  ( 7.250000000000005329, 7.250000000000000888, -19.00000000000000000 ) ) ;
#63942=ORIENTED_EDGE ( 'NONE', *, *, #50092, .F. ) ;
#63944=AXIS2_PLACEMENT_3D ( 'NONE', #49031, #592, #22161 ) ;
#63949=AXIS2_PLACEMENT_3D ( 'NONE', #20546, #48470, #21258 ) ;
#63952=ADVANCED_FACE ( 'NONE', ( #10638 ), #389, .F. ) ;
#63956=DIRECTION ( 'NONE',  ( -0.000000000000000000, -0.000000000000000000, 1.000000000000000000 ) ) ;
#63958=CARTESIAN_POINT ( 'NONE',  ( -8.250000000000001776, -8.249999999999998224, -26.00000000000001066 ) ) ;
#63959=ORIENTED_EDGE ( 'NONE', *, *, #5600, .F. ) ;
#63965=VECTOR ( 'NONE', #4364, 1000.000000000000000 ) ;
#63966=AXIS2_PLACEMENT_3D ( 'NONE', #58367, #20170, #64025 ) ;
#63968=ADVANCED_FACE ( 'NONE', ( #1085, #59782 ), #27599, .T. ) ;
#63970=CARTESIAN_POINT ( 'NONE',  ( -7.250000000000000888, 8.250000000000001776, -26.00000000000001066 ) ) ;
#63978=DIRECTION ( 'NONE',  ( 1.000000000000000000, 0.000000000000000000, 0.000000000000000000 ) ) ;
#63983=ADVANCED_FACE ( 'NONE', ( #48483 ), #32217, .F. ) ;
#63984=DIRECTION ( 'NONE',  ( 1.000000000000000000, 0.000000000000000000, 0.000000000000000000 ) ) ;
#63985=ADVANCED_FACE ( 'NONE', ( #43164 ), #5703, .F. ) ;
#63997=EDGE_CURVE ( 'NONE', #37776, #29168, #33596, .T. ) ;
#64005=CARTESIAN_POINT ( 'NONE',  ( 7.250000000000004441, 7.450000000000001954, -9.000000000000001776 ) ) ;
#64011=EDGE_LOOP ( 'NONE', ( #52015, #52523, #56177, #65345 ) ) ;
#64015=ORIENTED_EDGE ( 'NONE', *, *, #7151, .F. ) ;
#64025=DIRECTION ( 'NONE',  ( -1.000000000000000000, 0.000000000000000000, 0.000000000000000000 ) ) ;
#64029=DIRECTION ( 'NONE',  ( 1.000000000000000000, 0.000000000000000000, 0.000000000000000000 ) ) ;
#64035=CARTESIAN_POINT ( 'NONE',  ( 0.000000000000000000, 0.000000000000000000, -23.50000000000000000 ) ) ;
#64036=VECTOR ( 'NONE', #5359, 1000.000000000000000 ) ;
#64047=ORIENTED_EDGE ( 'NONE', *, *, #24619, .T. ) ;
#64049=DIRECTION ( 'NONE',  ( 1.000000000000000000, 0.000000000000000000, 0.000000000000000000 ) ) ;
#64056=EDGE_CURVE ( 'NONE', #63385, #12173, #8446, .T. ) ;
#64060=DIRECTION ( 'NONE',  ( 1.000000000000000000, 0.000000000000000000, -0.000000000000000000 ) ) ;
#64067=ADVANCED_FACE ( 'NONE', ( #66114 ), #66461, .T. ) ;
#64072=VERTEX_POINT ( 'NONE', #39243 ) ;
#64073=AXIS2_PLACEMENT_3D ( 'NONE', #30489, #67275, #51005 ) ;
#64080=VECTOR ( 'NONE', #55473, 1000.000000000000000 ) ;
#64081=EDGE_LOOP ( 'NONE', ( #20418, #5246, #22986, #48422 ) ) ;
#64084=ORIENTED_EDGE ( 'NONE', *, *, #47112, .F. ) ;
#64085=DIRECTION ( 'NONE',  ( 0.000000000000000000, 0.000000000000000000, 1.000000000000000000 ) ) ;
#64090=DIRECTION ( 'NONE',  ( 0.000000000000000000, 0.000000000000000000, 1.000000000000000000 ) ) ;
#64098=VERTEX_POINT ( 'NONE', #62197 ) ;
#64105=DIRECTION ( 'NONE',  ( -1.000000000000000000, 0.000000000000000000, 0.000000000000000000 ) ) ;
#64110=LINE ( 'NONE', #42163, #44694 ) ;
#64115=VECTOR ( 'NONE', #37359, 1000.000000000000000 ) ;
#64125=ORIENTED_EDGE ( 'NONE', *, *, #8643, .F. ) ;
#64134=CARTESIAN_POINT ( 'NONE',  ( -7.250000000000000888, 7.250000000000001776, -25.00000000000000000 ) ) ;
#64138=AXIS2_PLACEMENT_3D ( 'NONE', #40188, #13675, #45848 ) ;
#64142=DIRECTION ( 'NONE',  ( 0.000000000000000000, 0.000000000000000000, 1.000000000000000000 ) ) ;
#64151=EDGE_CURVE ( 'NONE', #22300, #63937, #7403, .T. ) ;
#64153=ORIENTED_EDGE ( 'NONE', *, *, #66000, .T. ) ;
#64155=VERTEX_POINT ( 'NONE', #2111 ) ;
#64158=EDGE_CURVE ( 'NONE', #2063, #21563, #8097, .T. ) ;
#64160=CARTESIAN_POINT ( 'NONE',  ( -7.250000000000000888, 7.250000000000001776, -8.500000000000000000 ) ) ;
#64167=DIRECTION ( 'NONE',  ( 1.000000000000000000, 0.000000000000000000, 0.000000000000000000 ) ) ;
#64174=ORIENTED_EDGE ( 'NONE', *, *, #62128, .F. ) ;
#64176=LINE ( 'NONE', #46833, #36168 ) ;
#64183=CIRCLE ( 'NONE', #31423, 0.2000000000000005107 ) ;
#64185=CARTESIAN_POINT ( 'NONE',  ( 7.450000000000004619, -1.336933437520057563E-15, -17.00000000000000000 ) ) ;
#64188=EDGE_CURVE ( 'NONE', #7124, #35485, #57898, .T. ) ;
#64203=VERTEX_POINT ( 'NONE', #14822 ) ;
#64204=ORIENTED_EDGE ( 'NONE', *, *, #35555, .T. ) ;
#64206=DIRECTION ( 'NONE',  ( -1.000000000000000000, 0.000000000000000000, 0.000000000000000000 ) ) ;
#64208=DIRECTION ( 'NONE',  ( 0.000000000000000000, 0.000000000000000000, 1.000000000000000000 ) ) ;
#64209=ORIENTED_EDGE ( 'NONE', *, *, #16454, .F. ) ;
#64210=VECTOR ( 'NONE', #18140, 1000.000000000000000 ) ;
#64211=LINE ( 'NONE', #53256, #61669 ) ;
#64212=LINE ( 'NONE', #16108, #14869 ) ;
#64222=DIRECTION ( 'NONE',  ( -1.000000000000000000, 0.000000000000000000, 0.000000000000000000 ) ) ;
#64245=ORIENTED_EDGE ( 'NONE', *, *, #39147, .T. ) ;
#64250=DIRECTION ( 'NONE',  ( 0.000000000000000000, 0.000000000000000000, 1.000000000000000000 ) ) ;
#64264=ORIENTED_EDGE ( 'NONE', *, *, #6355, .T. ) ;
#64282=ORIENTED_EDGE ( 'NONE', *, *, #24519, .T. ) ;
#64290=ORIENTED_EDGE ( 'NONE', *, *, #69567, .F. ) ;
#64291=PLANE ( 'NONE',  #43662 ) ;
#64298=ORIENTED_EDGE ( 'NONE', *, *, #65245, .T. ) ;
#64299=VECTOR ( 'NONE', #69980, 1000.000000000000000 ) ;
#64315=DIRECTION ( 'NONE',  ( -5.981805089575196197E-17, -1.000000000000000000, 0.000000000000000000 ) ) ;
#64328=CARTESIAN_POINT ( 'NONE',  ( -7.250000000000000888, 8.250000000000001776, -8.500000000000000000 ) ) ;
#64331=FACE_OUTER_BOUND ( 'NONE', #19008, .T. ) ;
#64336=ORIENTED_EDGE ( 'NONE', *, *, #43763, .F. ) ;
#64341=DIRECTION ( 'NONE',  ( -0.000000000000000000, -0.000000000000000000, -1.000000000000000000 ) ) ;
#64350=EDGE_CURVE ( 'NONE', #11735, #16770, #48886, .T. ) ;
#64351=ORIENTED_EDGE ( 'NONE', *, *, #63553, .F. ) ;
#64357=CIRCLE ( 'NONE', #21442, 1.000000000000000000 ) ;
#64358=CARTESIAN_POINT ( 'NONE',  ( 8.750000000000005329, 0.000000000000000000, -30.00000000000001066 ) ) ;
#64361=ORIENTED_EDGE ( 'NONE', *, *, #40004, .F. ) ;
#64366=VECTOR ( 'NONE', #44213, 1000.000000000000000 ) ;
#64369=VECTOR ( 'NONE', #51001, 1000.000000000000000 ) ;
#64376=LINE ( 'NONE', #31854, #48209 ) ;
#64378=EDGE_CURVE ( 'NONE', #29056, #55597, #5947, .T. ) ;
#64382=VERTEX_POINT ( 'NONE', #49080 ) ;
#64383=DIRECTION ( 'NONE',  ( 0.000000000000000000, 0.000000000000000000, -1.000000000000000000 ) ) ;
#64386=ORIENTED_EDGE ( 'NONE', *, *, #32334, .F. ) ;
#64390=EDGE_CURVE ( 'NONE', #32920, #56770, #69209, .T. ) ;
#64397=LINE ( 'NONE', #32572, #69080 ) ;
#64398=LINE ( 'NONE', #47771, #64036 ) ;
#64399=LINE ( 'NONE', #55168, #36920 ) ;
#64404=CARTESIAN_POINT ( 'NONE',  ( 0.000000000000000000, 8.250000000000001776, -14.50000000000000000 ) ) ;
#64405=AXIS2_PLACEMENT_3D ( 'NONE', #57020, #2232, #2933 ) ;
#64409=DIRECTION ( 'NONE',  ( 0.000000000000000000, 1.000000000000000000, 0.000000000000000000 ) ) ;
#64449=ORIENTED_EDGE ( 'NONE', *, *, #61950, .F. ) ;
#64467=VERTEX_POINT ( 'NONE', #55093 ) ;
#64478=ORIENTED_EDGE ( 'NONE', *, *, #45185, .T. ) ;
#64484=CARTESIAN_POINT ( 'NONE',  ( -7.250000000000001776, -7.249999999999998224, -12.00000000000000000 ) ) ;
#64488=EDGE_CURVE ( 'NONE', #50504, #27562, #21813, .T. ) ;
#64492=CIRCLE ( 'NONE', #26077, 0.1999999999999996503 ) ;
#64493=EDGE_CURVE ( 'NONE', #42459, #56941, #28558, .T. ) ;
#64494=CARTESIAN_POINT ( 'NONE',  ( -7.250000000000001776, -7.249999999999998224, -9.500000000000001776 ) ) ;
#64497=ORIENTED_EDGE ( 'NONE', *, *, #30529, .T. ) ;
#64498=DIRECTION ( 'NONE',  ( -1.000000000000000000, 0.000000000000000000, 0.000000000000000000 ) ) ;
#64499=VECTOR ( 'NONE', #53346, 1000.000000000000000 ) ;
#64501=AXIS2_PLACEMENT_3D ( 'NONE', #27509, #11235, #44440 ) ;
#64504=CARTESIAN_POINT ( 'NONE',  ( -7.450000000000001954, 7.250000000000000000, -17.00000000000000000 ) ) ;
#64506=VECTOR ( 'NONE', #68222, 1000.000000000000000 ) ;
#64508=CARTESIAN_POINT ( 'NONE',  ( -7.250000000000000888, 7.250000000000001776, -19.50000000000000000 ) ) ;
#64509=DIRECTION ( 'NONE',  ( -1.000000000000000000, 0.000000000000000000, 0.000000000000000000 ) ) ;
#64514=CARTESIAN_POINT ( 'NONE',  ( 8.250000000000005329, 7.250000000000000888, -23.50000000000000000 ) ) ;
#64525=EDGE_LOOP ( 'NONE', ( #55411, #6838, #33570, #30185, #52067, #31662, #15551, #2834 ) ) ;
#64533=EDGE_CURVE ( 'NONE', #36733, #34015, #54587, .T. ) ;
#64534=VERTEX_POINT ( 'NONE', #67436 ) ;
#64540=EDGE_CURVE ( 'NONE', #65447, #31143, #7105, .T. ) ;
#64544=DIRECTION ( 'NONE',  ( 0.000000000000000000, -1.000000000000000000, 0.000000000000000000 ) ) ;
#64557=EDGE_LOOP ( 'NONE', ( #2940, #35732, #38471, #19467 ) ) ;
#64558=CIRCLE ( 'NONE', #13707, 1.000000000000000000 ) ;
#64565=CARTESIAN_POINT ( 'NONE',  ( -7.250000000000001776, -7.249999999999998224, -21.50000000000000000 ) ) ;
#64566=ORIENTED_EDGE ( 'NONE', *, *, #5830, .T. ) ;
#64578=ORIENTED_EDGE ( 'NONE', *, *, #52389, .F. ) ;
#64580=CARTESIAN_POINT ( 'NONE',  ( 7.250000000000005329, 7.250000000000000888, -16.00000000000000000 ) ) ;
#64583=ORIENTED_EDGE ( 'NONE', *, *, #4491, .F. ) ;
#64586=DIRECTION ( 'NONE',  ( 1.000000000000000000, 0.000000000000000000, 0.000000000000000000 ) ) ;
#64589=CARTESIAN_POINT ( 'NONE',  ( -7.250000000000001776, -7.249999999999998224, -23.50000000000000000 ) ) ;
#64591=EDGE_LOOP ( 'NONE', ( #60395, #17210, #30383, #30986, #30882, #16100, #19556, #24903 ) ) ;
#64597=CARTESIAN_POINT ( 'NONE',  ( -8.250000000000001776, 0.000000000000000000, -12.50000000000000000 ) ) ;
#64599=AXIS2_PLACEMENT_3D ( 'NONE', #51107, #45798, #24939 ) ;
#64604=CARTESIAN_POINT ( 'NONE',  ( 7.250000000000005329, -7.249999999999998224, -21.50000000000000000 ) ) ;
#64605=EDGE_CURVE ( 'NONE', #69141, #27966, #50112, .T. ) ;
#64609=DIRECTION ( 'NONE',  ( -0.000000000000000000, -0.000000000000000000, 1.000000000000000000 ) ) ;
#64617=LINE ( 'NONE', #20432, #20946 ) ;
#64618=ORIENTED_EDGE ( 'NONE', *, *, #69626, .F. ) ;
#64643=DIRECTION ( 'NONE',  ( 0.000000000000000000, 0.000000000000000000, 1.000000000000000000 ) ) ;
#64644=AXIS2_PLACEMENT_3D ( 'NONE', #178, #22767, #22433 ) ;
#64664=ORIENTED_EDGE ( 'NONE', *, *, #17731, .F. ) ;
#64678=CARTESIAN_POINT ( 'NONE',  ( 7.450000000000004619, -1.336933437520057563E-15, -13.00000000000000178 ) ) ;
#64679=AXIS2_PLACEMENT_3D ( 'NONE', #68410, #31639, #19964 ) ;
#64691=CARTESIAN_POINT ( 'NONE',  ( 8.250000000000005329, -8.249999999999998224, -26.00000000000001066 ) ) ;
#64695=VECTOR ( 'NONE', #53410, 1000.000000000000000 ) ;
#64705=EDGE_CURVE ( 'NONE', #48543, #37936, #25709, .T. ) ;
#64717=ORIENTED_EDGE ( 'NONE', *, *, #68420, .T. ) ;
#64721=VECTOR ( 'NONE', #4828, 1000.000000000000000 ) ;
#64728=DIRECTION ( 'NONE',  ( -1.000000000000000000, 0.000000000000000000, 0.000000000000000000 ) ) ;
#64730=LINE ( 'NONE', #9956, #22200 ) ;
#64734=AXIS2_PLACEMENT_3D ( 'NONE', #37211, #33285, #42503 ) ;
#64743=LINE ( 'NONE', #48486, #6274 ) ;
#64750=VERTEX_POINT ( 'NONE', #62818 ) ;
#64777=ORIENTED_EDGE ( 'NONE', *, *, #64835, .T. ) ;
#64778=ORIENTED_EDGE ( 'NONE', *, *, #39307, .T. ) ;
#64780=ORIENTED_EDGE ( 'NONE', *, *, #14601, .T. ) ;
#64785=EDGE_CURVE ( 'NONE', #6993, #17846, #33113, .T. ) ;
#64792=CARTESIAN_POINT ( 'NONE',  ( -8.689999999999999503, -8.750000000000000000, -7.000000000000000000 ) ) ;
#64803=ORIENTED_EDGE ( 'NONE', *, *, #6566, .T. ) ;
#64812=ORIENTED_EDGE ( 'NONE', *, *, #43729, .T. ) ;
#64825=AXIS2_PLACEMENT_3D ( 'NONE', #13877, #51356, #24843 ) ;
#64833=ORIENTED_EDGE ( 'NONE', *, *, #8648, .T. ) ;
#64835=EDGE_CURVE ( 'NONE', #57460, #18304, #27081, .T. ) ;
#64840=EDGE_CURVE ( 'NONE', #50433, #48836, #37698, .T. ) ;
#64846=CYLINDRICAL_SURFACE ( 'NONE', #3107, 1.000000000000000000 ) ;
#64855=DIRECTION ( 'NONE',  ( 0.000000000000000000, 1.000000000000000000, -0.000000000000000000 ) ) ;
#64858=AXIS2_PLACEMENT_3D ( 'NONE', #34987, #50908, #24395 ) ;
#64860=EDGE_CURVE ( 'NONE', #59223, #43564, #26364, .T. ) ;
#64863=ORIENTED_EDGE ( 'NONE', *, *, #18939, .F. ) ;
#64867=CIRCLE ( 'NONE', #33263, 0.1999999999999996503 ) ;
#64869=CARTESIAN_POINT ( 'NONE',  ( 4.456444791733522252E-16, 7.450000000000002842, -14.50000000000000000 ) ) ;
#64870=CARTESIAN_POINT ( 'NONE',  ( 0.000000000000000000, 8.250000000000001776, -13.00000000000000178 ) ) ;
#64871=ORIENTED_EDGE ( 'NONE', *, *, #68969, .F. ) ;
#64880=EDGE_CURVE ( 'NONE', #3823, #56702, #1586, .T. ) ;
#64881=DIRECTION ( 'NONE',  ( 0.000000000000000000, -1.000000000000000000, -0.000000000000000000 ) ) ;
#64884=EDGE_CURVE ( 'NONE', #18304, #3392, #12541, .T. ) ;
#64887=ORIENTED_EDGE ( 'NONE', *, *, #34216, .T. ) ;
#64888=ORIENTED_EDGE ( 'NONE', *, *, #45637, .T. ) ;
#64905=LINE ( 'NONE', #38979, #66514 ) ;
#64913=DIRECTION ( 'NONE',  ( -1.000000000000000000, 0.000000000000000000, 0.000000000000000000 ) ) ;
#64920=CIRCLE ( 'NONE', #62631, 0.2000000000000005107 ) ;
#64931=CARTESIAN_POINT ( 'NONE',  ( 7.250000000000005329, 8.250000000000001776, -20.00000000000000000 ) ) ;
#64940=CARTESIAN_POINT ( 'NONE',  ( -8.250000000000001776, 7.250000000000000888, -26.00000000000001066 ) ) ;
#64944=ORIENTED_EDGE ( 'NONE', *, *, #28916, .F. ) ;
#64946=DIRECTION ( 'NONE',  ( -1.000000000000000000, 0.000000000000000000, 0.000000000000000000 ) ) ;
#64947=ORIENTED_EDGE ( 'NONE', *, *, #47422, .T. ) ;
#64948=DIRECTION ( 'NONE',  ( 0.000000000000000000, 0.000000000000000000, 1.000000000000000000 ) ) ;
#64949=DIRECTION ( 'NONE',  ( 0.000000000000000000, 0.000000000000000000, 1.000000000000000000 ) ) ;
#64958=FACE_BOUND ( 'NONE', #60166, .T. ) ;
#64961=AXIS2_PLACEMENT_3D ( 'NONE', #40518, #13646, #63141 ) ;
#64965=ORIENTED_EDGE ( 'NONE', *, *, #63069, .T. ) ;
#64968=CARTESIAN_POINT ( 'NONE',  ( -7.250000000000000888, -8.249999999999998224, -26.00000000000001066 ) ) ;
#64974=ADVANCED_FACE ( 'NONE', ( #50724 ), #2295, .F. ) ;
#64979=ORIENTED_EDGE ( 'NONE', *, *, #43320, .F. ) ;
#64996=ORIENTED_EDGE ( 'NONE', *, *, #28035, .T. ) ;
#65005=EDGE_CURVE ( 'NONE', #64098, #27857, #43316, .T. ) ;
#65006=EDGE_LOOP ( 'NONE', ( #64290, #49541, #48610, #50266 ) ) ;
#65013=AXIS2_PLACEMENT_3D ( 'NONE', #58812, #10369, #53509 ) ;
#65016=CARTESIAN_POINT ( 'NONE',  ( -7.250000000000000888, -8.249999999999998224, -17.50000000000000000 ) ) ;
#65019=CIRCLE ( 'NONE', #34500, 0.1999999999999987899 ) ;
#65035=VERTEX_POINT ( 'NONE', #11397 ) ;
#65039=CARTESIAN_POINT ( 'NONE',  ( -8.250000000000001776, -7.249999999999998224, -26.00000000000001066 ) ) ;
#65061=EDGE_LOOP ( 'NONE', ( #62960, #50843, #48648, #41891 ) ) ;
#65065=AXIS2_PLACEMENT_3D ( 'NONE', #7949, #19269, #45431 ) ;
#65075=DIRECTION ( 'NONE',  ( -1.000000000000000000, 0.000000000000000000, 0.000000000000000000 ) ) ;
#65089=CARTESIAN_POINT ( 'NONE',  ( 7.250000000000004441, 7.450000000000001954, -7.500000000000000000 ) ) ;
#65101=DIRECTION ( 'NONE',  ( -0.000000000000000000, 0.000000000000000000, 1.000000000000000000 ) ) ;
#65106=EDGE_CURVE ( 'NONE', #4795, #49394, #22017, .T. ) ;
#65113=DIRECTION ( 'NONE',  ( 1.000000000000000000, 0.000000000000000000, 0.000000000000000000 ) ) ;
#65117=FACE_OUTER_BOUND ( 'NONE', #69793, .T. ) ;
#65128=AXIS2_PLACEMENT_3D ( 'NONE', #59860, #33673, #17765 ) ;
#65129=CYLINDRICAL_SURFACE ( 'NONE', #64734, 0.1999999999999996503 ) ;
#65134=ORIENTED_EDGE ( 'NONE', *, *, #847, .F. ) ;
#65143=DIRECTION ( 'NONE',  ( 0.000000000000000000, 0.000000000000000000, 1.000000000000000000 ) ) ;
#65148=DIRECTION ( 'NONE',  ( -1.000000000000000000, 0.000000000000000000, -0.000000000000000000 ) ) ;
#65149=ORIENTED_EDGE ( 'NONE', *, *, #39131, .F. ) ;
#65154=LINE ( 'NONE', #54542, #419 ) ;
#65161=DIRECTION ( 'NONE',  ( 0.000000000000000000, 0.000000000000000000, 1.000000000000000000 ) ) ;
#65164=ORIENTED_EDGE ( 'NONE', *, *, #23480, .F. ) ;
#65166=AXIS2_PLACEMENT_3D ( 'NONE', #38812, #64315, #60368 ) ;
#65170=PLANE ( 'NONE',  #5203 ) ;
#65173=CIRCLE ( 'NONE', #34650, 1.000000000000003553 ) ;
#65175=CARTESIAN_POINT ( 'NONE',  ( 7.450000000000006395, 7.250000000000000888, -25.50000000000000355 ) ) ;
#65187=CARTESIAN_POINT ( 'NONE',  ( -7.450000000000001954, 0.000000000000000000, -25.50000000000000355 ) ) ;
#65190=CARTESIAN_POINT ( 'NONE',  ( 7.250000000000004441, 7.450000000000001954, -17.00000000000000000 ) ) ;
#65193=CARTESIAN_POINT ( 'NONE',  ( 0.000000000000000000, -8.249999999999998224, -7.500000000000000000 ) ) ;
#65198=CARTESIAN_POINT ( 'NONE',  ( -7.250000000000000888, -8.249999999999998224, -8.000000000000000000 ) ) ;
#65202=ADVANCED_FACE ( 'NONE', ( #12081 ), #2865, .T. ) ;
#65205=DIRECTION ( 'NONE',  ( -0.000000000000000000, -0.000000000000000000, 1.000000000000000000 ) ) ;
#65208=CARTESIAN_POINT ( 'NONE',  ( 7.250000000000004441, 7.450000000000001954, -15.50000000000000000 ) ) ;
#65212=ADVANCED_FACE ( 'NONE', ( #24442, #29040 ), #50956, .F. ) ;
#65220=CYLINDRICAL_SURFACE ( 'NONE', #67835, 1.000000000000000000 ) ;
#65222=VECTOR ( 'NONE', #4422, 1000.000000000000000 ) ;
#65241=AXIS2_PLACEMENT_3D ( 'NONE', #69951, #60024, #53699 ) ;
#65245=EDGE_CURVE ( 'NONE', #55597, #24719, #50262, .T. ) ;
#65246=CYLINDRICAL_SURFACE ( 'NONE', #49717, 0.1999999999999987899 ) ;
#65250=ORIENTED_EDGE ( 'NONE', *, *, #11722, .T. ) ;
#65258=FACE_BOUND ( 'NONE', #53378, .T. ) ;
#65260=ADVANCED_FACE ( 'NONE', ( #1471 ), #34685, .T. ) ;
#65268=EDGE_CURVE ( 'NONE', #57460, #67717, #67581, .T. ) ;
#65270=CARTESIAN_POINT ( 'NONE',  ( -7.250000000000000888, 7.250000000000001776, -20.50000000000000000 ) ) ;
#65271=DIRECTION ( 'NONE',  ( -0.000000000000000000, -0.000000000000000000, -1.000000000000000000 ) ) ;
#65273=VECTOR ( 'NONE', #11660, 1000.000000000000000 ) ;
#65283=LINE ( 'NONE', #59265, #12950 ) ;
#65293=CYLINDRICAL_SURFACE ( 'NONE', #53610, 1.000000000000002665 ) ;
#65295=DIRECTION ( 'NONE',  ( -1.000000000000000000, 0.000000000000000000, 0.000000000000000000 ) ) ;
#65305=ORIENTED_EDGE ( 'NONE', *, *, #44824, .F. ) ;
#65315=EDGE_CURVE ( 'NONE', #19554, #33973, #60162, .T. ) ;
#65316=DIRECTION ( 'NONE',  ( -1.000000000000000000, 0.000000000000000000, -0.000000000000000000 ) ) ;
#65317=DIRECTION ( 'NONE',  ( -1.000000000000000000, 0.000000000000000000, 0.000000000000000000 ) ) ;
#65324=ORIENTED_EDGE ( 'NONE', *, *, #5143, .T. ) ;
#65329=ADVANCED_FACE ( 'NONE', ( #19132 ), #36444, .T. ) ;
#65331=DIRECTION ( 'NONE',  ( 0.000000000000000000, 0.000000000000000000, 1.000000000000000000 ) ) ;
#65333=CIRCLE ( 'NONE', #10016, 0.1999999999999996503 ) ;
#65338=VERTEX_POINT ( 'NONE', #19476 ) ;
#65345=ORIENTED_EDGE ( 'NONE', *, *, #54113, .F. ) ;
#65353=ORIENTED_EDGE ( 'NONE', *, *, #26942, .T. ) ;
#65366=CARTESIAN_POINT ( 'NONE',  ( -7.450000000000001954, 7.250000000000000000, -22.50000000000000000 ) ) ;
#65370=EDGE_LOOP ( 'NONE', ( #68260, #62335, #66790, #30103 ) ) ;
#65382=EDGE_CURVE ( 'NONE', #26490, #32938, #30091, .T. ) ;
#65391=ORIENTED_EDGE ( 'NONE', *, *, #56278, .T. ) ;
#65396=ORIENTED_EDGE ( 'NONE', *, *, #44364, .F. ) ;
#65407=VECTOR ( 'NONE', #24622, 1000.000000000000000 ) ;
#65424=LINE ( 'NONE', #27935, #16552 ) ;
#65431=AXIS2_PLACEMENT_3D ( 'NONE', #12783, #45313, #45665 ) ;
#65435=DIRECTION ( 'NONE',  ( 1.334402673828313093E-16, 1.000000000000000000, 0.000000000000000000 ) ) ;
#65436=DIRECTION ( 'NONE',  ( 0.000000000000000000, -0.000000000000000000, 1.000000000000000000 ) ) ;
#65438=FACE_OUTER_BOUND ( 'NONE', #56234, .T. ) ;
#65439=DIRECTION ( 'NONE',  ( 0.000000000000000000, -1.000000000000000000, 0.000000000000000000 ) ) ;
#65441=DIRECTION ( 'NONE',  ( 0.000000000000000000, 1.000000000000000000, 0.000000000000000000 ) ) ;
#65446=ADVANCED_FACE ( 'NONE', ( #66566, #34365 ), #67270, .F. ) ;
#65447=VERTEX_POINT ( 'NONE', #50649 ) ;
#65450=ADVANCED_FACE ( 'NONE', ( #2213, #34731 ), #23438, .T. ) ;
#65455=PLANE ( 'NONE',  #57581 ) ;
#65461=ORIENTED_EDGE ( 'NONE', *, *, #62597, .T. ) ;
#65464=CARTESIAN_POINT ( 'NONE',  ( -7.250000000000001776, -7.249999999999998224, -24.50000000000000000 ) ) ;
#65466=AXIS2_PLACEMENT_3D ( 'NONE', #44555, #12718, #28644 ) ;
#65467=FACE_OUTER_BOUND ( 'NONE', #63395, .T. ) ;
#65468=LINE ( 'NONE', #22675, #55512 ) ;
#65472=ORIENTED_EDGE ( 'NONE', *, *, #60640, .F. ) ;
#65477=DIRECTION ( 'NONE',  ( -1.000000000000000000, 0.000000000000000000, -0.000000000000000000 ) ) ;
#65486=VERTEX_POINT ( 'NONE', #56655 ) ;
#65490=EDGE_CURVE ( 'NONE', #58160, #26913, #39345, .T. ) ;
#65491=LINE ( 'NONE', #43913, #42148 ) ;
#65492=ADVANCED_FACE ( 'NONE', ( #19175 ), #28729, .F. ) ;
#65497=ORIENTED_EDGE ( 'NONE', *, *, #1163, .F. ) ;
#65501=VERTEX_POINT ( 'NONE', #56307 ) ;
#65509=AXIS2_PLACEMENT_3D ( 'NONE', #57525, #51169, #61784 ) ;
#65522=VECTOR ( 'NONE', #57975, 1000.000000000000000 ) ;
#65524=EDGE_LOOP ( 'NONE', ( #12361, #24190, #24706, #21396, #41386, #7129, #17347, #41987 ) ) ;
#65530=CARTESIAN_POINT ( 'NONE',  ( 8.250000000000005329, -8.249999999999998224, -26.00000000000001066 ) ) ;
#65531=ORIENTED_EDGE ( 'NONE', *, *, #16396, .F. ) ;
#65541=CARTESIAN_POINT ( 'NONE',  ( 7.250000000000005329, 8.250000000000001776, -24.00000000000000000 ) ) ;
#65548=LINE ( 'NONE', #38338, #54363 ) ;
#65553=AXIS2_PLACEMENT_3D ( 'NONE', #53637, #63889, #15460 ) ;
#65564=VECTOR ( 'NONE', #49385, 1000.000000000000000 ) ;
#65577=VERTEX_POINT ( 'NONE', #25544 ) ;
#65588=DIRECTION ( 'NONE',  ( -1.000000000000000000, 0.000000000000000000, 0.000000000000000000 ) ) ;
#65590=EDGE_LOOP ( 'NONE', ( #8894, #30950, #35200, #46859, #48009, #63220, #18087, #68535 ) ) ;
#65596=LINE ( 'NONE', #28446, #57431 ) ;
#65599=DIRECTION ( 'NONE',  ( 1.000000000000000000, 0.000000000000000000, 0.000000000000000000 ) ) ;
#65610=AXIS2_PLACEMENT_3D ( 'NONE', #19979, #42237, #3718 ) ;
#65615=CARTESIAN_POINT ( 'NONE',  ( -7.450000000000001954, -7.249999999999998224, -23.00000000000000000 ) ) ;
#65623=CARTESIAN_POINT ( 'NONE',  ( 7.250000000000005329, -7.249999999999998224, -26.00000000000001066 ) ) ;
#65629=LINE ( 'NONE', #49713, #24817 ) ;
#65632=ADVANCED_FACE ( 'NONE', ( #42137 ), #63725, .F. ) ;
#65634=EDGE_CURVE ( 'NONE', #9491, #46497, #31551, .T. ) ;
#65640=DIRECTION ( 'NONE',  ( -0.000000000000000000, -0.000000000000000000, 1.000000000000000000 ) ) ;
#65642=ORIENTED_EDGE ( 'NONE', *, *, #4511, .F. ) ;
#65647=ADVANCED_FACE ( 'NONE', ( #22580 ), #54757, .T. ) ;
#65658=ORIENTED_EDGE ( 'NONE', *, *, #47944, .T. ) ;
#65659=AXIS2_PLACEMENT_3D ( 'NONE', #44224, #33961, #39613 ) ;
#65661=ORIENTED_EDGE ( 'NONE', *, *, #34400, .F. ) ;
#65662=CARTESIAN_POINT ( 'NONE',  ( 8.250000000000005329, 7.250000000000000888, -21.50000000000000000 ) ) ;
#65663=EDGE_CURVE ( 'NONE', #53017, #6284, #39852, .T. ) ;
#65667=EDGE_CURVE ( 'NONE', #46124, #1043, #37576, .T. ) ;
#65683=LINE ( 'NONE', #34526, #10432 ) ;
#65684=CARTESIAN_POINT ( 'NONE',  ( 7.250000000000005329, 7.250000000000000888, -26.00000000000001066 ) ) ;
#65686=EDGE_CURVE ( 'NONE', #53195, #52907, #55786, .T. ) ;
#65703=EDGE_CURVE ( 'NONE', #27724, #21330, #39843, .T. ) ;
#65744=EDGE_CURVE ( 'NONE', #67142, #26429, #25193, .T. ) ;
#65754=DIRECTION ( 'NONE',  ( -1.000000000000000000, 0.000000000000000000, 0.000000000000000000 ) ) ;
#65763=ORIENTED_EDGE ( 'NONE', *, *, #66481, .T. ) ;
#65776=CARTESIAN_POINT ( 'NONE',  ( 8.250000000000005329, 0.000000000000000000, -21.50000000000000000 ) ) ;
#65777=VERTEX_POINT ( 'NONE', #33182 ) ;
#65779=CARTESIAN_POINT ( 'NONE',  ( -7.450000000000001954, -7.249999999999998224, -24.50000000000000000 ) ) ;
#65782=CARTESIAN_POINT ( 'NONE',  ( -7.250000000000001776, -7.249999999999998224, -26.00000000000001066 ) ) ;
#65788=CARTESIAN_POINT ( 'NONE',  ( -7.450000000000001954, -7.249999999999998224, -11.00000000000000000 ) ) ;
#65795=DIRECTION ( 'NONE',  ( 0.000000000000000000, 0.000000000000000000, 1.000000000000000000 ) ) ;
#65799=ORIENTED_EDGE ( 'NONE', *, *, #45821, .F. ) ;
#65803=CYLINDRICAL_SURFACE ( 'NONE', #15208, 1.000000000000000000 ) ;
#65816=CARTESIAN_POINT ( 'NONE',  ( -7.450000000000001954, 7.250000000000000000, -22.00000000000000000 ) ) ;
#65822=ORIENTED_EDGE ( 'NONE', *, *, #25254, .F. ) ;
#65835=CARTESIAN_POINT ( 'NONE',  ( -7.250000000000000888, 7.450000000000003730, -11.00000000000000000 ) ) ;
#65840=DIRECTION ( 'NONE',  ( -1.000000000000000000, 0.000000000000000000, 0.000000000000000000 ) ) ;
#65842=CARTESIAN_POINT ( 'NONE',  ( 8.250000000000005329, 7.250000000000000888, -20.50000000000000000 ) ) ;
#65843=VERTEX_POINT ( 'NONE', #13694 ) ;
#65846=EDGE_LOOP ( 'NONE', ( #45737, #7089, #3749, #35099, #62966, #67131, #58842, #67749 ) ) ;
#65851=CYLINDRICAL_SURFACE ( 'NONE', #35724, 0.1999999999999996503 ) ;
#65855=ORIENTED_EDGE ( 'NONE', *, *, #41455, .F. ) ;
#65861=AXIS2_PLACEMENT_3D ( 'NONE', #44919, #55874, #7428 ) ;
#65869=EDGE_CURVE ( 'NONE', #29168, #47564, #31969, .T. ) ;
#65876=DIRECTION ( 'NONE',  ( 0.000000000000000000, 1.000000000000000000, -0.000000000000000000 ) ) ;
#65882=DIRECTION ( 'NONE',  ( -1.000000000000000000, 0.000000000000000000, 0.000000000000000000 ) ) ;
#65884=CARTESIAN_POINT ( 'NONE',  ( 0.000000000000000000, -8.249999999999998224, -17.00000000000000000 ) ) ;
#65888=CARTESIAN_POINT ( 'NONE',  ( -7.250000000000000000, -7.449999999999998401, -22.50000000000000000 ) ) ;
#65893=ORIENTED_EDGE ( 'NONE', *, *, #55021, .F. ) ;
#65904=EDGE_CURVE ( 'NONE', #68595, #8070, #15800, .T. ) ;
#65905=DIRECTION ( 'NONE',  ( -1.000000000000000000, 0.000000000000000000, 0.000000000000000000 ) ) ;
#65907=VECTOR ( 'NONE', #45348, 1000.000000000000000 ) ;
#65912=ORIENTED_EDGE ( 'NONE', *, *, #49100, .T. ) ;
#65914=AXIS2_PLACEMENT_3D ( 'NONE', #60155, #42858, #43553 ) ;
#65923=DIRECTION ( 'NONE',  ( 1.000000000000000000, -5.981805089575196197E-17, 0.000000000000000000 ) ) ;
#65931=ORIENTED_EDGE ( 'NONE', *, *, #36789, .T. ) ;
#65946=EDGE_CURVE ( 'NONE', #20828, #42371, #4159, .T. ) ;
#65948=CARTESIAN_POINT ( 'NONE',  ( 7.250000000000005329, 7.250000000000000888, -16.00000000000000000 ) ) ;
#65953=LINE ( 'NONE', #18213, #60341 ) ;
#65955=ADVANCED_FACE ( 'NONE', ( #48675, #9814 ), #57879, .F. ) ;
#65969=VECTOR ( 'NONE', #8144, 1000.000000000000000 ) ;
#65992=ORIENTED_EDGE ( 'NONE', *, *, #29900, .F. ) ;
#65993=CARTESIAN_POINT ( 'NONE',  ( 6.500000000000002665, 6.500000000000000888, 0.000000000000000000 ) ) ;
#66000=EDGE_CURVE ( 'NONE', #56941, #41772, #1274, .T. ) ;
#66003=CARTESIAN_POINT ( 'NONE',  ( 7.250000000000005329, 7.250000000000000888, -19.00000000000000000 ) ) ;
#66009=CIRCLE ( 'NONE', #35530, 1.000000000000000000 ) ;
#66015=CARTESIAN_POINT ( 'NONE',  ( -7.250000000000001776, -7.249999999999998224, -26.00000000000001066 ) ) ;
#66018=ADVANCED_FACE ( 'NONE', ( #16843 ), #22153, .T. ) ;
#66020=DIRECTION ( 'NONE',  ( -1.000000000000000000, 0.000000000000000000, 0.000000000000000000 ) ) ;
#66021=ORIENTED_EDGE ( 'NONE', *, *, #62422, .T. ) ;
#66028=AXIS2_PLACEMENT_3D ( 'NONE', #47259, #58574, #36638 ) ;
#66037=DIRECTION ( 'NONE',  ( -1.000000000000000000, 0.000000000000000000, -0.000000000000000000 ) ) ;
#66040=EDGE_CURVE ( 'NONE', #31960, #17879, #52355, .T. ) ;
#66045=ORIENTED_EDGE ( 'NONE', *, *, #3354, .F. ) ;
#66058=VERTEX_POINT ( 'NONE', #59634 ) ;
#66060=LINE ( 'NONE', #22262, #64299 ) ;
#66067=DIRECTION ( 'NONE',  ( 1.000000000000000000, -0.000000000000000000, 0.000000000000000000 ) ) ;
#66073=VERTEX_POINT ( 'NONE', #6911 ) ;
#66074=EDGE_CURVE ( 'NONE', #26429, #27857, #50403, .T. ) ;
#66080=ORIENTED_EDGE ( 'NONE', *, *, #9253, .T. ) ;
#66108=DIRECTION ( 'NONE',  ( -0.000000000000000000, 0.000000000000000000, 1.000000000000000000 ) ) ;
#66109=DIRECTION ( 'NONE',  ( 0.000000000000000000, 0.000000000000000000, 1.000000000000000000 ) ) ;
#66113=AXIS2_PLACEMENT_3D ( 'NONE', #26113, #68890, #52991 ) ;
#66114=FACE_OUTER_BOUND ( 'NONE', #19442, .T. ) ;
#66117=CARTESIAN_POINT ( 'NONE',  ( 7.250000000000005329, -7.249999999999998224, -26.00000000000001066 ) ) ;
#66126=ORIENTED_EDGE ( 'NONE', *, *, #7950, .T. ) ;
#66128=DIRECTION ( 'NONE',  ( -1.000000000000000000, 0.000000000000000000, 0.000000000000000000 ) ) ;
#66129=VERTEX_POINT ( 'NONE', #56397 ) ;
#66130=CARTESIAN_POINT ( 'NONE',  ( -7.250000000000000888, 7.250000000000001776, -8.500000000000000000 ) ) ;
#66131=CARTESIAN_POINT ( 'NONE',  ( -7.250000000000000888, 7.450000000000003730, -23.00000000000000000 ) ) ;
#66135=LINE ( 'NONE', #6733, #64366 ) ;
#66136=EDGE_CURVE ( 'NONE', #6447, #13636, #46685, .T. ) ;
#66141=VECTOR ( 'NONE', #65271, 1000.000000000000000 ) ;
#66147=VECTOR ( 'NONE', #11863, 1000.000000000000000 ) ;
#66151=DIRECTION ( 'NONE',  ( 0.000000000000000000, 0.000000000000000000, 1.000000000000000000 ) ) ;
#66152=VERTEX_POINT ( 'NONE', #24586 ) ;
#66155=AXIS2_PLACEMENT_3D ( 'NONE', #52018, #36814, #30092 ) ;
#66156=CARTESIAN_POINT ( 'NONE',  ( 7.250000000000005329, 8.250000000000001776, -19.50000000000000000 ) ) ;
#66164=PLANE ( 'NONE',  #33460 ) ;
#66167=ORIENTED_EDGE ( 'NONE', *, *, #30133, .F. ) ;
#66176=ORIENTED_EDGE ( 'NONE', *, *, #45456, .T. ) ;
#66190=ORIENTED_EDGE ( 'NONE', *, *, #38701, .F. ) ;
#66192=CIRCLE ( 'NONE', #17631, 1.000000000000000000 ) ;
#66195=ORIENTED_EDGE ( 'NONE', *, *, #64884, .F. ) ;
#66205=ORIENTED_EDGE ( 'NONE', *, *, #17258, .T. ) ;
#66213=DIRECTION ( 'NONE',  ( -1.000000000000000000, 0.000000000000000000, 0.000000000000000000 ) ) ;
#66233=CARTESIAN_POINT ( 'NONE',  ( 4.456444791733522252E-16, 7.450000000000002842, -24.50000000000000000 ) ) ;
#66246=VECTOR ( 'NONE', #7062, 1000.000000000000000 ) ;
#66253=AXIS2_PLACEMENT_3D ( 'NONE', #33579, #39230, #29655 ) ;
#66254=ORIENTED_EDGE ( 'NONE', *, *, #46000, .F. ) ;
#66258=AXIS2_PLACEMENT_3D ( 'NONE', #65948, #39088, #23522 ) ;
#66268=ORIENTED_EDGE ( 'NONE', *, *, #20370, .T. ) ;
#66272=EDGE_LOOP ( 'NONE', ( #1961, #63328 ) ) ;
#66273=ORIENTED_EDGE ( 'NONE', *, *, #21388, .F. ) ;
#66278=VERTEX_POINT ( 'NONE', #47888 ) ;
#66291=CARTESIAN_POINT ( 'NONE',  ( -8.689999999999999503, 8.750000000000000000, -7.000000000000000000 ) ) ;
#66293=LINE ( 'NONE', #23146, #66141 ) ;
#66322=LINE ( 'NONE', #39430, #32791 ) ;
#66325=DIRECTION ( 'NONE',  ( -1.000000000000000000, 0.000000000000000000, 0.000000000000000000 ) ) ;
#66326=DIRECTION ( 'NONE',  ( 1.000000000000000000, 0.000000000000000000, 0.000000000000000000 ) ) ;
#66339=FACE_OUTER_BOUND ( 'NONE', #59090, .T. ) ;
#66346=VERTEX_POINT ( 'NONE', #64514 ) ;
#66351=VECTOR ( 'NONE', #59608, 1000.000000000000000 ) ;
#66362=ORIENTED_EDGE ( 'NONE', *, *, #17512, .F. ) ;
#66363=ORIENTED_EDGE ( 'NONE', *, *, #32220, .F. ) ;
#66367=LINE ( 'NONE', #3064, #51844 ) ;
#66369=EDGE_CURVE ( 'NONE', #66152, #28918, #1522, .T. ) ;
#66374=LINE ( 'NONE', #33500, #16659 ) ;
#66390=CARTESIAN_POINT ( 'NONE',  ( -7.250000000000000888, 8.250000000000001776, -26.00000000000001066 ) ) ;
#66411=ADVANCED_FACE ( 'NONE', ( #17795 ), #5813, .F. ) ;
#66414=DIRECTION ( 'NONE',  ( 0.000000000000000000, 1.000000000000000000, 0.000000000000000000 ) ) ;
#66426=CARTESIAN_POINT ( 'NONE',  ( -7.250000000000000888, 7.450000000000003730, -11.50000000000000000 ) ) ;
#66435=VERTEX_POINT ( 'NONE', #43636 ) ;
#66438=EDGE_CURVE ( 'NONE', #30263, #6680, #38336, .T. ) ;
#66444=LINE ( 'NONE', #55151, #40987 ) ;
#66445=FACE_OUTER_BOUND ( 'NONE', #60867, .T. ) ;
#66449=ADVANCED_FACE ( 'NONE', ( #22422 ), #56665, .T. ) ;
#66453=LINE ( 'NONE', #18004, #53302 ) ;
#66461=CYLINDRICAL_SURFACE ( 'NONE', #5971, 0.2000000000000005107 ) ;
#66462=ORIENTED_EDGE ( 'NONE', *, *, #47380, .F. ) ;
#66463=DIRECTION ( 'NONE',  ( 1.000000000000000000, 0.000000000000000000, 0.000000000000000000 ) ) ;
#66469=ORIENTED_EDGE ( 'NONE', *, *, #66920, .F. ) ;
#66475=ORIENTED_EDGE ( 'NONE', *, *, #62382, .T. ) ;
#66478=CARTESIAN_POINT ( 'NONE',  ( 8.250000000000005329, 0.000000000000000000, -14.50000000000000000 ) ) ;
#66481=EDGE_CURVE ( 'NONE', #15934, #60538, #43347, .T. ) ;
#66486=EDGE_CURVE ( 'NONE', #34907, #67031, #8217, .T. ) ;
#66493=ORIENTED_EDGE ( 'NONE', *, *, #26846, .F. ) ;
#66499=DIRECTION ( 'NONE',  ( 0.000000000000000000, 0.000000000000000000, -1.000000000000000000 ) ) ;
#66500=EDGE_CURVE ( 'NONE', #25548, #33741, #7525, .T. ) ;
#66507=DIRECTION ( 'NONE',  ( 1.000000000000000000, 0.000000000000000000, 0.000000000000000000 ) ) ;
#66508=ORIENTED_EDGE ( 'NONE', *, *, #23920, .T. ) ;
#66513=EDGE_CURVE ( 'NONE', #52692, #22594, #46401, .T. ) ;
#66514=VECTOR ( 'NONE', #12104, 1000.000000000000000 ) ;
#66516=ADVANCED_FACE ( 'NONE', ( #7865 ), #56317, .F. ) ;
#66521=DIRECTION ( 'NONE',  ( -1.000000000000000000, 0.000000000000000000, 0.000000000000000000 ) ) ;
#66526=CARTESIAN_POINT ( 'NONE',  ( -7.250000000000001776, -7.249999999999998224, -15.50000000000000000 ) ) ;
#66532=DIRECTION ( 'NONE',  ( 0.000000000000000000, 0.000000000000000000, 1.000000000000000000 ) ) ;
#66539=DIRECTION ( 'NONE',  ( -0.000000000000000000, -0.000000000000000000, 1.000000000000000000 ) ) ;
#66543=DIRECTION ( 'NONE',  ( -1.000000000000000000, 0.000000000000000000, 0.000000000000000000 ) ) ;
#66546=DIRECTION ( 'NONE',  ( -0.000000000000000000, -0.000000000000000000, 1.000000000000000000 ) ) ;
#66548=DIRECTION ( 'NONE',  ( 0.000000000000000000, 0.000000000000000000, 1.000000000000000000 ) ) ;
#66555=CYLINDRICAL_SURFACE ( 'NONE', #6521, 1.000000000000000000 ) ;
#66556=LINE ( 'NONE', #1179, #17114 ) ;
#66561=VECTOR ( 'NONE', #52137, 1000.000000000000000 ) ;
#66562=CARTESIAN_POINT ( 'NONE',  ( -7.250000000000000888, 7.250000000000001776, -11.50000000000000000 ) ) ;
#66566=FACE_BOUND ( 'NONE', #48097, .T. ) ;
#66595=CARTESIAN_POINT ( 'NONE',  ( 8.250000000000005329, -7.249999999999998224, -13.50000000000000178 ) ) ;
#66599=DIRECTION ( 'NONE',  ( -0.000000000000000000, -0.000000000000000000, 1.000000000000000000 ) ) ;
#66602=ORIENTED_EDGE ( 'NONE', *, *, #37098, .F. ) ;
#66608=ORIENTED_EDGE ( 'NONE', *, *, #29253, .F. ) ;
#66616=VERTEX_POINT ( 'NONE', #10334 ) ;
#66618=EDGE_CURVE ( 'NONE', #27416, #11776, #33213, .T. ) ;
#66620=CARTESIAN_POINT ( 'NONE',  ( -7.450000000000001954, 0.000000000000000000, -7.500000000000000000 ) ) ;
#66631=DIRECTION ( 'NONE',  ( 0.000000000000000000, -0.000000000000000000, 1.000000000000000000 ) ) ;
#66633=AXIS2_PLACEMENT_3D ( 'NONE', #38368, #37331, #32373 ) ;
#66647=DIRECTION ( 'NONE',  ( 0.000000000000000000, 0.000000000000000000, 1.000000000000000000 ) ) ;
#66650=EDGE_CURVE ( 'NONE', #63937, #30915, #47901, .T. ) ;
#66657=EDGE_CURVE ( 'NONE', #14316, #17827, #58101, .T. ) ;
#66663=VECTOR ( 'NONE', #58478, 1000.000000000000000 ) ;
#66667=EDGE_CURVE ( 'NONE', #2145, #47295, #36496, .T. ) ;
#66673=FACE_OUTER_BOUND ( 'NONE', #4669, .T. ) ;
#66678=LINE ( 'NONE', #49396, #11444 ) ;
#66681=CARTESIAN_POINT ( 'NONE',  ( 7.250000000000005329, -7.249999999999998224, -13.50000000000000178 ) ) ;
#66682=AXIS2_PLACEMENT_3D ( 'NONE', #29644, #46960, #56182 ) ;
#66683=ORIENTED_EDGE ( 'NONE', *, *, #2016, .F. ) ;
#66693=LINE ( 'NONE', #40870, #34505 ) ;
#66695=DIRECTION ( 'NONE',  ( 0.000000000000000000, 0.000000000000000000, 1.000000000000000000 ) ) ;
#66696=ORIENTED_EDGE ( 'NONE', *, *, #31426, .T. ) ;
#66712=VERTEX_POINT ( 'NONE', #5393 ) ;
#66713=DIRECTION ( 'NONE',  ( -0.000000000000000000, 0.000000000000000000, 1.000000000000000000 ) ) ;
#66716=DIRECTION ( 'NONE',  ( 0.000000000000000000, 0.000000000000000000, 1.000000000000000000 ) ) ;
#66717=CARTESIAN_POINT ( 'NONE',  ( 7.250000000000005329, 7.250000000000000888, -10.00000000000000000 ) ) ;
#66720=CARTESIAN_POINT ( 'NONE',  ( -9.690000000000001279, 10.50000000000000000, -4.250000000000000000 ) ) ;
#66723=CIRCLE ( 'NONE', #30605, 1.000000000000000000 ) ;
#66733=DIRECTION ( 'NONE',  ( -0.000000000000000000, 1.000000000000000000, 0.000000000000000000 ) ) ;
#66737=AXIS2_PLACEMENT_3D ( 'NONE', #20631, #36923, #47855 ) ;
#66739=DIRECTION ( 'NONE',  ( 0.000000000000000000, 1.000000000000000000, 0.000000000000000000 ) ) ;
#66740=VECTOR ( 'NONE', #26205, 1000.000000000000000 ) ;
#66741=ORIENTED_EDGE ( 'NONE', *, *, #65904, .T. ) ;
#66746=DIRECTION ( 'NONE',  ( -0.000000000000000000, -0.000000000000000000, 1.000000000000000000 ) ) ;
#66747=AXIS2_PLACEMENT_3D ( 'NONE', #8921, #51722, #20585 ) ;
#66749=DIRECTION ( 'NONE',  ( 8.951101527228104953E-17, -1.000000000000000000, 0.000000000000000000 ) ) ;
#66751=VERTEX_POINT ( 'NONE', #49546 ) ;
#66752=ORIENTED_EDGE ( 'NONE', *, *, #44828, .T. ) ;
#66754=EDGE_CURVE ( 'NONE', #28918, #67361, #30989, .T. ) ;
#66772=DIRECTION ( 'NONE',  ( 0.000000000000000000, 0.000000000000000000, 1.000000000000000000 ) ) ;
#66774=VECTOR ( 'NONE', #37336, 1000.000000000000000 ) ;
#66782=CARTESIAN_POINT ( 'NONE',  ( 7.250000000000005329, 7.250000000000000888, -13.00000000000000178 ) ) ;
#66785=ORIENTED_EDGE ( 'NONE', *, *, #20499, .F. ) ;
#66790=ORIENTED_EDGE ( 'NONE', *, *, #39087, .T. ) ;
#66791=LINE ( 'NONE', #40626, #45558 ) ;
#66794=ADVANCED_FACE ( 'NONE', ( #38256 ), #80, .F. ) ;
#66800=ADVANCED_FACE ( 'NONE', ( #65467 ), #16328, .F. ) ;
#66810=VECTOR ( 'NONE', #49527, 1000.000000000000000 ) ;
#66813=DIRECTION ( 'NONE',  ( -1.000000000000000000, 0.000000000000000000, 0.000000000000000000 ) ) ;
#66817=CARTESIAN_POINT ( 'NONE',  ( -7.450000000000001954, 7.250000000000000000, -13.50000000000000178 ) ) ;
#66818=CARTESIAN_POINT ( 'NONE',  ( 8.250000000000005329, 7.250000000000000888, -13.50000000000000178 ) ) ;
#66821=ORIENTED_EDGE ( 'NONE', *, *, #59173, .T. ) ;
#66827=VERTEX_POINT ( 'NONE', #22674 ) ;
#66829=ADVANCED_FACE ( 'NONE', ( #44223 ), #65803, .T. ) ;
#66830=AXIS2_PLACEMENT_3D ( 'NONE', #55101, #6645, #44810 ) ;
#66838=CIRCLE ( 'NONE', #54454, 0.2000000000000005107 ) ;
#66841=ORIENTED_EDGE ( 'NONE', *, *, #1057, .F. ) ;
#66844=LINE ( 'NONE', #50932, #24060 ) ;
#66847=PLANE ( 'NONE',  #69372 ) ;
#66853=ORIENTED_EDGE ( 'NONE', *, *, #46232, .T. ) ;
#66861=VECTOR ( 'NONE', #15548, 1000.000000000000000 ) ;
#66862=DIRECTION ( 'NONE',  ( 1.000000000000000000, 0.000000000000000000, 0.000000000000000000 ) ) ;
#66863=DIRECTION ( 'NONE',  ( -1.794541526872559352E-16, -1.000000000000000000, 0.000000000000000000 ) ) ;
#66866=EDGE_LOOP ( 'NONE', ( #12748, #58897, #55975, #27851 ) ) ;
#66870=CARTESIAN_POINT ( 'NONE',  ( -7.250000000000000888, 7.250000000000001776, -24.00000000000000000 ) ) ;
#66873=ORIENTED_EDGE ( 'NONE', *, *, #55887, .F. ) ;
#66885=CARTESIAN_POINT ( 'NONE',  ( 7.450000000000006395, 7.250000000000000888, -16.50000000000000000 ) ) ;
#66888=DIRECTION ( 'NONE',  ( -1.000000000000000000, 0.000000000000000000, 0.000000000000000000 ) ) ;
#66889=DIRECTION ( 'NONE',  ( -0.000000000000000000, -0.000000000000000000, 1.000000000000000000 ) ) ;
#66892=ADVANCED_FACE ( 'NONE', ( #34298 ), #19101, .F. ) ;
#66901=CARTESIAN_POINT ( 'NONE',  ( 7.450000000000003730, -7.249999999999997335, -18.00000000000000000 ) ) ;
#66903=CARTESIAN_POINT ( 'NONE',  ( 7.450000000000003730, -7.249999999999997335, -20.50000000000000000 ) ) ;
#66907=CYLINDRICAL_SURFACE ( 'NONE', #21454, 1.000000000000000000 ) ;
#66911=AXIS2_PLACEMENT_3D ( 'NONE', #1265, #48667, #49374 ) ;
#66916=AXIS2_PLACEMENT_3D ( 'NONE', #58014, #31161, #13826 ) ;
#66919=VERTEX_POINT ( 'NONE', #13086 ) ;
#66920=EDGE_CURVE ( 'NONE', #29528, #51208, #17455, .T. ) ;
#66925=EDGE_LOOP ( 'NONE', ( #2739, #53684, #40049, #59718 ) ) ;
#66927=AXIS2_PLACEMENT_3D ( 'NONE', #54555, #1476, #65840 ) ;
#66930=DIRECTION ( 'NONE',  ( 1.000000000000000000, 0.000000000000000000, 0.000000000000000000 ) ) ;
#66931=CARTESIAN_POINT ( 'NONE',  ( 4.456444791733522252E-16, 7.450000000000002842, -16.50000000000000000 ) ) ;
#66939=AXIS2_PLACEMENT_3D ( 'NONE', #33314, #28009, #17382 ) ;
#66973=ADVANCED_FACE ( 'NONE', ( #10249 ), #69291, .F. ) ;
#66979=EDGE_CURVE ( 'NONE', #15537, #9996, #20851, .T. ) ;
#66981=EDGE_CURVE ( 'NONE', #32501, #25255, #8844, .T. ) ;
#66982=DIRECTION ( 'NONE',  ( 0.000000000000000000, 1.000000000000000000, 0.000000000000000000 ) ) ;
#66985=EDGE_CURVE ( 'NONE', #12173, #37776, #53617, .T. ) ;
#66996=DIRECTION ( 'NONE',  ( -1.000000000000000000, 0.000000000000000000, -0.000000000000000000 ) ) ;
#67022=VECTOR ( 'NONE', #2582, 1000.000000000000000 ) ;
#67023=ORIENTED_EDGE ( 'NONE', *, *, #33674, .T. ) ;
#67025=VERTEX_POINT ( 'NONE', #37130 ) ;
#67027=CARTESIAN_POINT ( 'NONE',  ( 7.450000000000004619, -1.336933437520057563E-15, -16.50000000000000000 ) ) ;
#67031=VERTEX_POINT ( 'NONE', #9202 ) ;
#67037=PLANE ( 'NONE',  #30505 ) ;
#67039=VERTEX_POINT ( 'NONE', #30767 ) ;
#67043=DIRECTION ( 'NONE',  ( -1.000000000000000000, 0.000000000000000000, 0.000000000000000000 ) ) ;
#67045=VECTOR ( 'NONE', #66647, 1000.000000000000000 ) ;
#67047=VERTEX_POINT ( 'NONE', #69656 ) ;
#67049=EDGE_CURVE ( 'NONE', #23968, #16718, #31045, .T. ) ;
#67051=CARTESIAN_POINT ( 'NONE',  ( 8.250000000000005329, 8.250000000000001776, -26.00000000000001066 ) ) ;
#67056=AXIS2_PLACEMENT_3D ( 'NONE', #6173, #64881, #59573 ) ;
#67066=VECTOR ( 'NONE', #4564, 1000.000000000000000 ) ;
#67072=DIRECTION ( 'NONE',  ( -1.794541526872559352E-16, -1.000000000000000000, 0.000000000000000000 ) ) ;
#67106=ORIENTED_EDGE ( 'NONE', *, *, #69320, .T. ) ;
#67112=CARTESIAN_POINT ( 'NONE',  ( -8.250000000000001776, 7.250000000000000888, -8.500000000000000000 ) ) ;
#67123=ORIENTED_EDGE ( 'NONE', *, *, #62735, .F. ) ;
#67129=DIRECTION ( 'NONE',  ( 0.000000000000000000, -1.000000000000000000, 0.000000000000000000 ) ) ;
#67131=ORIENTED_EDGE ( 'NONE', *, *, #17407, .F. ) ;
#67132=ORIENTED_EDGE ( 'NONE', *, *, #16501, .F. ) ;
#67142=VERTEX_POINT ( 'NONE', #33192 ) ;
#67146=FACE_OUTER_BOUND ( 'NONE', #40945, .T. ) ;
#67147=ORIENTED_EDGE ( 'NONE', *, *, #48549, .F. ) ;
#67150=DIRECTION ( 'NONE',  ( 0.000000000000000000, 0.000000000000000000, 1.000000000000000000 ) ) ;
#67155=CARTESIAN_POINT ( 'NONE',  ( 7.250000000000005329, 7.250000000000000888, -20.50000000000000000 ) ) ;
#67156=ORIENTED_EDGE ( 'NONE', *, *, #52864, .F. ) ;
#67176=AXIS2_PLACEMENT_3D ( 'NONE', #24293, #30999, #4142 ) ;
#67177=ORIENTED_EDGE ( 'NONE', *, *, #32068, .T. ) ;
#67179=ORIENTED_EDGE ( 'NONE', *, *, #65315, .T. ) ;
#67191=ORIENTED_EDGE ( 'NONE', *, *, #7408, .F. ) ;
#67192=ORIENTED_EDGE ( 'NONE', *, *, #19743, .T. ) ;
#67196=DIRECTION ( 'NONE',  ( -1.000000000000000000, 0.000000000000000000, 0.000000000000000000 ) ) ;
#67205=ORIENTED_EDGE ( 'NONE', *, *, #16501, .T. ) ;
#67214=CARTESIAN_POINT ( 'NONE',  ( 7.250000000000005329, -7.249999999999998224, -26.00000000000001066 ) ) ;
#67217=VERTEX_POINT ( 'NONE', #23966 ) ;
#67223=ORIENTED_EDGE ( 'NONE', *, *, #12644, .T. ) ;
#67234=ADVANCED_FACE ( 'NONE', ( #39866 ), #39524, .T. ) ;
#67244=PLANE ( 'NONE',  #9804 ) ;
#67248=DIRECTION ( 'NONE',  ( -1.000000000000000000, 0.000000000000000000, 0.000000000000000000 ) ) ;
#67262=ORIENTED_EDGE ( 'NONE', *, *, #14644, .F. ) ;
#67267=DIRECTION ( 'NONE',  ( 0.000000000000000000, 0.000000000000000000, 1.000000000000000000 ) ) ;
#67270=PLANE ( 'NONE',  #19475 ) ;
#67275=DIRECTION ( 'NONE',  ( -0.000000000000000000, -0.000000000000000000, 1.000000000000000000 ) ) ;
#67277=AXIS2_PLACEMENT_3D ( 'NONE', #59978, #65640, #48342 ) ;
#67281=CIRCLE ( 'NONE', #15309, 1.000000000000000000 ) ;
#67284=ORIENTED_EDGE ( 'NONE', *, *, #42578, .F. ) ;
#67287=EDGE_LOOP ( 'NONE', ( #66190, #48528, #42015, #54437 ) ) ;
#67293=DIRECTION ( 'NONE',  ( 0.000000000000000000, 0.000000000000000000, -1.000000000000000000 ) ) ;
#67295=AXIS2_PLACEMENT_3D ( 'NONE', #69625, #22564, #12965 ) ;
#67297=DIRECTION ( 'NONE',  ( -1.000000000000000000, 0.000000000000000000, 0.000000000000000000 ) ) ;
#67301=ORIENTED_EDGE ( 'NONE', *, *, #39131, .T. ) ;
#67303=CARTESIAN_POINT ( 'NONE',  ( -8.250000000000000000, 7.250000000000001776, -22.00000000000000000 ) ) ;
#67314=VERTEX_POINT ( 'NONE', #15736 ) ;
#67316=EDGE_CURVE ( 'NONE', #10256, #6549, #29917, .T. ) ;
#67317=ORIENTED_EDGE ( 'NONE', *, *, #57807, .F. ) ;
#67320=LINE ( 'NONE', #3667, #41788 ) ;
#67322=ORIENTED_EDGE ( 'NONE', *, *, #27268, .T. ) ;
#67323=VERTEX_POINT ( 'NONE', #20677 ) ;
#67329=ADVANCED_FACE ( 'NONE', ( #58878 ), #48266, .F. ) ;
#67337=CARTESIAN_POINT ( 'NONE',  ( -7.250000000000000888, 7.450000000000003730, -15.00000000000000000 ) ) ;
#67339=AXIS2_PLACEMENT_3D ( 'NONE', #48289, #21408, #32029 ) ;
#67342=CARTESIAN_POINT ( 'NONE',  ( -7.250000000000000888, 7.250000000000001776, -13.50000000000000178 ) ) ;
#67346=CARTESIAN_POINT ( 'NONE',  ( -7.250000000000000888, -8.249999999999998224, -7.500000000000000000 ) ) ;
#67361=VERTEX_POINT ( 'NONE', #41900 ) ;
#67371=EDGE_LOOP ( 'NONE', ( #40587, #5185, #38433, #6177, #12153, #45067, #64386, #28307 ) ) ;
#67372=DIRECTION ( 'NONE',  ( -1.000000000000000000, 0.000000000000000000, 0.000000000000000000 ) ) ;
#67386=CIRCLE ( 'NONE', #50420, 0.2000000000000005107 ) ;
#67393=FACE_OUTER_BOUND ( 'NONE', #36005, .T. ) ;
#67395=AXIS2_PLACEMENT_3D ( 'NONE', #61217, #45660, #13492 ) ;
#67401=LINE ( 'NONE', #28846, #53135 ) ;
#67415=EDGE_LOOP ( 'NONE', ( #47405, #54146 ) ) ;
#67435=FACE_OUTER_BOUND ( 'NONE', #26946, .T. ) ;
#67436=CARTESIAN_POINT ( 'NONE',  ( -8.250000000000001776, -7.249999999999998224, -19.50000000000000000 ) ) ;
#67439=CARTESIAN_POINT ( 'NONE',  ( -9.750000000000001776, 9.690000000000001279, -4.250000000000000000 ) ) ;
#67462=AXIS2_PLACEMENT_3D ( 'NONE', #36039, #47350, #53024 ) ;
#67465=CARTESIAN_POINT ( 'NONE',  ( 7.250000000000005329, -7.249999999999998224, -10.00000000000000000 ) ) ;
#67471=EDGE_LOOP ( 'NONE', ( #29422, #9046, #19532, #1474 ) ) ;
#67478=CIRCLE ( 'NONE', #59606, 1.000000000000003553 ) ;
#67482=LINE ( 'NONE', #43099, #53120 ) ;
#67490=LINE ( 'NONE', #3821, #20676 ) ;
#67502=CARTESIAN_POINT ( 'NONE',  ( -7.750000000000001776, -7.348062532927999158, -5.000000000000000000 ) ) ;
#67503=DIRECTION ( 'NONE',  ( -0.000000000000000000, -0.000000000000000000, -1.000000000000000000 ) ) ;
#67504=ORIENTED_EDGE ( 'NONE', *, *, #13507, .F. ) ;
#67511=CARTESIAN_POINT ( 'NONE',  ( 7.450000000000006395, 7.250000000000000888, -10.00000000000000000 ) ) ;
#67520=FACE_OUTER_BOUND ( 'NONE', #1765, .T. ) ;
#67522=DIRECTION ( 'NONE',  ( 1.000000000000000000, -0.000000000000000000, 0.000000000000000000 ) ) ;
#67557=LINE ( 'NONE', #36422, #58956 ) ;
#67561=DIRECTION ( 'NONE',  ( -1.794541526872559352E-16, -1.000000000000000000, 0.000000000000000000 ) ) ;
#67567=DIRECTION ( 'NONE',  ( -1.000000000000000000, 1.794541526872559352E-16, 0.000000000000000000 ) ) ;
#67571=ORIENTED_EDGE ( 'NONE', *, *, #50032, .F. ) ;
#67581=LINE ( 'NONE', #20184, #17358 ) ;
#67606=FACE_OUTER_BOUND ( 'NONE', #46622, .T. ) ;
#67614=CARTESIAN_POINT ( 'NONE',  ( -7.250000000000000888, 7.250000000000001776, -10.50000000000000000 ) ) ;
#67622=EDGE_LOOP ( 'NONE', ( #51213, #47293, #57044, #12709 ) ) ;
#67625=LINE ( 'NONE', #29092, #17752 ) ;
#67626=CYLINDRICAL_SURFACE ( 'NONE', #11610, 0.2000000000000005107 ) ;
#67628=VECTOR ( 'NONE', #53469, 1000.000000000000000 ) ;
#67629=DIRECTION ( 'NONE',  ( 0.000000000000000000, 0.000000000000000000, 1.000000000000000000 ) ) ;
#67631=ORIENTED_EDGE ( 'NONE', *, *, #11575, .F. ) ;
#67632=ORIENTED_EDGE ( 'NONE', *, *, #31079, .T. ) ;
#67634=DIRECTION ( 'NONE',  ( -1.000000000000000000, 0.000000000000000000, 0.000000000000000000 ) ) ;
#67639=FACE_OUTER_BOUND ( 'NONE', #47743, .T. ) ;
#67645=DIRECTION ( 'NONE',  ( 0.000000000000000000, 0.000000000000000000, 1.000000000000000000 ) ) ;
#67646=EDGE_LOOP ( 'NONE', ( #65931, #55652, #13797, #20355 ) ) ;
#67655=EDGE_LOOP ( 'NONE', ( #3726, #37021, #43173, #41356 ) ) ;
#67656=ORIENTED_EDGE ( 'NONE', *, *, #54155, .T. ) ;
#67659=EDGE_LOOP ( 'NONE', ( #34484, #19203, #42711, #18320 ) ) ;
#67662=CIRCLE ( 'NONE', #10088, 1.000000000000000000 ) ;
#67665=LINE ( 'NONE', #19569, #27756 ) ;
#67676=CARTESIAN_POINT ( 'NONE',  ( 7.250000000000005329, 7.250000000000000888, -9.000000000000001776 ) ) ;
#67677=FACE_OUTER_BOUND ( 'NONE', #49762, .T. ) ;
#67678=EDGE_CURVE ( 'NONE', #33741, #6284, #47131, .T. ) ;
#67695=VERTEX_POINT ( 'NONE', #20248 ) ;
#67699=FACE_OUTER_BOUND ( 'NONE', #2161, .T. ) ;
#67706=DIRECTION ( 'NONE',  ( -1.000000000000000000, 0.000000000000000000, 0.000000000000000000 ) ) ;
#67711=VECTOR ( 'NONE', #27128, 1000.000000000000000 ) ;
#67715=DIRECTION ( 'NONE',  ( -1.000000000000000000, 0.000000000000000000, 0.000000000000000000 ) ) ;
#67717=VERTEX_POINT ( 'NONE', #10005 ) ;
#67718=ADVANCED_FACE ( 'NONE', ( #47470 ), #58449, .F. ) ;
#67724=ORIENTED_EDGE ( 'NONE', *, *, #50520, .F. ) ;
#67725=EDGE_LOOP ( 'NONE', ( #17333, #52456 ) ) ;
#67727=EDGE_CURVE ( 'NONE', #13864, #35273, #42161, .T. ) ;
#67728=CARTESIAN_POINT ( 'NONE',  ( 7.450000000000006395, 7.250000000000000888, -22.50000000000000000 ) ) ;
#67731=CARTESIAN_POINT ( 'NONE',  ( -7.250000000000001776, -7.249999999999998224, -10.50000000000000000 ) ) ;
#67735=CARTESIAN_POINT ( 'NONE',  ( 7.450000000000003730, -7.249999999999997335, -22.50000000000000000 ) ) ;
#67746=AXIS2_PLACEMENT_3D ( 'NONE', #53252, #16802, #9762 ) ;
#67749=ORIENTED_EDGE ( 'NONE', *, *, #45257, .F. ) ;
#67750=ADVANCED_FACE ( 'NONE', ( #32256 ), #5407, .F. ) ;
#67764=DIRECTION ( 'NONE',  ( 0.000000000000000000, -0.000000000000000000, 1.000000000000000000 ) ) ;
#67778=ADVANCED_FACE ( 'NONE', ( #17037 ), #17727, .T. ) ;
#67781=AXIS2_PLACEMENT_3D ( 'NONE', #7752, #29314, #50886 ) ;
#67782=CYLINDRICAL_SURFACE ( 'NONE', #35222, 1.000000000000000000 ) ;
#67783=ORIENTED_EDGE ( 'NONE', *, *, #43642, .F. ) ;
#67785=FACE_OUTER_BOUND ( 'NONE', #54227, .T. ) ;
#67792=CARTESIAN_POINT ( 'NONE',  ( 8.689999999999999503, 8.750000000000000000, -5.000000000000000000 ) ) ;
#67795=ORIENTED_EDGE ( 'NONE', *, *, #35850, .T. ) ;
#67797=LINE ( 'NONE', #29604, #415 ) ;
#67798=ORIENTED_EDGE ( 'NONE', *, *, #47052, .F. ) ;
#67805=CARTESIAN_POINT ( 'NONE',  ( -8.250000000000001776, 0.000000000000000000, -8.500000000000000000 ) ) ;
#67813=ADVANCED_FACE ( 'NONE', ( #54185, #60159 ), #50936, .F. ) ;
#67815=ORIENTED_EDGE ( 'NONE', *, *, #60490, .F. ) ;
#67832=CARTESIAN_POINT ( 'NONE',  ( -7.250000000000000888, 7.250000000000001776, -23.50000000000000000 ) ) ;
#67834=ORIENTED_EDGE ( 'NONE', *, *, #3015, .T. ) ;
#67835=AXIS2_PLACEMENT_3D ( 'NONE', #44309, #38340, #877 ) ;
#67836=DIRECTION ( 'NONE',  ( 0.000000000000000000, 0.000000000000000000, -1.000000000000000000 ) ) ;
#67837=DIRECTION ( 'NONE',  ( 0.000000000000000000, 0.000000000000000000, -1.000000000000000000 ) ) ;
#67839=ORIENTED_EDGE ( 'NONE', *, *, #19092, .F. ) ;
#67846=CARTESIAN_POINT ( 'NONE',  ( 7.250000000000005329, 7.250000000000000888, -16.50000000000000000 ) ) ;
#67860=CARTESIAN_POINT ( 'NONE',  ( 8.250000000000005329, 7.250000000000000888, -12.50000000000000000 ) ) ;
#67861=EDGE_CURVE ( 'NONE', #21718, #35045, #62242, .T. ) ;
#67868=CARTESIAN_POINT ( 'NONE',  ( 7.450000000000003730, -7.249999999999997335, -16.50000000000000000 ) ) ;
#67883=FACE_OUTER_BOUND ( 'NONE', #12861, .T. ) ;
#67885=CARTESIAN_POINT ( 'NONE',  ( -7.250000000000000888, -8.249999999999998224, -26.00000000000001066 ) ) ;
#67891=ORIENTED_EDGE ( 'NONE', *, *, #67727, .T. ) ;
#67897=VERTEX_POINT ( 'NONE', #55897 ) ;
#67900=EDGE_CURVE ( 'NONE', #20521, #23324, #50313, .T. ) ;
#67906=DIRECTION ( 'NONE',  ( -1.000000000000000000, 0.000000000000000000, 0.000000000000000000 ) ) ;
#67908=LINE ( 'NONE', #14153, #39891 ) ;
#67930=CARTESIAN_POINT ( 'NONE',  ( -7.750000000000001776, -7.348062532927999158, -5.000000000000000000 ) ) ;
#67933=AXIS2_PLACEMENT_3D ( 'NONE', #17362, #66151, #1792 ) ;
#67934=EDGE_CURVE ( 'NONE', #17842, #16692, #2153, .T. ) ;
#67941=VECTOR ( 'NONE', #17690, 1000.000000000000000 ) ;
#67942=LINE ( 'NONE', #7826, #29388 ) ;
#67944=DIRECTION ( 'NONE',  ( -0.000000000000000000, 0.000000000000000000, 1.000000000000000000 ) ) ;
#67951=EDGE_CURVE ( 'NONE', #25681, #8234, #62588, .T. ) ;
#67968=AXIS2_PLACEMENT_3D ( 'NONE', #50883, #6381, #60456 ) ;
#67980=CARTESIAN_POINT ( 'NONE',  ( -6.749999999999998224, 7.750000000000001776, -5.000000000000000000 ) ) ;
#67985=AXIS2_PLACEMENT_3D ( 'NONE', #51643, #14146, #15216 ) ;
#67986=VERTEX_POINT ( 'NONE', #4619 ) ;
#67990=DIRECTION ( 'NONE',  ( -1.000000000000000000, 0.000000000000000000, 0.000000000000000000 ) ) ;
#67992=EDGE_CURVE ( 'NONE', #68319, #63525, #662, .T. ) ;
#67993=EDGE_CURVE ( 'NONE', #68976, #29522, #57646, .T. ) ;
#67998=ORIENTED_EDGE ( 'NONE', *, *, #55873, .F. ) ;
#68009=ORIENTED_EDGE ( 'NONE', *, *, #58543, .T. ) ;
#68011=CARTESIAN_POINT ( 'NONE',  ( 9.690000000000001279, -9.750000000000001776, -7.000000000000000000 ) ) ;
#68016=VECTOR ( 'NONE', #28200, 1000.000000000000000 ) ;
#68028=FACE_OUTER_BOUND ( 'NONE', #32583, .T. ) ;
#68032=EDGE_CURVE ( 'NONE', #47318, #31506, #25477, .T. ) ;
#68045=VERTEX_POINT ( 'NONE', #48094 ) ;
#68049=VECTOR ( 'NONE', #13124, 1000.000000000000000 ) ;
#68050=CARTESIAN_POINT ( 'NONE',  ( 7.250000000000005329, 7.250000000000000888, -17.50000000000000000 ) ) ;
#68054=FACE_OUTER_BOUND ( 'NONE', #36985, .T. ) ;
#68060=AXIS2_PLACEMENT_3D ( 'NONE', #57094, #2645, #34816 ) ;
#68065=VERTEX_POINT ( 'NONE', #37488 ) ;
#68068=CARTESIAN_POINT ( 'NONE',  ( 0.000000000000000000, -8.249999999999998224, -16.00000000000000000 ) ) ;
#68069=CARTESIAN_POINT ( 'NONE',  ( 7.250000000000005329, -7.249999999999998224, -26.00000000000001066 ) ) ;
#68072=ADVANCED_FACE ( 'NONE', ( #57996 ), #20516, .F. ) ;
#68073=CARTESIAN_POINT ( 'NONE',  ( 7.250000000000005329, -7.249999999999998224, -16.50000000000000000 ) ) ;
#68078=CARTESIAN_POINT ( 'NONE',  ( 7.250000000000005329, -7.249999999999998224, -26.00000000000001066 ) ) ;
#68080=CARTESIAN_POINT ( 'NONE',  ( -7.250000000000001776, -7.249999999999998224, -26.00000000000001066 ) ) ;
#68081=FACE_OUTER_BOUND ( 'NONE', #8947, .T. ) ;
#68088=ORIENTED_EDGE ( 'NONE', *, *, #3877, .T. ) ;
#68092=ORIENTED_EDGE ( 'NONE', *, *, #64860, .T. ) ;
#68093=EDGE_CURVE ( 'NONE', #63685, #13194, #24428, .T. ) ;
#68097=ORIENTED_EDGE ( 'NONE', *, *, #17853, .F. ) ;
#68107=EDGE_CURVE ( 'NONE', #26429, #3987, #9568, .T. ) ;
#68108=DIRECTION ( 'NONE',  ( 0.000000000000000000, 0.000000000000000000, 1.000000000000000000 ) ) ;
#68114=CARTESIAN_POINT ( 'NONE',  ( 7.450000000000004619, -1.336933437520057563E-15, -22.50000000000000000 ) ) ;
#68115=CARTESIAN_POINT ( 'NONE',  ( 0.000000000000000000, -8.249999999999998224, -25.00000000000000000 ) ) ;
#68121=DIRECTION ( 'NONE',  ( -1.794541526872559352E-16, -1.000000000000000000, 0.000000000000000000 ) ) ;
#68133=FACE_OUTER_BOUND ( 'NONE', #13091, .T. ) ;
#68149=ORIENTED_EDGE ( 'NONE', *, *, #34652, .T. ) ;
#68163=LINE ( 'NONE', #3814, #45664 ) ;
#68167=CARTESIAN_POINT ( 'NONE',  ( 0.000000000000000000, 0.000000000000000000, -18.00000000000000000 ) ) ;
#68171=PLANE ( 'NONE',  #60187 ) ;
#68178=EDGE_LOOP ( 'NONE', ( #11400, #63306, #59668, #34724 ) ) ;
#68179=DIRECTION ( 'NONE',  ( 1.000000000000000000, 0.000000000000000000, 0.000000000000000000 ) ) ;
#68194=VECTOR ( 'NONE', #47791, 1000.000000000000000 ) ;
#68207=DIRECTION ( 'NONE',  ( 0.000000000000000000, 0.000000000000000000, 1.000000000000000000 ) ) ;
#68220=EDGE_LOOP ( 'NONE', ( #28001, #34677, #2838, #5105 ) ) ;
#68222=DIRECTION ( 'NONE',  ( -0.000000000000000000, -0.000000000000000000, -1.000000000000000000 ) ) ;
#68224=AXIS2_PLACEMENT_3D ( 'NONE', #671, #22240, #60053 ) ;
#68233=CARTESIAN_POINT ( 'NONE',  ( 0.000000000000000000, -7.449999999999998401, -22.50000000000000000 ) ) ;
#68235=ORIENTED_EDGE ( 'NONE', *, *, #35033, .F. ) ;
#68237=DIRECTION ( 'NONE',  ( 1.000000000000000000, -5.981805089575194965E-17, 0.000000000000000000 ) ) ;
#68246=CARTESIAN_POINT ( 'NONE',  ( -7.250000000000000888, 7.250000000000001776, -26.00000000000001066 ) ) ;
#68252=CARTESIAN_POINT ( 'NONE',  ( 0.000000000000000000, 8.250000000000001776, -25.50000000000000355 ) ) ;
#68256=VECTOR ( 'NONE', #38853, 1000.000000000000000 ) ;
#68258=CARTESIAN_POINT ( 'NONE',  ( 7.450000000000004619, -1.336933437520057563E-15, -7.500000000000000000 ) ) ;
#68260=ORIENTED_EDGE ( 'NONE', *, *, #41042, .T. ) ;
#68264=ORIENTED_EDGE ( 'NONE', *, *, #38289, .T. ) ;
#68270=ADVANCED_FACE ( 'NONE', ( #17633 ), #6676, .F. ) ;
#68271=AXIS2_PLACEMENT_3D ( 'NONE', #14859, #47028, #69292 ) ;
#68272=EDGE_CURVE ( 'NONE', #53780, #17018, #46989, .T. ) ;
#68275=CIRCLE ( 'NONE', #12928, 1.000000000000000000 ) ;
#68277=ADVANCED_FACE ( 'NONE', ( #61443 ), #13375, .T. ) ;
#68282=VERTEX_POINT ( 'NONE', #33889 ) ;
#68286=CYLINDRICAL_SURFACE ( 'NONE', #44776, 1.000000000000000000 ) ;
#68294=LINE ( 'NONE', #57333, #18825 ) ;
#68303=ADVANCED_FACE ( 'NONE', ( #39879 ), #55477, .F. ) ;
#68310=ORIENTED_EDGE ( 'NONE', *, *, #30198, .T. ) ;
#68319=VERTEX_POINT ( 'NONE', #2416 ) ;
#68328=ORIENTED_EDGE ( 'NONE', *, *, #30627, .T. ) ;
#68348=ORIENTED_EDGE ( 'NONE', *, *, #30627, .F. ) ;
#68356=DIRECTION ( 'NONE',  ( -0.000000000000000000, -0.000000000000000000, 1.000000000000000000 ) ) ;
#68365=ORIENTED_EDGE ( 'NONE', *, *, #61914, .F. ) ;
#68366=CARTESIAN_POINT ( 'NONE',  ( 4.456444791733522252E-16, 7.450000000000002842, -13.50000000000000178 ) ) ;
#68367=ORIENTED_EDGE ( 'NONE', *, *, #22046, .T. ) ;
#68373=DIRECTION ( 'NONE',  ( 0.000000000000000000, 0.000000000000000000, 1.000000000000000000 ) ) ;
#68374=DIRECTION ( 'NONE',  ( -0.000000000000000000, -0.000000000000000000, 1.000000000000000000 ) ) ;
#68384=CARTESIAN_POINT ( 'NONE',  ( -7.750000000000001776, -7.348062532927999158, 0.000000000000000000 ) ) ;
#68387=CIRCLE ( 'NONE', #9645, 0.06000000000000102474 ) ;
#68388=CIRCLE ( 'NONE', #38017, 0.7500000000000006661 ) ;
#68400=AXIS2_PLACEMENT_3D ( 'NONE', #23561, #3058, #50439 ) ;
#68402=VECTOR ( 'NONE', #32502, 1000.000000000000000 ) ;
#68410=CARTESIAN_POINT ( 'NONE',  ( 7.750000000000001776, 7.750000000000000000, -5.000000000000000000 ) ) ;
#68411=VERTEX_POINT ( 'NONE', #36699 ) ;
#68418=CARTESIAN_POINT ( 'NONE',  ( -7.450000000000001954, 7.250000000000000000, -22.50000000000000000 ) ) ;
#68420=EDGE_CURVE ( 'NONE', #62704, #36865, #4528, .T. ) ;
#68427=CIRCLE ( 'NONE', #49258, 0.2000000000000005107 ) ;
#68435=EDGE_CURVE ( 'NONE', #60745, #51045, #43613, .T. ) ;
#68437=CARTESIAN_POINT ( 'NONE',  ( 0.000000000000000000, 0.000000000000000000, -5.000000000000000000 ) ) ;
#68447=CARTESIAN_POINT ( 'NONE',  ( 7.250000000000005329, -7.449999999999998401, -8.000000000000000000 ) ) ;
#68456=CARTESIAN_POINT ( 'NONE',  ( 7.450000000000004619, -1.336933437520057563E-15, -10.50000000000000000 ) ) ;
#68459=ORIENTED_EDGE ( 'NONE', *, *, #15952, .T. ) ;
#68464=ORIENTED_EDGE ( 'NONE', *, *, #23973, .T. ) ;
#68465=CARTESIAN_POINT ( 'NONE',  ( 7.250000000000005329, -7.249999999999998224, -20.50000000000000000 ) ) ;
#68466=CARTESIAN_POINT ( 'NONE',  ( -7.250000000000000000, -7.449999999999998401, -10.50000000000000000 ) ) ;
#68467=ORIENTED_EDGE ( 'NONE', *, *, #44828, .F. ) ;
#68487=CARTESIAN_POINT ( 'NONE',  ( -7.250000000000001776, -7.249999999999998224, -14.50000000000000000 ) ) ;
#68491=CYLINDRICAL_SURFACE ( 'NONE', #17952, 0.2000000000000005107 ) ;
#68496=CARTESIAN_POINT ( 'NONE',  ( -7.250000000000000888, -8.249999999999998224, -18.50000000000000000 ) ) ;
#68499=LINE ( 'NONE', #63182, #24868 ) ;
#68500=ORIENTED_EDGE ( 'NONE', *, *, #38950, .F. ) ;
#68517=ORIENTED_EDGE ( 'NONE', *, *, #27802, .F. ) ;
#68535=ORIENTED_EDGE ( 'NONE', *, *, #37772, .T. ) ;
#68546=DIRECTION ( 'NONE',  ( -0.000000000000000000, -0.000000000000000000, 1.000000000000000000 ) ) ;
#68549=ORIENTED_EDGE ( 'NONE', *, *, #44214, .T. ) ;
#68552=CARTESIAN_POINT ( 'NONE',  ( 0.000000000000000000, 8.250000000000001776, -8.000000000000000000 ) ) ;
#68555=VECTOR ( 'NONE', #37083, 1000.000000000000000 ) ;
#68558=ORIENTED_EDGE ( 'NONE', *, *, #56429, .T. ) ;
#68559=CIRCLE ( 'NONE', #65241, 0.1999999999999987899 ) ;
#68564=VERTEX_POINT ( 'NONE', #11210 ) ;
#68565=DIRECTION ( 'NONE',  ( 1.000000000000000000, 0.000000000000000000, 0.000000000000000000 ) ) ;
#68578=AXIS2_PLACEMENT_3D ( 'NONE', #47001, #24737, #52310 ) ;
#68583=CARTESIAN_POINT ( 'NONE',  ( 8.250000000000005329, -7.249999999999998224, -26.00000000000001066 ) ) ;
#68595=VERTEX_POINT ( 'NONE', #21824 ) ;
#68599=ORIENTED_EDGE ( 'NONE', *, *, #65490, .F. ) ;
#68604=EDGE_CURVE ( 'NONE', #39010, #13815, #970, .T. ) ;
#68605=CARTESIAN_POINT ( 'NONE',  ( -7.250000000000000888, 7.250000000000001776, -17.50000000000000000 ) ) ;
#68607=EDGE_LOOP ( 'NONE', ( #14506, #60674, #63481, #43084, #2749, #13741, #44665, #18578 ) ) ;
#68610=ORIENTED_EDGE ( 'NONE', *, *, #38901, .F. ) ;
#68613=CARTESIAN_POINT ( 'NONE',  ( 7.450000000000004619, -1.336933437520057563E-15, -25.00000000000000000 ) ) ;
#68615=LINE ( 'NONE', #68252, #55824 ) ;
#68618=DIRECTION ( 'NONE',  ( -0.000000000000000000, -0.000000000000000000, -1.000000000000000000 ) ) ;
#68619=CARTESIAN_POINT ( 'NONE',  ( -7.450000000000001954, -7.249999999999998224, -18.50000000000000000 ) ) ;
#68620=CARTESIAN_POINT ( 'NONE',  ( -7.250000000000000888, -8.249999999999998224, -20.50000000000000000 ) ) ;
#68629=DIRECTION ( 'NONE',  ( 0.000000000000000000, 1.000000000000000000, 0.000000000000000000 ) ) ;
#68636=ORIENTED_EDGE ( 'NONE', *, *, #65106, .T. ) ;
#68638=LINE ( 'NONE', #37168, #51131 ) ;
#68654=FACE_OUTER_BOUND ( 'NONE', #17360, .T. ) ;
#68655=CARTESIAN_POINT ( 'NONE',  ( -7.250000000000000888, 7.450000000000003730, -15.50000000000000000 ) ) ;
#68657=LINE ( 'NONE', #3244, #38474 ) ;
#68658=CYLINDRICAL_SURFACE ( 'NONE', #11212, 1.000000000000000000 ) ;
#68668=EDGE_CURVE ( 'NONE', #55879, #37116, #40262, .T. ) ;
#68687=DIRECTION ( 'NONE',  ( -0.000000000000000000, -0.000000000000000000, -1.000000000000000000 ) ) ;
#68689=ADVANCED_FACE ( 'NONE', ( #1299 ), #39122, .F. ) ;
#68690=ADVANCED_FACE ( 'NONE', ( #13291 ), #34496, .F. ) ;
#68691=CARTESIAN_POINT ( 'NONE',  ( -7.250000000000000888, 7.250000000000001776, -8.000000000000000000 ) ) ;
#68699=VECTOR ( 'NONE', #20500, 1000.000000000000000 ) ;
#68700=FACE_OUTER_BOUND ( 'NONE', #12166, .T. ) ;
#68703=DIRECTION ( 'NONE',  ( -0.000000000000000000, -0.000000000000000000, 1.000000000000000000 ) ) ;
#68708=CARTESIAN_POINT ( 'NONE',  ( -7.250000000000000000, -7.449999999999998401, -25.50000000000000355 ) ) ;
#68716=ADVANCED_FACE ( 'NONE', ( #13638, #8327 ), #28501, .F. ) ;
#68717=AXIS2_PLACEMENT_3D ( 'NONE', #51338, #4923, #8545 ) ;
#68733=DIRECTION ( 'NONE',  ( -1.000000000000000000, 0.000000000000000000, 0.000000000000000000 ) ) ;
#68756=CARTESIAN_POINT ( 'NONE',  ( 0.000000000000000000, -7.449999999999998401, -22.50000000000000000 ) ) ;
#68760=CARTESIAN_POINT ( 'NONE',  ( -7.450000000000001954, -7.249999999999998224, -20.00000000000000000 ) ) ;
#68763=FACE_OUTER_BOUND ( 'NONE', #34585, .T. ) ;
#68765=ORIENTED_EDGE ( 'NONE', *, *, #17177, .T. ) ;
#68768=DIRECTION ( 'NONE',  ( -0.000000000000000000, -0.000000000000000000, -1.000000000000000000 ) ) ;
#68780=DIRECTION ( 'NONE',  ( 0.000000000000000000, 0.000000000000000000, 1.000000000000000000 ) ) ;
#68782=ORIENTED_EDGE ( 'NONE', *, *, #10877, .F. ) ;
#68790=EDGE_CURVE ( 'NONE', #53780, #8234, #24612, .T. ) ;
#68805=VECTOR ( 'NONE', #20738, 1000.000000000000000 ) ;
#68812=CIRCLE ( 'NONE', #25924, 1.000000000000002665 ) ;
#68816=ADVANCED_FACE ( 'NONE', ( #62413 ), #4101, .F. ) ;
#68821=CARTESIAN_POINT ( 'NONE',  ( 8.250000000000005329, -8.249999999999998224, -26.00000000000001066 ) ) ;
#68822=DIRECTION ( 'NONE',  ( 0.000000000000000000, 1.000000000000000000, -0.000000000000000000 ) ) ;
#68830=ORIENTED_EDGE ( 'NONE', *, *, #50884, .F. ) ;
#68847=DIRECTION ( 'NONE',  ( 1.000000000000000000, -5.981805089575194965E-17, 0.000000000000000000 ) ) ;
#68848=CARTESIAN_POINT ( 'NONE',  ( 8.250000000000005329, 7.250000000000000888, -26.00000000000001066 ) ) ;
#68856=LINE ( 'NONE', #14760, #56400 ) ;
#68858=ORIENTED_EDGE ( 'NONE', *, *, #4360, .T. ) ;
#68885=CARTESIAN_POINT ( 'NONE',  ( 9.690000000000001279, -9.690000000000001279, 0.000000000000000000 ) ) ;
#68890=DIRECTION ( 'NONE',  ( -0.000000000000000000, -0.000000000000000000, 1.000000000000000000 ) ) ;
#68894=EDGE_LOOP ( 'NONE', ( #62738, #55534, #2430, #36966, #63125, #50503, #11505, #62953 ) ) ;
#68896=CARTESIAN_POINT ( 'NONE',  ( -7.250000000000000888, 7.250000000000001776, -21.50000000000000000 ) ) ;
#68908=ORIENTED_EDGE ( 'NONE', *, *, #40706, .T. ) ;
#68910=VECTOR ( 'NONE', #14198, 1000.000000000000000 ) ;
#68914=FACE_OUTER_BOUND ( 'NONE', #63408, .T. ) ;
#68916=ORIENTED_EDGE ( 'NONE', *, *, #8343, .F. ) ;
#68921=ORIENTED_EDGE ( 'NONE', *, *, #51496, .F. ) ;
#68929=CARTESIAN_POINT ( 'NONE',  ( -7.250000000000001776, -7.249999999999998224, -16.50000000000000000 ) ) ;
#68935=LINE ( 'NONE', #41705, #28253 ) ;
#68936=CIRCLE ( 'NONE', #28288, 0.2000000000000005107 ) ;
#68938=EDGE_CURVE ( 'NONE', #52946, #55726, #35719, .T. ) ;
#68939=VECTOR ( 'NONE', #4843, 1000.000000000000000 ) ;
#68943=ORIENTED_EDGE ( 'NONE', *, *, #65382, .F. ) ;
#68944=ORIENTED_EDGE ( 'NONE', *, *, #2016, .T. ) ;
#68946=LINE ( 'NONE', #4603, #22410 ) ;
#68951=ORIENTED_EDGE ( 'NONE', *, *, #52267, .F. ) ;
#68958=VERTEX_POINT ( 'NONE', #40678 ) ;
#68969=EDGE_CURVE ( 'NONE', #15601, #54166, #56587, .T. ) ;
#68972=VERTEX_POINT ( 'NONE', #19110 ) ;
#68973=CARTESIAN_POINT ( 'NONE',  ( 8.250000000000005329, -7.249999999999998224, -26.00000000000001066 ) ) ;
#68976=VERTEX_POINT ( 'NONE', #29707 ) ;
#68988=ORIENTED_EDGE ( 'NONE', *, *, #20451, .F. ) ;
#68991=LINE ( 'NONE', #41760, #3620 ) ;
#68999=EDGE_CURVE ( 'NONE', #9824, #32145, #13453, .T. ) ;
#69008=EDGE_CURVE ( 'NONE', #9016, #16443, #27915, .T. ) ;
#69013=CARTESIAN_POINT ( 'NONE',  ( -7.250000000000000888, 7.250000000000001776, -20.50000000000000000 ) ) ;
#69015=EDGE_CURVE ( 'NONE', #61156, #35196, #18760, .T. ) ;
#69019=DIRECTION ( 'NONE',  ( -1.000000000000000000, 0.000000000000000000, 0.000000000000000000 ) ) ;
#69026=FACE_OUTER_BOUND ( 'NONE', #4527, .T. ) ;
#69029=CIRCLE ( 'NONE', #66737, 0.8100000000000017186 ) ;
#69038=DIRECTION ( 'NONE',  ( 0.000000000000000000, -1.000000000000000000, -0.000000000000000000 ) ) ;
#69044=VECTOR ( 'NONE', #31907, 1000.000000000000000 ) ;
#69049=VECTOR ( 'NONE', #2929, 1000.000000000000000 ) ;
#69053=ORIENTED_EDGE ( 'NONE', *, *, #46098, .F. ) ;
#69054=VECTOR ( 'NONE', #29765, 1000.000000000000000 ) ;
#69058=LINE ( 'NONE', #46438, #19819 ) ;
#69059=ORIENTED_EDGE ( 'NONE', *, *, #52975, .T. ) ;
#69066=CARTESIAN_POINT ( 'NONE',  ( 0.000000000000000000, 0.000000000000000000, -13.00000000000000178 ) ) ;
#69073=DIRECTION ( 'NONE',  ( 0.000000000000000000, 0.000000000000000000, 1.000000000000000000 ) ) ;
#69080=VECTOR ( 'NONE', #740, 1000.000000000000000 ) ;
#69088=EDGE_CURVE ( 'NONE', #34803, #49703, #343, .T. ) ;
#69098=DIRECTION ( 'NONE',  ( -0.000000000000000000, -0.000000000000000000, 1.000000000000000000 ) ) ;
#69099=CIRCLE ( 'NONE', #67933, 1.000000000000000000 ) ;
#69104=CARTESIAN_POINT ( 'NONE',  ( -7.250000000000000888, 8.250000000000001776, -10.50000000000000000 ) ) ;
#69113=CARTESIAN_POINT ( 'NONE',  ( 7.250000000000005329, 8.250000000000001776, -26.00000000000001066 ) ) ;
#69121=PLANE ( 'NONE',  #56767 ) ;
#69123=DIRECTION ( 'NONE',  ( 0.000000000000000000, 0.000000000000000000, -1.000000000000000000 ) ) ;
#69124=DIRECTION ( 'NONE',  ( 0.000000000000000000, 0.000000000000000000, 1.000000000000000000 ) ) ;
#69140=ADVANCED_FACE ( 'NONE', ( #43118 ), #16250, .T. ) ;
#69141=VERTEX_POINT ( 'NONE', #48784 ) ;
#69142=VECTOR ( 'NONE', #50329, 1000.000000000000000 ) ;
#69154=ORIENTED_EDGE ( 'NONE', *, *, #39438, .F. ) ;
#69175=ORIENTED_EDGE ( 'NONE', *, *, #24696, .F. ) ;
#69178=VECTOR ( 'NONE', #28798, 1000.000000000000000 ) ;
#69189=ORIENTED_EDGE ( 'NONE', *, *, #14629, .F. ) ;
#69193=DIRECTION ( 'NONE',  ( -1.000000000000000000, 0.000000000000000000, 0.000000000000000000 ) ) ;
#69195=CARTESIAN_POINT ( 'NONE',  ( -7.250000000000001776, -7.249999999999998224, -21.50000000000000000 ) ) ;
#69197=VECTOR ( 'NONE', #53567, 1000.000000000000000 ) ;
#69204=AXIS2_PLACEMENT_3D ( 'NONE', #57356, #57704, #30837 ) ;
#69205=LINE ( 'NONE', #4517, #9280 ) ;
#69209=CIRCLE ( 'NONE', #17263, 0.9999999999999991118 ) ;
#69211=DIRECTION ( 'NONE',  ( -1.000000000000000000, 0.000000000000000000, 0.000000000000000000 ) ) ;
#69217=VERTEX_POINT ( 'NONE', #17629 ) ;
#69219=EDGE_CURVE ( 'NONE', #7880, #9481, #22599, .T. ) ;
#69220=DIRECTION ( 'NONE',  ( 1.000000000000000000, 0.000000000000000000, 0.000000000000000000 ) ) ;
#69230=EDGE_CURVE ( 'NONE', #40458, #67314, #12653, .T. ) ;
#69232=LINE ( 'NONE', #69588, #43493 ) ;
#69235=VERTEX_POINT ( 'NONE', #17284 ) ;
#69241=DIRECTION ( 'NONE',  ( 0.000000000000000000, 1.000000000000000000, -0.000000000000000000 ) ) ;
#69246=VERTEX_POINT ( 'NONE', #5993 ) ;
#69254=AXIS2_PLACEMENT_3D ( 'NONE', #24397, #40999, #34993 ) ;
#69256=AXIS2_PLACEMENT_3D ( 'NONE', #43799, #1688, #6318 ) ;
#69257=LINE ( 'NONE', #26475, #4786 ) ;
#69260=DIRECTION ( 'NONE',  ( 0.000000000000000000, -0.000000000000000000, 1.000000000000000000 ) ) ;
#69267=LINE ( 'NONE', #54059, #59353 ) ;
#69268=ORIENTED_EDGE ( 'NONE', *, *, #45257, .T. ) ;
#69283=PLANE ( 'NONE',  #30742 ) ;
#69289=AXIS2_PLACEMENT_3D ( 'NONE', #39765, #34454, #18555 ) ;
#69291=PLANE ( 'NONE',  #50159 ) ;
#69292=DIRECTION ( 'NONE',  ( -1.000000000000000000, 0.000000000000000000, 0.000000000000000000 ) ) ;
#69295=DIRECTION ( 'NONE',  ( -0.000000000000000000, -0.000000000000000000, 1.000000000000000000 ) ) ;
#69299=LINE ( 'NONE', #36790, #43989 ) ;
#69303=FACE_OUTER_BOUND ( 'NONE', #41209, .T. ) ;
#69307=CARTESIAN_POINT ( 'NONE',  ( 4.456444791733522252E-16, 7.450000000000002842, -23.50000000000000000 ) ) ;
#69318=LINE ( 'NONE', #16632, #14117 ) ;
#69319=CARTESIAN_POINT ( 'NONE',  ( 4.456444791733522252E-16, 7.450000000000002842, -7.500000000000000000 ) ) ;
#69320=EDGE_CURVE ( 'NONE', #56954, #11793, #40933, .T. ) ;
#69322=PLANE ( 'NONE',  #5317 ) ;
#69328=LINE ( 'NONE', #53779, #63280 ) ;
#69330=DIRECTION ( 'NONE',  ( 0.000000000000000000, -0.000000000000000000, 1.000000000000000000 ) ) ;
#69336=ORIENTED_EDGE ( 'NONE', *, *, #30821, .T. ) ;
#69358=AXIS2_PLACEMENT_3D ( 'NONE', #29846, #63791, #19592 ) ;
#69371=EDGE_LOOP ( 'NONE', ( #16756, #28782, #69421, #610 ) ) ;
#69372=AXIS2_PLACEMENT_3D ( 'NONE', #56594, #67567, #13459 ) ;
#69379=FACE_OUTER_BOUND ( 'NONE', #30189, .T. ) ;
#69380=VERTEX_POINT ( 'NONE', #46942 ) ;
#69381=VERTEX_POINT ( 'NONE', #29266 ) ;
#69383=CARTESIAN_POINT ( 'NONE',  ( -7.250000000000000000, -7.449999999999998401, -24.50000000000000000 ) ) ;
#69398=VECTOR ( 'NONE', #55365, 1000.000000000000000 ) ;
#69399=VECTOR ( 'NONE', #3651, 1000.000000000000000 ) ;
#69405=ORIENTED_EDGE ( 'NONE', *, *, #12868, .F. ) ;
#69408=AXIS2_PLACEMENT_3D ( 'NONE', #22274, #5999, #39209 ) ;
#69411=EDGE_CURVE ( 'NONE', #56437, #34317, #57205, .T. ) ;
#69412=CARTESIAN_POINT ( 'NONE',  ( -7.250000000000000888, 7.450000000000003730, -24.50000000000000000 ) ) ;
#69417=EDGE_CURVE ( 'NONE', #43147, #55829, #34578, .T. ) ;
#69420=ADVANCED_FACE ( 'NONE', ( #45533 ), #61437, .T. ) ;
#69421=ORIENTED_EDGE ( 'NONE', *, *, #1229, .F. ) ;
#69422=AXIS2_PLACEMENT_3D ( 'NONE', #20819, #58664, #10219 ) ;
#69423=LINE ( 'NONE', #36539, #32978 ) ;
#69424=CARTESIAN_POINT ( 'NONE',  ( -7.250000000000001776, -7.249999999999998224, -25.00000000000000000 ) ) ;
#69436=ORIENTED_EDGE ( 'NONE', *, *, #23183, .F. ) ;
#69448=LINE ( 'NONE', #57087, #66561 ) ;
#69454=LINE ( 'NONE', #36224, #20661 ) ;
#69456=AXIS2_PLACEMENT_3D ( 'NONE', #43294, #69123, #21384 ) ;
#69467=ORIENTED_EDGE ( 'NONE', *, *, #23263, .T. ) ;
#69471=CARTESIAN_POINT ( 'NONE',  ( 7.250000000000005329, -7.449999999999998401, -10.50000000000000000 ) ) ;
#69477=ORIENTED_EDGE ( 'NONE', *, *, #44624, .F. ) ;
#69481=DIRECTION ( 'NONE',  ( -1.000000000000000000, 0.000000000000000000, 0.000000000000000000 ) ) ;
#69482=DIRECTION ( 'NONE',  ( 0.000000000000000000, -0.000000000000000000, 1.000000000000000000 ) ) ;
#69494=EDGE_CURVE ( 'NONE', #55788, #13160, #59613, .T. ) ;
#69501=CIRCLE ( 'NONE', #50303, 0.8100000000000017186 ) ;
#69502=LINE ( 'NONE', #31686, #55489 ) ;
#69503=CARTESIAN_POINT ( 'NONE',  ( 8.250000000000005329, 0.000000000000000000, -10.00000000000000000 ) ) ;
#69506=VECTOR ( 'NONE', #19019, 1000.000000000000000 ) ;
#69515=DIRECTION ( 'NONE',  ( 1.000000000000000000, 0.000000000000000000, 0.000000000000000000 ) ) ;
#69517=ORIENTED_EDGE ( 'NONE', *, *, #34497, .F. ) ;
#69520=CARTESIAN_POINT ( 'NONE',  ( -9.690000000000001279, 9.690000000000001279, -5.000000000000000000 ) ) ;
#69531=EDGE_LOOP ( 'NONE', ( #62604, #38518, #6591, #42628 ) ) ;
#69534=FACE_BOUND ( 'NONE', #48611, .T. ) ;
#69536=LINE ( 'NONE', #21100, #50452 ) ;
#69546=CARTESIAN_POINT ( 'NONE',  ( 7.450000000000004619, -1.336933437520057563E-15, -15.00000000000000000 ) ) ;
#69549=ORIENTED_EDGE ( 'NONE', *, *, #28184, .F. ) ;
#69557=ORIENTED_EDGE ( 'NONE', *, *, #31379, .T. ) ;
#69561=VECTOR ( 'NONE', #53312, 1000.000000000000000 ) ;
#69563=DIRECTION ( 'NONE',  ( 0.000000000000000000, 1.000000000000000000, 0.000000000000000000 ) ) ;
#69565=ORIENTED_EDGE ( 'NONE', *, *, #2112, .F. ) ;
#69567=EDGE_CURVE ( 'NONE', #20448, #61277, #47999, .T. ) ;
#69570=VERTEX_POINT ( 'NONE', #14776 ) ;
#69577=DIRECTION ( 'NONE',  ( -1.000000000000000000, 0.000000000000000000, 0.000000000000000000 ) ) ;
#69578=DIRECTION ( 'NONE',  ( 0.000000000000000000, 0.000000000000000000, -1.000000000000000000 ) ) ;
#69585=ORIENTED_EDGE ( 'NONE', *, *, #46867, .F. ) ;
#69586=ORIENTED_EDGE ( 'NONE', *, *, #61914, .T. ) ;
#69588=CARTESIAN_POINT ( 'NONE',  ( 7.250000000000005329, -8.249999999999998224, -26.00000000000001066 ) ) ;
#69595=EDGE_LOOP ( 'NONE', ( #68636, #68951, #68464, #45606 ) ) ;
#69600=ORIENTED_EDGE ( 'NONE', *, *, #26374, .F. ) ;
#69606=VECTOR ( 'NONE', #49590, 1000.000000000000000 ) ;
#69608=AXIS2_PLACEMENT_3D ( 'NONE', #2088, #38874, #56186 ) ;
#69619=DIRECTION ( 'NONE',  ( 0.000000000000000000, 0.000000000000000000, 1.000000000000000000 ) ) ;
#69622=ORIENTED_EDGE ( 'NONE', *, *, #37311, .T. ) ;
#69623=FACE_OUTER_BOUND ( 'NONE', #9997, .T. ) ;
#69625=CARTESIAN_POINT ( 'NONE',  ( 7.250000000000005329, 7.250000000000000888, -10.00000000000000000 ) ) ;
#69626=EDGE_CURVE ( 'NONE', #40971, #11123, #888, .T. ) ;
#69630=CIRCLE ( 'NONE', #39119, 1.000000000000000000 ) ;
#69639=PLANE ( 'NONE',  #30573 ) ;
#69647=ORIENTED_EDGE ( 'NONE', *, *, #37315, .T. ) ;
#69653=DIRECTION ( 'NONE',  ( -1.000000000000000000, 0.000000000000000000, 0.000000000000000000 ) ) ;
#69655=EDGE_CURVE ( 'NONE', #69570, #11380, #34140, .T. ) ;
#69656=CARTESIAN_POINT ( 'NONE',  ( -7.250000000000000888, -8.249999999999998224, -19.50000000000000000 ) ) ;
#69681=LINE ( 'NONE', #48449, #37809 ) ;
#69685=DIRECTION ( 'NONE',  ( -0.000000000000000000, 0.000000000000000000, 1.000000000000000000 ) ) ;
#69688=DIRECTION ( 'NONE',  ( -1.000000000000000000, 0.000000000000000000, -0.000000000000000000 ) ) ;
#69728=FACE_OUTER_BOUND ( 'NONE', #61185, .T. ) ;
#69735=EDGE_LOOP ( 'NONE', ( #67123, #35962, #17672, #54053 ) ) ;
#69741=VERTEX_POINT ( 'NONE', #49044 ) ;
#69753=ORIENTED_EDGE ( 'NONE', *, *, #50614, .T. ) ;
#69756=VERTEX_POINT ( 'NONE', #5910 ) ;
#69769=EDGE_CURVE ( 'NONE', #49703, #2734, #12149, .T. ) ;
#69770=CARTESIAN_POINT ( 'NONE',  ( 7.250000000000004441, 8.750000000000001776, -26.00000000000001066 ) ) ;
#69781=CARTESIAN_POINT ( 'NONE',  ( -7.450000000000001954, 0.000000000000000000, -19.00000000000000000 ) ) ;
#69783=AXIS2_PLACEMENT_3D ( 'NONE', #50107, #51513, #28879 ) ;
#69787=EDGE_LOOP ( 'NONE', ( #53070, #65822, #23776, #20224 ) ) ;
#69788=CARTESIAN_POINT ( 'NONE',  ( 8.250000000000005329, 7.250000000000000888, -18.50000000000000000 ) ) ;
#69793=EDGE_LOOP ( 'NONE', ( #2994, #14067, #27300, #38781 ) ) ;
#69803=EDGE_CURVE ( 'NONE', #5400, #25235, #35911, .T. ) ;
#69809=DIRECTION ( 'NONE',  ( -1.000000000000000000, 0.000000000000000000, 0.000000000000000000 ) ) ;
#69812=AXIS2_PLACEMENT_3D ( 'NONE', #29283, #67836, #19386 ) ;
#69814=AXIS2_PLACEMENT_3D ( 'NONE', #10436, #69482, #20345 ) ;
#69815=CARTESIAN_POINT ( 'NONE',  ( 7.750000000000001776, 7.750000000000000000, 5.000000000000000000 ) ) ;
#69816=ORIENTED_EDGE ( 'NONE', *, *, #64350, .F. ) ;
#69819=LINE ( 'NONE', #17102, #3532 ) ;
#69835=CARTESIAN_POINT ( 'NONE',  ( 7.250000000000005329, -8.249999999999998224, -12.00000000000000000 ) ) ;
#69849=LINE ( 'NONE', #15063, #63912 ) ;
#69851=LINE ( 'NONE', #21067, #52767 ) ;
#69853=CIRCLE ( 'NONE', #41630, 1.000000000000003553 ) ;
#69858=VERTEX_POINT ( 'NONE', #62409 ) ;
#69859=CARTESIAN_POINT ( 'NONE',  ( -7.250000000000000888, 7.250000000000001776, -25.50000000000000355 ) ) ;
#69861=FACE_OUTER_BOUND ( 'NONE', #18616, .T. ) ;
#69862=CARTESIAN_POINT ( 'NONE',  ( -7.250000000000000888, 7.450000000000003730, -18.50000000000000000 ) ) ;
#69864=DIRECTION ( 'NONE',  ( -0.000000000000000000, -0.000000000000000000, -1.000000000000000000 ) ) ;
#69872=ADVANCED_FACE ( 'NONE', ( #45451, #13634 ), #50427, .F. ) ;
#69883=EDGE_CURVE ( 'NONE', #67695, #6090, #46506, .T. ) ;
#69884=CARTESIAN_POINT ( 'NONE',  ( 7.250000000000005329, -7.249999999999998224, -25.00000000000000000 ) ) ;
#69885=ADVANCED_FACE ( 'NONE', ( #68081 ), #19633, .T. ) ;
#69886=AXIS2_PLACEMENT_3D ( 'NONE', #9030, #41562, #4788 ) ;
#69890=CARTESIAN_POINT ( 'NONE',  ( -7.250000000000000888, 7.250000000000001776, -26.00000000000001066 ) ) ;
#69911=DIRECTION ( 'NONE',  ( 0.000000000000000000, 0.000000000000000000, 1.000000000000000000 ) ) ;
#69917=DIRECTION ( 'NONE',  ( -1.000000000000000000, 0.000000000000000000, 0.000000000000000000 ) ) ;
#69920=VERTEX_POINT ( 'NONE', #69835 ) ;
#69923=CARTESIAN_POINT ( 'NONE',  ( -8.250000000000001776, -7.249999999999998224, -26.00000000000001066 ) ) ;
#69924=FACE_OUTER_BOUND ( 'NONE', #27361, .T. ) ;
#69925=ORIENTED_EDGE ( 'NONE', *, *, #38901, .T. ) ;
#69927=DIRECTION ( 'NONE',  ( 1.000000000000000000, -0.000000000000000000, -0.000000000000000000 ) ) ;
#69935=CARTESIAN_POINT ( 'NONE',  ( -7.250000000000000888, 7.450000000000003730, -17.00000000000000000 ) ) ;
#69943=CARTESIAN_POINT ( 'NONE',  ( 7.250000000000005329, 8.250000000000001776, -21.50000000000000000 ) ) ;
#69951=CARTESIAN_POINT ( 'NONE',  ( 7.250000000000005329, -7.249999999999998224, -15.50000000000000000 ) ) ;
#69956=DIRECTION ( 'NONE',  ( -1.000000000000000000, 0.000000000000000000, 0.000000000000000000 ) ) ;
#69962=AXIS2_PLACEMENT_3D ( 'NONE', #22141, #60656, #43707 ) ;
#69969=ADVANCED_FACE ( 'NONE', ( #4095 ), #47228, .T. ) ;
#69978=DIRECTION ( 'NONE',  ( 1.000000000000000000, 0.000000000000000000, 0.000000000000000000 ) ) ;
#69979=ADVANCED_FACE ( 'NONE', ( #53242 ), #4789, .T. ) ;
#69980=DIRECTION ( 'NONE',  ( 0.000000000000000000, 1.000000000000000000, 0.000000000000000000 ) ) ;
ENDSEC;
END-ISO-10303-21;
